ISO-10303-21;
HEADER;
FILE_DESCRIPTION (('STEP AP214'),
    '1' );
FILE_NAME ('Pneumatic Cylinder Piston.step',
    '2026-10-09T17:48:21',
    ( '' ),
    ( '' ),
    'SwSTEP 2.0',
    'SolidWorks 2024',
    '' );
FILE_SCHEMA (( 'AUTOMOTIVE_DESIGN' ));
ENDSEC;

DATA;
#1=ORIENTED_EDGE ( 'NONE', *, *, #1535, .F. ) ;
#2=ORIENTED_EDGE ( 'NONE', *, *, #10952, .T. ) ;
#7=DIRECTION ( 'NONE',  ( -1.000000000000000000, 0.000000000000000000, 0.000000000000000000 ) ) ;
#8=FACE_OUTER_BOUND ( 'NONE', #14235, .T. ) ;
#11=CARTESIAN_POINT ( 'NONE',  ( -48.27438362644000591, 99.17411849586700612, -145.4984795835769660 ) ) ;
#13=DIRECTION ( 'NONE',  ( 0.8660254037844381525, 1.060575238724905436E-16, -0.5000000000000007772 ) ) ;
#14=EDGE_LOOP ( 'NONE', ( #11433, #3957, #4882, #12655, #13949, #5070, #15047, #7038 ) ) ;
#15=DIRECTION ( 'NONE',  ( 0.000000000000000000, 0.000000000000000000, 1.000000000000000000 ) ) ;
#16=VERTEX_POINT ( 'NONE', #1531 ) ;
#17=EDGE_LOOP ( 'NONE', ( #15211, #10608 ) ) ;
#23=DIRECTION ( 'NONE',  ( 0.000000000000000000, 0.000000000000000000, -1.000000000000000000 ) ) ;
#25=CIRCLE ( 'NONE', #1757, 2.000000000000001776 ) ;
#27=EDGE_CURVE ( 'NONE', #14843, #4755, #2589, .T. ) ;
#28=CARTESIAN_POINT ( 'NONE',  ( -69.77438362644001302, 82.17411849586700612, -29.37106258560738681 ) ) ;
#29=ORIENTED_EDGE ( 'NONE', *, *, #8974, .F. ) ;
#33=ADVANCED_FACE ( 'NONE', ( #6140 ), #1221, .T. ) ;
#35=AXIS2_PLACEMENT_3D ( 'NONE', #11187, #8790, #2898 ) ;
#38=VECTOR ( 'NONE', #447, 1000.000000000000114 ) ;
#40=EDGE_CURVE ( 'NONE', #11360, #1952, #11269, .T. ) ;
#43=AXIS2_PLACEMENT_3D ( 'NONE', #8460, #2484, #4677 ) ;
#44=LINE ( 'NONE', #15319, #14958 ) ;
#45=EDGE_CURVE ( 'NONE', #7802, #1067, #10681, .T. ) ;
#52=FACE_OUTER_BOUND ( 'NONE', #854, .T. ) ;
#61=CARTESIAN_POINT ( 'NONE',  ( -52.77438362643999881, 65.17411849586700612, -149.9984795835770228 ) ) ;
#62=DIRECTION ( 'NONE',  ( 0.000000000000000000, 0.000000000000000000, -1.000000000000000000 ) ) ;
#65=CARTESIAN_POINT ( 'NONE',  ( -96.77438362643999881, 110.1741184958670061, -15.85886927678779834 ) ) ;
#68=DIRECTION ( 'NONE',  ( -1.000000000000000000, 0.000000000000000000, 0.000000000000000000 ) ) ;
#72=ORIENTED_EDGE ( 'NONE', *, *, #1086, .F. ) ;
#73=EDGE_LOOP ( 'NONE', ( #5706, #14466 ) ) ;
#78=VECTOR ( 'NONE', #4596, 1000.000000000000000 ) ;
#79=CARTESIAN_POINT ( 'NONE',  ( -66.41143315690761995, 66.60412428008086749, -81.84847958357697451 ) ) ;
#84=DIRECTION ( 'NONE',  ( 0.000000000000000000, 0.000000000000000000, -1.000000000000000000 ) ) ;
#86=CARTESIAN_POINT ( 'NONE',  ( -52.77438362644100067, 101.5320169952374414, -147.9984795835769944 ) ) ;
#87=AXIS2_PLACEMENT_3D ( 'NONE', #15229, #11833, #9343 ) ;
#88=ORIENTED_EDGE ( 'NONE', *, *, #3312, .F. ) ;
#90=ADVANCED_FACE ( 'NONE', ( #3635 ), #13178, .F. ) ;
#92=ORIENTED_EDGE ( 'NONE', *, *, #11605, .T. ) ;
#99=PLANE ( 'NONE',  #8327 ) ;
#102=AXIS2_PLACEMENT_3D ( 'NONE', #7303, #5128, #12107 ) ;
#103=ADVANCED_FACE ( 'NONE', ( #4721 ), #2539, .F. ) ;
#105=CARTESIAN_POINT ( 'NONE',  ( -55.27438362644100067, 99.17411849586700612, -145.2984795835770058 ) ) ;
#106=ORIENTED_EDGE ( 'NONE', *, *, #3872, .T. ) ;
#107=CARTESIAN_POINT ( 'NONE',  ( -89.52438362644001302, 99.17411849586700612, -86.49847958357699440 ) ) ;
#108=ADVANCED_FACE ( 'NONE', ( #11856, #8368 ), #12015, .T. ) ;
#110=ORIENTED_EDGE ( 'NONE', *, *, #7891, .F. ) ;
#113=ORIENTED_EDGE ( 'NONE', *, *, #13222, .F. ) ;
#116=AXIS2_PLACEMENT_3D ( 'NONE', #9604, #4733, #11793 ) ;
#121=FACE_OUTER_BOUND ( 'NONE', #4343, .T. ) ;
#124=CIRCLE ( 'NONE', #5857, 3.750000000000003553 ) ;
#128=AXIS2_PLACEMENT_3D ( 'NONE', #1233, #11714, #2169 ) ;
#133=EDGE_LOOP ( 'NONE', ( #9596, #14625, #7458, #244 ) ) ;
#135=ORIENTED_EDGE ( 'NONE', *, *, #4809, .F. ) ;
#136=EDGE_CURVE ( 'NONE', #3919, #16, #2769, .T. ) ;
#140=AXIS2_PLACEMENT_3D ( 'NONE', #12539, #11367, #14918 ) ;
#143=EDGE_CURVE ( 'NONE', #10494, #8073, #2934, .T. ) ;
#144=CARTESIAN_POINT ( 'NONE',  ( -52.77438362643999881, 67.53201699523744139, -147.9984795835769944 ) ) ;
#149=EDGE_CURVE ( 'NONE', #14279, #1795, #4826, .T. ) ;
#152=ORIENTED_EDGE ( 'NONE', *, *, #14283, .F. ) ;
#153=CARTESIAN_POINT ( 'NONE',  ( -86.77438362643999881, 67.53201699523744139, -150.4984795835770228 ) ) ;
#156=CIRCLE ( 'NONE', #9319, 2.750000000000002665 ) ;
#158=EDGE_LOOP ( 'NONE', ( #13988, #8666, #2521, #1723 ) ) ;
#161=( NAMED_UNIT ( * ) SI_UNIT ( $, .STERADIAN. ) SOLID_ANGLE_UNIT ( ) );
#166=DIRECTION ( 'NONE',  ( 0.000000000000000000, -0.000000000000000000, 1.000000000000000000 ) ) ;
#170=FACE_OUTER_BOUND ( 'NONE', #13767, .T. ) ;
#171=CARTESIAN_POINT ( 'NONE',  ( -86.77438362644100778, 101.5320169952374414, -147.9984795835769944 ) ) ;
#172=CARTESIAN_POINT ( 'NONE',  ( -86.77438362644100778, 96.81621999649657084, -150.4984795835770228 ) ) ;
#173=FACE_OUTER_BOUND ( 'NONE', #7801, .T. ) ;
#174=ORIENTED_EDGE ( 'NONE', *, *, #12843, .T. ) ;
#176=EDGE_LOOP ( 'NONE', ( #13806, #13422, #10645, #9844 ) ) ;
#177=EDGE_LOOP ( 'NONE', ( #7583, #9630, #5793, #14257 ) ) ;
#179=AXIS2_PLACEMENT_3D ( 'NONE', #10567, #13983, #7013 ) ;
#184=CARTESIAN_POINT ( 'NONE',  ( -89.27438362644100778, 99.17411849586700612, -182.2484795835770228 ) ) ;
#187=FACE_OUTER_BOUND ( 'NONE', #12629, .T. ) ;
#191=VERTEX_POINT ( 'NONE', #7522 ) ;
#193=ORIENTED_EDGE ( 'NONE', *, *, #14265, .T. ) ;
#195=CIRCLE ( 'NONE', #7158, 5.500000000000005329 ) ;
#197=EDGE_CURVE ( 'NONE', #3708, #3101, #10343, .T. ) ;
#201=CARTESIAN_POINT ( 'NONE',  ( -88.81638362644000040, 63.99516924618178848, -147.9984795835769944 ) ) ;
#202=CARTESIAN_POINT ( 'NONE',  ( -69.77438362644100778, 72.17411849586700612, -67.49847958357700861 ) ) ;
#208=ORIENTED_EDGE ( 'NONE', *, *, #4156, .T. ) ;
#209=DIRECTION ( 'NONE',  ( 0.000000000000000000, -1.000000000000000000, 0.000000000000000000 ) ) ;
#212=ADVANCED_FACE ( 'NONE', ( #8971 ), #14705, .T. ) ;
#213=EDGE_LOOP ( 'NONE', ( #14069, #5865 ) ) ;
#217=DIRECTION ( 'NONE',  ( 1.000000000000000000, 0.000000000000000000, 0.000000000000000000 ) ) ;
#218=FACE_OUTER_BOUND ( 'NONE', #9920, .T. ) ;
#220=FACE_BOUND ( 'NONE', #13407, .T. ) ;
#221=CARTESIAN_POINT ( 'NONE',  ( -90.52438362644100778, 99.17411849586700612, -150.4984795835770228 ) ) ;
#224=EDGE_CURVE ( 'NONE', #8420, #5168, #5339, .T. ) ;
#225=ORIENTED_EDGE ( 'NONE', *, *, #3832, .T. ) ;
#226=ORIENTED_EDGE ( 'NONE', *, *, #4376, .F. ) ;
#228=EDGE_LOOP ( 'NONE', ( #12564, #488 ) ) ;
#232=EDGE_CURVE ( 'NONE', #1220, #5341, #3328, .T. ) ;
#233=ADVANCED_FACE ( 'NONE', ( #7744 ), #2100, .F. ) ;
#234=FILL_AREA_STYLE ('',( #7467 ) ) ;
#235=PLANE ( 'NONE',  #9452 ) ;
#239=DIRECTION ( 'NONE',  ( -0.000000000000000000, 0.000000000000000000, -1.000000000000000000 ) ) ;
#242=CARTESIAN_POINT ( 'NONE',  ( -84.02438362643999881, 65.17411849586700612, -86.49847958357699440 ) ) ;
#243=EDGE_CURVE ( 'NONE', #3902, #13427, #9900, .T. ) ;
#244=ORIENTED_EDGE ( 'NONE', *, *, #1570, .T. ) ;
#245=DIRECTION ( 'NONE',  ( 0.000000000000000000, -1.000000000000000000, 0.000000000000000000 ) ) ;
#246=ORIENTED_EDGE ( 'NONE', *, *, #2791, .T. ) ;
#249=EDGE_CURVE ( 'NONE', #6663, #9914, #13638, .T. ) ;
#255=DIRECTION ( 'NONE',  ( 0.000000000000000000, 0.000000000000000000, -1.000000000000000000 ) ) ;
#259=CARTESIAN_POINT ( 'NONE',  ( -86.77438362644100778, 101.5320169952374414, -147.9984795835769944 ) ) ;
#260=ORIENTED_EDGE ( 'NONE', *, *, #8838, .T. ) ;
#265=CIRCLE ( 'NONE', #4742, 9.999999999999994671 ) ;
#267=CARTESIAN_POINT ( 'NONE',  ( -59.02799568714584666, 164.3482369917340122, -79.59847958357700293 ) ) ;
#269=DIRECTION ( 'NONE',  ( 0.000000000000000000, -1.000000000000000000, 0.000000000000000000 ) ) ;
#270=CARTESIAN_POINT ( 'NONE',  ( -73.76311196519618818, 67.29799558322736175, -81.84847958357697451 ) ) ;
#271=DIRECTION ( 'NONE',  ( 1.000000000000000000, 0.000000000000000000, 0.000000000000000000 ) ) ;
#274=CIRCLE ( 'NONE', #12179, 17.85000000000000497 ) ;
#275=ORIENTED_EDGE ( 'NONE', *, *, #2044, .F. ) ;
#277=EDGE_CURVE ( 'NONE', #4210, #1225, #6107, .T. ) ;
#279=CARTESIAN_POINT ( 'NONE',  ( -75.01311196519617397, 67.29799558322736175, -83.44847958357698303 ) ) ;
#282=EDGE_LOOP ( 'NONE', ( #3121, #10852 ) ) ;
#284=CARTESIAN_POINT ( 'NONE',  ( -48.27438362644000591, 99.17411849586700612, -145.4984795835769660 ) ) ;
#285=AXIS2_PLACEMENT_3D ( 'NONE', #3423, #3496, #1409 ) ;
#287=CIRCLE ( 'NONE', #13919, 17.00000000000000000 ) ;
#288=DIRECTION ( 'NONE',  ( 0.000000000000000000, 0.000000000000000000, -1.000000000000000000 ) ) ;
#290=CARTESIAN_POINT ( 'NONE',  ( -52.77438362644100067, 99.17411849586700612, -145.2984795835770058 ) ) ;
#295=DIRECTION ( 'NONE',  ( 1.000000000000000000, 0.000000000000000000, 0.000000000000000000 ) ) ;
#299=ORIENTED_EDGE ( 'NONE', *, *, #15082, .F. ) ;
#300=ORIENTED_EDGE ( 'NONE', *, *, #2020, .F. ) ;
#303=DIRECTION ( 'NONE',  ( -0.000000000000000000, -0.000000000000000000, -1.000000000000000000 ) ) ;
#308=CYLINDRICAL_SURFACE ( 'NONE', #15272, 4.249999999999996447 ) ;
#309=CARTESIAN_POINT ( 'NONE',  ( -80.52077156573417938, 60.67411849586702743, -73.34256232478206528 ) ) ;
#310=CARTESIAN_POINT ( 'NONE',  ( -86.77438362644100778, 96.81621999649657084, -147.9984795835769944 ) ) ;
#311=CARTESIAN_POINT ( 'NONE',  ( -76.48108760497456160, 68.65632084656354550, -81.84847958357697451 ) ) ;
#313=ADVANCED_FACE ( 'NONE', ( #6955 ), #3455, .T. ) ;
#316=DIRECTION ( 'NONE',  ( -1.000000000000000000, 0.000000000000000000, 0.000000000000000000 ) ) ;
#317=ORIENTED_EDGE ( 'NONE', *, *, #10977, .T. ) ;
#318=CARTESIAN_POINT ( 'NONE',  ( -69.77438362644001302, 82.17411849586700612, -93.49847958357699440 ) ) ;
#319=EDGE_CURVE ( 'NONE', #10983, #14726, #818, .T. ) ;
#320=ORIENTED_EDGE ( 'NONE', *, *, #1529, .T. ) ;
#322=EDGE_CURVE ( 'NONE', #15299, #4417, #124, .T. ) ;
#326=CARTESIAN_POINT ( 'NONE',  ( -82.27438362643999881, 65.17411849586700612, -86.49847958357699440 ) ) ;
#331=EDGE_CURVE ( 'NONE', #13653, #13217, #4545, .T. ) ;
#337=DIRECTION ( 'NONE',  ( 0.000000000000000000, 0.000000000000000000, 1.000000000000000000 ) ) ;
#342=DIRECTION ( 'NONE',  ( 1.000000000000000000, 0.000000000000000000, 0.000000000000000000 ) ) ;
#343=AXIS2_PLACEMENT_3D ( 'NONE', #9775, #7400, #13368 ) ;
#344=VECTOR ( 'NONE', #14343, 1000.000000000000000 ) ;
#347=ORIENTED_EDGE ( 'NONE', *, *, #5578, .T. ) ;
#353=AXIS2_PLACEMENT_3D ( 'NONE', #3405, #4807, #5912 ) ;
#355=DIRECTION ( 'NONE',  ( 0.000000000000000000, 0.000000000000000000, 1.000000000000000000 ) ) ;
#357=BREP_WITH_VOIDS ( 'NONE', #12735, ( #9878 ) );
#358=CARTESIAN_POINT ( 'NONE',  ( -69.77438362644001302, 82.17411849586700612, -138.4984795835769944 ) ) ;
#359=CARTESIAN_POINT ( 'NONE',  ( 0.000000000000000000, 0.000000000000000000, -79.59847958357700293 ) ) ;
#360=DIRECTION ( 'NONE',  ( -1.000000000000000000, 0.000000000000000000, 0.000000000000000000 ) ) ;
#361=DIRECTION ( 'NONE',  ( 0.000000000000000000, 0.000000000000000000, -1.000000000000000000 ) ) ;
#362=PLANE ( 'NONE',  #14403 ) ;
#366=CONICAL_SURFACE ( 'NONE', #1846, 2.042000000000002036, 1.047197551196596965 ) ;
#372=LINE ( 'NONE', #8825, #6733 ) ;
#377=DIRECTION ( 'NONE',  ( 1.000000000000000000, 0.000000000000000000, 0.000000000000000000 ) ) ;
#378=FACE_BOUND ( 'NONE', #838, .T. ) ;
#379=VECTOR ( 'NONE', #1869, 1000.000000000000000 ) ;
#384=VERTEX_POINT ( 'NONE', #4938 ) ;
#386=ORIENTED_EDGE ( 'NONE', *, *, #13860, .F. ) ;
#388=( GEOMETRIC_REPRESENTATION_CONTEXT ( 3 ) GLOBAL_UNCERTAINTY_ASSIGNED_CONTEXT ( ( #5155 ) ) GLOBAL_UNIT_ASSIGNED_CONTEXT ( ( #11839, #2746, #8645 ) ) REPRESENTATION_CONTEXT ( 'NONE', 'WORKASPACE' ) );
#389=VERTEX_POINT ( 'NONE', #5889 ) ;
#390=VECTOR ( 'NONE', #8485, 1000.000000000000000 ) ;
#393=EDGE_CURVE ( 'NONE', #14684, #12550, #2354, .T. ) ;
#399=FACE_OUTER_BOUND ( 'NONE', #13259, .T. ) ;
#401=CARTESIAN_POINT ( 'NONE',  ( -52.77438362643999881, 65.17411849586700612, -147.9984795835769944 ) ) ;
#403=CARTESIAN_POINT ( 'NONE',  ( -61.64938362644000591, 82.17411849586700612, -85.04847958357700577 ) ) ;
#405=CARTESIAN_POINT ( 'NONE',  ( -69.77438362644100778, 92.17411849586700612, -67.49847958357700861 ) ) ;
#407=ORIENTED_EDGE ( 'NONE', *, *, #14933, .T. ) ;
#409=CARTESIAN_POINT ( 'NONE',  ( -52.77438362644100067, 96.81621999649657084, -150.4984795835770228 ) ) ;
#415=VECTOR ( 'NONE', #10901, 1000.000000000000000 ) ;
#416=EDGE_CURVE ( 'NONE', #3919, #9472, #10591, .T. ) ;
#418=MANIFOLD_SOLID_BREP ( 'Move Face10', #630 ) ;
#419=FACE_BOUND ( 'NONE', #14484, .T. ) ;
#420=CARTESIAN_POINT ( 'NONE',  ( -60.52799568714584666, 60.67411849586701322, -152.4984795835769944 ) ) ;
#421=EDGE_CURVE ( 'NONE', #13943, #13082, #6349, .T. ) ;
#423=DIRECTION ( 'NONE',  ( 0.000000000000000000, 0.000000000000000000, -1.000000000000000000 ) ) ;
#424=LINE ( 'NONE', #2671, #3060 ) ;
#425=DIRECTION ( 'NONE',  ( 0.000000000000000000, 0.000000000000000000, -1.000000000000000000 ) ) ;
#427=VECTOR ( 'NONE', #13074, 1000.000000000000000 ) ;
#428=DIRECTION ( 'NONE',  ( 1.000000000000000000, 0.000000000000000000, 0.000000000000000000 ) ) ;
#432=ORIENTED_EDGE ( 'NONE', *, *, #14693, .T. ) ;
#436=EDGE_CURVE ( 'NONE', #2455, #11284, #12306, .T. ) ;
#437=DIRECTION ( 'NONE',  ( 0.000000000000000000, 0.000000000000000000, -1.000000000000000000 ) ) ;
#438=EDGE_CURVE ( 'NONE', #7835, #506, #1594, .T. ) ;
#439=LINE ( 'NONE', #12387, #4347 ) ;
#440=DIRECTION ( 'NONE',  ( 0.000000000000000000, 0.000000000000000000, -1.000000000000000000 ) ) ;
#443=DIRECTION ( 'NONE',  ( -1.000000000000000000, 0.000000000000000000, 0.000000000000000000 ) ) ;
#445=DIRECTION ( 'NONE',  ( 1.287488025362404182E-15, 1.000000000000000000, 0.000000000000000000 ) ) ;
#447=DIRECTION ( 'NONE',  ( 0.8660254037844383745, -0.5000000000000003331, 0.000000000000000000 ) ) ;
#449=VERTEX_POINT ( 'NONE', #3990 ) ;
#451=EDGE_LOOP ( 'NONE', ( #11553, #2716, #2919, #8346 ) ) ;
#453=DIRECTION ( 'NONE',  ( 0.000000000000000000, 0.000000000000000000, -1.000000000000000000 ) ) ;
#457=DIRECTION ( 'NONE',  ( 0.000000000000000000, -0.000000000000000000, 1.000000000000000000 ) ) ;
#459=FACE_OUTER_BOUND ( 'NONE', #3880, .T. ) ;
#460=VECTOR ( 'NONE', #9602, 1000.000000000000000 ) ;
#462=DIRECTION ( 'NONE',  ( 1.000000000000000000, 0.000000000000000000, 0.000000000000000000 ) ) ;
#463=LINE ( 'NONE', #3951, #7338 ) ;
#464=DIRECTION ( 'NONE',  ( -0.8660254037844387076, -0.4999999999999998890, 0.000000000000000000 ) ) ;
#465=ORIENTED_EDGE ( 'NONE', *, *, #14188, .T. ) ;
#469=VERTEX_POINT ( 'NONE', #11132 ) ;
#470=ORIENTED_EDGE ( 'NONE', *, *, #7793, .T. ) ;
#471=EDGE_LOOP ( 'NONE', ( #12338, #12653, #4071, #4133, #10276 ) ) ;
#478=CYLINDRICAL_SURFACE ( 'NONE', #3382, 4.249999999999996447 ) ;
#479=DIRECTION ( 'NONE',  ( -0.000000000000000000, -0.000000000000000000, 1.000000000000000000 ) ) ;
#482=CARTESIAN_POINT ( 'NONE',  ( -50.73238362644099197, 100.3530677455522238, -147.9984795835769944 ) ) ;
#483=DIRECTION ( 'NONE',  ( 1.000000000000000000, 0.000000000000000000, 0.000000000000000000 ) ) ;
#484=ORIENTED_EDGE ( 'NONE', *, *, #14470, .F. ) ;
#485=LINE ( 'NONE', #8858, #14927 ) ;
#486=VERTEX_POINT ( 'NONE', #6013 ) ;
#487=ORIENTED_EDGE ( 'NONE', *, *, #1261, .T. ) ;
#488=ORIENTED_EDGE ( 'NONE', *, *, #1646, .T. ) ;
#491=DIRECTION ( 'NONE',  ( 0.000000000000000000, 0.000000000000000000, 1.000000000000000000 ) ) ;
#493=CARTESIAN_POINT ( 'NONE',  ( -80.27438362643999881, 82.17411849586700612, -152.4984795835769944 ) ) ;
#495=CARTESIAN_POINT ( 'NONE',  ( -85.77438362644001302, 82.17411849586700612, -93.49847958357699440 ) ) ;
#499=ORIENTED_EDGE ( 'NONE', *, *, #15094, .T. ) ;
#501=ADVANCED_FACE ( 'NONE', ( #6177 ), #7170, .F. ) ;
#503=PRODUCT_DEFINITION_SHAPE ( 'NONE', 'NONE',  #14892 ) ;
#506=VERTEX_POINT ( 'NONE', #172 ) ;
#507=CARTESIAN_POINT ( 'NONE',  ( -77.52077156573416516, 110.1741184958670061, -152.4984795835769944 ) ) ;
#508=CARTESIAN_POINT ( 'NONE',  ( -62.27438362644000591, 89.17411849586700612, -58.99847958357700151 ) ) ;
#509=CARTESIAN_POINT ( 'NONE',  ( -69.77438362644001302, 82.17411849586700612, -117.9984795835769944 ) ) ;
#510=CARTESIAN_POINT ( 'NONE',  ( -52.77438362644000591, 82.17411849586700612, -81.84847958357697451 ) ) ;
#515=CARTESIAN_POINT ( 'NONE',  ( -52.77438362644000591, 65.17411849586700612, -79.59847958357700293 ) ) ;
#516=ORIENTED_EDGE ( 'NONE', *, *, #4971, .T. ) ;
#519=VECTOR ( 'NONE', #6591, 1000.000000000000000 ) ;
#520=DIRECTION ( 'NONE',  ( -1.000000000000000000, 0.000000000000000000, 0.000000000000000000 ) ) ;
#521=EDGE_CURVE ( 'NONE', #12362, #3959, #5064, .T. ) ;
#524=LINE ( 'NONE', #2855, #12667 ) ;
#525=AXIS2_PLACEMENT_3D ( 'NONE', #11127, #1437, #6341 ) ;
#526=EDGE_CURVE ( 'NONE', #897, #10418, #12125, .T. ) ;
#530=CARTESIAN_POINT ( 'NONE',  ( -86.77438362643999881, 65.17411849586700612, -150.4984795835770228 ) ) ;
#533=PLANE ( 'NONE',  #4081 ) ;
#538=EDGE_LOOP ( 'NONE', ( #9721, #11855, #10440, #988 ) ) ;
#539=ORIENTED_EDGE ( 'NONE', *, *, #8974, .T. ) ;
#540=ORIENTED_EDGE ( 'NONE', *, *, #2131, .F. ) ;
#542=CARTESIAN_POINT ( 'NONE',  ( -59.02799568714584666, 0.000000000000000000, -152.4984795835769944 ) ) ;
#546=CARTESIAN_POINT ( 'NONE',  ( -104.2743836264399988, 111.1741184958670061, -79.49847958357700861 ) ) ;
#547=CARTESIAN_POINT ( 'NONE',  ( -61.59970400812709102, 70.01464610989972925, -81.84847958357697451 ) ) ;
#548=AXIS2_PLACEMENT_3D ( 'NONE', #9377, #14114, #15187 ) ;
#554=EDGE_LOOP ( 'NONE', ( #14518, #4651, #12673, #5642 ) ) ;
#555=AXIS2_PLACEMENT_3D ( 'NONE', #5570, #7949, #4702 ) ;
#556=EDGE_LOOP ( 'NONE', ( #3420, #4653, #2541, #2426, #5631, #2495, #10644, #3786 ) ) ;
#557=VERTEX_POINT ( 'NONE', #10954 ) ;
#558=VERTEX_POINT ( 'NONE', #4985 ) ;
#560=DIRECTION ( 'NONE',  ( -1.000000000000000000, 0.000000000000000000, 0.000000000000000000 ) ) ;
#561=CARTESIAN_POINT ( 'NONE',  ( -77.89938362643999881, 82.17411849586700612, -85.04847958357699156 ) ) ;
#563=PLANE ( 'NONE',  #11832 ) ;
#565=ADVANCED_FACE ( 'NONE', ( #9777 ), #14512, .F. ) ;
#566=VECTOR ( 'NONE', #14294, 1000.000000000000000 ) ;
#568=ORIENTED_EDGE ( 'NONE', *, *, #10428, .F. ) ;
#569=LINE ( 'NONE', #5318, #8356 ) ;
#570=ORIENTED_EDGE ( 'NONE', *, *, #1954, .T. ) ;
#571=AXIS2_PLACEMENT_3D ( 'NONE', #14495, #9610, #8611 ) ;
#573=EDGE_LOOP ( 'NONE', ( #4904, #6585 ) ) ;
#575=DIRECTION ( 'NONE',  ( -1.000000000000000000, 0.000000000000000000, 0.000000000000000000 ) ) ;
#577=DIRECTION ( 'NONE',  ( 1.000000000000000000, 0.000000000000000000, 0.000000000000000000 ) ) ;
#578=CARTESIAN_POINT ( 'NONE',  ( -75.01311196519617397, 67.29799558322736175, -81.84847958357697451 ) ) ;
#582=LINE ( 'NONE', #13561, #8644 ) ;
#583=LINE ( 'NONE', #14698, #1556 ) ;
#585=FACE_OUTER_BOUND ( 'NONE', #1025, .T. ) ;
#587=VERTEX_POINT ( 'NONE', #3898 ) ;
#588=ORIENTED_EDGE ( 'NONE', *, *, #11348, .F. ) ;
#592=AXIS2_PLACEMENT_3D ( 'NONE', #8213, #2313, #12876 ) ;
#596=DIRECTION ( 'NONE',  ( -1.000000000000000000, 0.000000000000000000, 0.000000000000000000 ) ) ;
#602=AXIS2_PLACEMENT_3D ( 'NONE', #3092, #14863, #1848 ) ;
#603=DIRECTION ( 'NONE',  ( 0.000000000000000000, 0.000000000000000000, 1.000000000000000000 ) ) ;
#605=FACE_OUTER_BOUND ( 'NONE', #1148, .T. ) ;
#607=EDGE_CURVE ( 'NONE', #1588, #4413, #13538, .T. ) ;
#609=ORIENTED_EDGE ( 'NONE', *, *, #6334, .F. ) ;
#611=ORIENTED_EDGE ( 'NONE', *, *, #11056, .T. ) ;
#612=ORIENTED_EDGE ( 'NONE', *, *, #8854, .F. ) ;
#615=EDGE_CURVE ( 'NONE', #7422, #10445, #10046, .T. ) ;
#616=AXIS2_PLACEMENT_3D ( 'NONE', #13381, #1660, #8559 ) ;
#619=CARTESIAN_POINT ( 'NONE',  ( -52.77438362644000591, 65.17411849586700612, -86.49847958357699440 ) ) ;
#620=EDGE_CURVE ( 'NONE', #9201, #8717, #3737, .T. ) ;
#622=CARTESIAN_POINT ( 'NONE',  ( -61.59970400812709102, 70.01464610989972925, -83.44847958357698303 ) ) ;
#624=DIRECTION ( 'NONE',  ( 1.000000000000000000, 0.000000000000000000, 0.000000000000000000 ) ) ;
#629=MECHANICAL_DESIGN_GEOMETRIC_PRESENTATION_REPRESENTATION('',(#3103),#2611);
#630=CLOSED_SHELL ( 'NONE', ( #9474, #9132, #12966, #1902, #8555, #15074, #6488, #13690, #5762, #8386, #1849, #1749, #1679, #13727 ) ) ;
#631=ORIENTED_EDGE ( 'NONE', *, *, #5639, .T. ) ;
#632=VERTEX_POINT ( 'NONE', #10151 ) ;
#636=LINE ( 'NONE', #326, #1022 ) ;
#638=CARTESIAN_POINT ( 'NONE',  ( -62.02799568714584666, 0.000000000000000000, -152.4984795835769944 ) ) ;
#640=PLANE ( 'NONE',  #6024 ) ;
#642=AXIS2_PLACEMENT_3D ( 'NONE', #2822, #11192, #3981 ) ;
#643=DIRECTION ( 'NONE',  ( 0.000000000000000000, 0.000000000000000000, -1.000000000000000000 ) ) ;
#644=FACE_OUTER_BOUND ( 'NONE', #5137, .T. ) ;
#645=AXIS2_PLACEMENT_3D ( 'NONE', #14851, #1827, #14781 ) ;
#651=AXIS2_PLACEMENT_3D ( 'NONE', #6543, #2963, #12274 ) ;
#653=AXIS2_PLACEMENT_3D ( 'NONE', #7648, #14451, #14528 ) ;
#657=FACE_OUTER_BOUND ( 'NONE', #8173, .T. ) ;
#661=CONICAL_SURFACE ( 'NONE', #10574, 3.750000000000003553, 0.7853981633974476129 ) ;
#665=CARTESIAN_POINT ( 'NONE',  ( -67.55245199152457758, 98.02101855758749593, -94.16081083965335097 ) ) ;
#667=EDGE_CURVE ( 'NONE', #10367, #5341, #9792, .T. ) ;
#668=ORIENTED_EDGE ( 'NONE', *, *, #12451, .T. ) ;
#672=AXIS2_PLACEMENT_3D ( 'NONE', #12988, #15, #10403 ) ;
#675=CARTESIAN_POINT ( 'NONE',  ( -61.72438362644000165, 82.17411849586700612, -80.44847958357698303 ) ) ;
#676=LINE ( 'NONE', #4328, #6394 ) ;
#677=CARTESIAN_POINT ( 'NONE',  ( -69.77438362644100778, 72.17411849586700612, -79.49847958357700861 ) ) ;
#678=DIRECTION ( 'NONE',  ( -1.000000000000000000, 0.000000000000000000, 0.000000000000000000 ) ) ;
#681=LINE ( 'NONE', #5433, #14902 ) ;
#682=VERTEX_POINT ( 'NONE', #13445 ) ;
#683=DIRECTION ( 'NONE',  ( 0.000000000000000000, 0.000000000000000000, -1.000000000000000000 ) ) ;
#684=ADVANCED_FACE ( 'NONE', ( #11177 ), #13521, .F. ) ;
#686=VERTEX_POINT ( 'NONE', #3114 ) ;
#689=EDGE_CURVE ( 'NONE', #13826, #3095, #14258, .T. ) ;
#690=ORIENTED_EDGE ( 'NONE', *, *, #12073, .F. ) ;
#693=AXIS2_PLACEMENT_3D ( 'NONE', #11712, #11636, #14039 ) ;
#694=DIRECTION ( 'NONE',  ( -1.000000000000000000, 0.000000000000000000, 0.000000000000000000 ) ) ;
#698=EDGE_CURVE ( 'NONE', #4969, #8760, #13664, .T. ) ;
#701=CARTESIAN_POINT ( 'NONE',  ( -84.73238362643999722, 63.99516924618178848, -150.4984795835770228 ) ) ;
#704=VERTEX_POINT ( 'NONE', #10084 ) ;
#705=DIRECTION ( 'NONE',  ( -1.000000000000000000, 0.000000000000000000, 0.000000000000000000 ) ) ;
#706=EDGE_CURVE ( 'NONE', #9229, #2624, #7635, .T. ) ;
#715=FACE_BOUND ( 'NONE', #7426, .T. ) ;
#716=DIRECTION ( 'NONE',  ( 0.000000000000000000, 0.000000000000000000, 1.000000000000000000 ) ) ;
#717=DIRECTION ( 'NONE',  ( 1.000000000000000000, 0.000000000000000000, 0.000000000000000000 ) ) ;
#718=CIRCLE ( 'NONE', #14335, 8.124999999999992895 ) ;
#719=LINE ( 'NONE', #4067, #9840 ) ;
#721=CARTESIAN_POINT ( 'NONE',  ( -52.77438362643999881, 65.17411849586700612, -150.4984795835770228 ) ) ;
#725=EDGE_CURVE ( 'NONE', #13232, #1792, #6398, .T. ) ;
#727=FACE_OUTER_BOUND ( 'NONE', #7858, .T. ) ;
#730=ORIENTED_EDGE ( 'NONE', *, *, #6098, .F. ) ;
#734=LINE ( 'NONE', #962, #11977 ) ;
#735=DIRECTION ( 'NONE',  ( -1.000000000000000000, 0.000000000000000000, 0.000000000000000000 ) ) ;
#738=CARTESIAN_POINT ( 'NONE',  ( -69.77438362644001302, 82.17411849586700612, -150.4984795835769944 ) ) ;
#739=DIRECTION ( 'NONE',  ( 0.000000000000000000, 0.000000000000000000, 1.000000000000000000 ) ) ;
#740=ORIENTED_EDGE ( 'NONE', *, *, #6624, .F. ) ;
#742=ORIENTED_EDGE ( 'NONE', *, *, #277, .F. ) ;
#743=CARTESIAN_POINT ( 'NONE',  ( -91.27438362643999881, 65.17411849586700612, -86.49847958357699440 ) ) ;
#744=CARTESIAN_POINT ( 'NONE',  ( -59.02799568714584666, 164.3482369917340122, -152.4984795835769944 ) ) ;
#745=DIRECTION ( 'NONE',  ( 0.000000000000000000, 1.000000000000000000, 0.000000000000000000 ) ) ;
#749=DIRECTION ( 'NONE',  ( 0.000000000000000000, 0.000000000000000000, -1.000000000000000000 ) ) ;
#750=ORIENTED_EDGE ( 'NONE', *, *, #7341, .T. ) ;
#751=CARTESIAN_POINT ( 'NONE',  ( -50.02438362644000591, 65.17411849586700612, -152.4984795835769944 ) ) ;
#755=ORIENTED_EDGE ( 'NONE', *, *, #5452, .T. ) ;
#756=ORIENTED_EDGE ( 'NONE', *, *, #1230, .F. ) ;
#757=ORIENTED_EDGE ( 'NONE', *, *, #10286, .F. ) ;
#759=DIRECTION ( 'NONE',  ( 1.000000000000000000, 0.000000000000000000, 0.000000000000000000 ) ) ;
#764=EDGE_CURVE ( 'NONE', #13867, #7621, #14028, .T. ) ;
#768=LINE ( 'NONE', #1789, #12528 ) ;
#769=EDGE_CURVE ( 'NONE', #2388, #13148, #7355, .T. ) ;
#771=AXIS2_PLACEMENT_3D ( 'NONE', #6411, #4147, #2977 ) ;
#772=ORIENTED_EDGE ( 'NONE', *, *, #3947, .T. ) ;
#773=DIRECTION ( 'NONE',  ( 0.8660254037844387076, 0.4999999999999998890, 0.000000000000000000 ) ) ;
#774=ORIENTED_EDGE ( 'NONE', *, *, #232, .T. ) ;
#779=AXIS2_PLACEMENT_3D ( 'NONE', #13782, #9894, #12321 ) ;
#780=LINE ( 'NONE', #4511, #9954 ) ;
#783=FACE_OUTER_BOUND ( 'NONE', #4137, .T. ) ;
#784=CARTESIAN_POINT ( 'NONE',  ( -86.77438362644001302, 99.17411849586700612, -79.59847958357700293 ) ) ;
#785=ADVANCED_FACE ( 'NONE', ( #13597 ), #11109, .F. ) ;
#786=LINE ( 'NONE', #13977, #3884 ) ;
#788=DIRECTION ( 'NONE',  ( 0.8660254037844381525, 1.060575238724905436E-16, -0.5000000000000007772 ) ) ;
#789=DIRECTION ( 'NONE',  ( 0.000000000000000000, 0.000000000000000000, -1.000000000000000000 ) ) ;
#790=CARTESIAN_POINT ( 'NONE',  ( -91.27438362643999881, 99.17411849586700612, -145.4984795835769660 ) ) ;
#795=EDGE_LOOP ( 'NONE', ( #11221, #317, #14436, #2392, #10585 ) ) ;
#801=ORIENTED_EDGE ( 'NONE', *, *, #3085, .T. ) ;
#802=CIRCLE ( 'NONE', #3288, 4.499999999999997335 ) ;
#806=DIRECTION ( 'NONE',  ( -1.000000000000000000, 0.000000000000000000, 0.000000000000000000 ) ) ;
#807=VECTOR ( 'NONE', #13371, 1000.000000000000000 ) ;
#809=ADVANCED_FACE ( 'NONE', ( #11486 ), #4663, .T. ) ;
#811=EDGE_CURVE ( 'NONE', #11511, #3473, #14043, .T. ) ;
#812=DIRECTION ( 'NONE',  ( -1.000000000000000000, 0.000000000000000000, 0.000000000000000000 ) ) ;
#813=AXIS2_PLACEMENT_3D ( 'NONE', #12268, #1639, #8994 ) ;
#814=CIRCLE ( 'NONE', #8252, 4.709525205202999665 ) ;
#815=CARTESIAN_POINT ( 'NONE',  ( -66.41143315690761995, 66.60412428008086749, -83.44847958357698303 ) ) ;
#817=ORIENTED_EDGE ( 'NONE', *, *, #6878, .F. ) ;
#818=LINE ( 'NONE', #5573, #3352 ) ;
#824=VECTOR ( 'NONE', #14391, 1000.000000000000000 ) ;
#826=DIRECTION ( 'NONE',  ( 1.000000000000000000, 0.000000000000000000, 0.000000000000000000 ) ) ;
#827=FACE_OUTER_BOUND ( 'NONE', #4879, .T. ) ;
#832=DIRECTION ( 'NONE',  ( 1.000000000000000000, 0.000000000000000000, 0.000000000000000000 ) ) ;
#834=CIRCLE ( 'NONE', #7800, 10.49999999999999467 ) ;
#835=ORIENTED_EDGE ( 'NONE', *, *, #11996, .T. ) ;
#838=EDGE_LOOP ( 'NONE', ( #8455, #3676 ) ) ;
#840=VERTEX_POINT ( 'NONE', #10385 ) ;
#846=VECTOR ( 'NONE', #239, 1000.000000000000000 ) ;
#847=DIRECTION ( 'NONE',  ( 0.000000000000000000, 0.000000000000000000, -1.000000000000000000 ) ) ;
#851=LINE ( 'NONE', #4429, #8047 ) ;
#852=CARTESIAN_POINT ( 'NONE',  ( -76.26311196519618818, 67.29799558322736175, -81.84847958357697451 ) ) ;
#853=CARTESIAN_POINT ( 'NONE',  ( -84.73238362643999722, 66.35306774555222376, -147.9984795835769944 ) ) ;
#854=EDGE_LOOP ( 'NONE', ( #10172, #8366, #12990, #13556 ) ) ;
#855=DIRECTION ( 'NONE',  ( 0.000000000000000000, 1.000000000000000000, 0.000000000000000000 ) ) ;
#857=ORIENTED_EDGE ( 'NONE', *, *, #4793, .F. ) ;
#858=VERTEX_POINT ( 'NONE', #852 ) ;
#861=AXIS2_PLACEMENT_3D ( 'NONE', #11815, #4836, #8324 ) ;
#862=EDGE_CURVE ( 'NONE', #10484, #6682, #4430, .T. ) ;
#863=LINE ( 'NONE', #638, #2101 ) ;
#865=CARTESIAN_POINT ( 'NONE',  ( -69.77438362644001302, 74.17411849586699191, -79.49847958357700861 ) ) ;
#866=DIRECTION ( 'NONE',  ( -0.000000000000000000, 0.000000000000000000, 1.000000000000000000 ) ) ;
#870=EDGE_LOOP ( 'NONE', ( #7613, #12898, #857 ) ) ;
#875=CARTESIAN_POINT ( 'NONE',  ( -80.52077156573417938, 103.6741184958669777, -79.59847958357700293 ) ) ;
#877=VERTEX_POINT ( 'NONE', #9379 ) ;
#879=ORIENTED_EDGE ( 'NONE', *, *, #5951, .F. ) ;
#882=FACE_OUTER_BOUND ( 'NONE', #4907, .T. ) ;
#883=CARTESIAN_POINT ( 'NONE',  ( -73.64736697264537213, 89.17411849586700612, -57.99847958357699440 ) ) ;
#885=DIRECTION ( 'NONE',  ( 0.8660254037844387076, 0.4999999999999998890, 0.000000000000000000 ) ) ;
#886=EDGE_CURVE ( 'NONE', #2365, #2303, #929, .T. ) ;
#887=DIRECTION ( 'NONE',  ( 1.000000000000000000, 0.000000000000000000, 0.000000000000000000 ) ) ;
#889=VECTOR ( 'NONE', #2242, 1000.000000000000000 ) ;
#892=AXIS2_PLACEMENT_3D ( 'NONE', #9092, #5399, #943 ) ;
#893=AXIS2_PLACEMENT_3D ( 'NONE', #10244, #13754, #3201 ) ;
#894=EDGE_CURVE ( 'NONE', #9154, #8986, #5120, .T. ) ;
#897=VERTEX_POINT ( 'NONE', #15111 ) ;
#898=ADVANCED_FACE ( 'NONE', ( #3412 ), #4578, .F. ) ;
#901=AXIS2_PLACEMENT_3D ( 'NONE', #8143, #62, #9295 ) ;
#902=CARTESIAN_POINT ( 'NONE',  ( -69.77438362644001302, 82.17411849586700612, -80.44847958357698303 ) ) ;
#903=CARTESIAN_POINT ( 'NONE',  ( -69.77438362644001302, 82.17411849586700612, -81.84847958357697451 ) ) ;
#905=DIRECTION ( 'NONE',  ( 0.000000000000000000, 0.000000000000000000, -1.000000000000000000 ) ) ;
#909=ORIENTED_EDGE ( 'NONE', *, *, #15198, .F. ) ;
#910=CARTESIAN_POINT ( 'NONE',  ( -57.02438362643999170, 65.17411849586700612, -149.9984795835770228 ) ) ;
#911=CONICAL_SURFACE ( 'NONE', #5404, 2.500000000000002220, 1.029744258676651425 ) ;
#913=VERTEX_POINT ( 'NONE', #14963 ) ;
#917=ORIENTED_EDGE ( 'NONE', *, *, #10777, .F. ) ;
#918=ORIENTED_EDGE ( 'NONE', *, *, #3458, .F. ) ;
#924=CARTESIAN_POINT ( 'NONE',  ( -59.27438362644000591, 82.17411849586700612, -82.44847958357698303 ) ) ;
#926=VECTOR ( 'NONE', #11580, 1000.000000000000000 ) ;
#929=LINE ( 'NONE', #10314, #7602 ) ;
#930=FACE_OUTER_BOUND ( 'NONE', #9434, .T. ) ;
#935=ORIENTED_EDGE ( 'NONE', *, *, #8658, .T. ) ;
#937=AXIS2_PLACEMENT_3D ( 'NONE', #2010, #6986, #10226 ) ;
#940=CARTESIAN_POINT ( 'NONE',  ( -35.27438362644000591, 111.1741184958670061, -79.49847958357700861 ) ) ;
#941=DIRECTION ( 'NONE',  ( 0.000000000000000000, 0.000000000000000000, 1.000000000000000000 ) ) ;
#942=CARTESIAN_POINT ( 'NONE',  ( -88.81638362644100937, 97.99516924618178848, -147.9984795835769944 ) ) ;
#943=DIRECTION ( 'NONE',  ( 1.000000000000000000, 0.000000000000000000, 0.000000000000000000 ) ) ;
#945=CARTESIAN_POINT ( 'NONE',  ( -35.27438362644000591, 111.1741184958670061, -67.49847958357700861 ) ) ;
#946=DIRECTION ( 'NONE',  ( -0.000000000000000000, 0.7071067811865441310, 0.7071067811865510144 ) ) ;
#947=PLANE ( 'NONE',  #13258 ) ;
#949=ORIENTED_EDGE ( 'NONE', *, *, #6427, .T. ) ;
#950=DIRECTION ( 'NONE',  ( 0.000000000000000000, 0.000000000000000000, 1.000000000000000000 ) ) ;
#951=ADVANCED_FACE ( 'NONE', ( #9079 ), #3778, .F. ) ;
#952=ORIENTED_EDGE ( 'NONE', *, *, #14604, .F. ) ;
#954=CARTESIAN_POINT ( 'NONE',  ( -52.77438362644100067, 99.17411849586700612, -145.4984795835769944 ) ) ;
#955=ORIENTED_EDGE ( 'NONE', *, *, #243, .F. ) ;
#957=VERTEX_POINT ( 'NONE', #9741 ) ;
#962=CARTESIAN_POINT ( 'NONE',  ( -86.77438362643999881, 62.81621999649657084, -147.9984795835769944 ) ) ;
#963=ADVANCED_FACE ( 'NONE', ( #4948 ), #6368, .T. ) ;
#964=CARTESIAN_POINT ( 'NONE',  ( -86.77438362644001302, 65.17411849586700612, -145.4984795835769660 ) ) ;
#970=ORIENTED_EDGE ( 'NONE', *, *, #13625, .T. ) ;
#975=EDGE_CURVE ( 'NONE', #6718, #10037, #7105, .T. ) ;
#976=CARTESIAN_POINT ( 'NONE',  ( -69.77438362644001302, 82.17411849586700612, -80.44847958357698303 ) ) ;
#979=CARTESIAN_POINT ( 'NONE',  ( -80.52077156573417938, 59.67411849586701322, -15.85886927678779834 ) ) ;
#981=LINE ( 'NONE', #3393, #10692 ) ;
#983=EDGE_LOOP ( 'NONE', ( #1998, #985 ) ) ;
#985=ORIENTED_EDGE ( 'NONE', *, *, #10099, .T. ) ;
#988=ORIENTED_EDGE ( 'NONE', *, *, #10578, .F. ) ;
#989=B_SPLINE_CURVE_WITH_KNOTS ( 'NONE', 3,
 ( #4367, #11577, #2032, #4517, #9091, #5770, #6928, #11351 ),
 .UNSPECIFIED., .F., .F.,
 ( 4, 2, 2, 4 ),
 ( 0.04315383327197147567, 0.04413750674005950669, 0.04512118020814753772, 0.04708852714432359976 ),
 .UNSPECIFIED. ) ;
#990=ORIENTED_EDGE ( 'NONE', *, *, #10629, .F. ) ;
#991=ORIENTED_EDGE ( 'NONE', *, *, #11903, .T. ) ;
#998=FACE_OUTER_BOUND ( 'NONE', #11079, .T. ) ;
#1003=FACE_OUTER_BOUND ( 'NONE', #12432, .T. ) ;
#1006=CYLINDRICAL_SURFACE ( 'NONE', #12711, 4.709525205202999665 ) ;
#1008=ORIENTED_EDGE ( 'NONE', *, *, #6965, .F. ) ;
#1011=DIRECTION ( 'NONE',  ( 0.000000000000000000, 0.000000000000000000, 1.000000000000000000 ) ) ;
#1014=DIRECTION ( 'NONE',  ( 0.000000000000000000, 0.000000000000000000, -1.000000000000000000 ) ) ;
#1015=DIRECTION ( 'NONE',  ( 0.000000000000000000, 0.000000000000000000, 1.000000000000000000 ) ) ;
#1017=CIRCLE ( 'NONE', #525, 4.250000000000003553 ) ;
#1018=CARTESIAN_POINT ( 'NONE',  ( -84.27438362644100778, 99.17411849586700612, -79.59847958357700293 ) ) ;
#1019=DIRECTION ( 'NONE',  ( 1.000000000000000000, 0.000000000000000000, 0.000000000000000000 ) ) ;
#1020=CARTESIAN_POINT ( 'NONE',  ( -48.52438362643999881, 65.17411849586700612, -182.2484795835770228 ) ) ;
#1021=DIRECTION ( 'NONE',  ( 0.000000000000000000, 0.000000000000000000, -1.000000000000000000 ) ) ;
#1022=VECTOR ( 'NONE', #491, 1000.000000000000000 ) ;
#1023=ORIENTED_EDGE ( 'NONE', *, *, #811, .T. ) ;
#1024=DIRECTION ( 'NONE',  ( -1.287488025362404182E-15, -1.000000000000000000, 0.000000000000000000 ) ) ;
#1025=EDGE_LOOP ( 'NONE', ( #12553, #9996 ) ) ;
#1026=ORIENTED_EDGE ( 'NONE', *, *, #3001, .F. ) ;
#1027=CARTESIAN_POINT ( 'NONE',  ( -77.52077156573416516, 103.6741184958669777, -152.4984795835769944 ) ) ;
#1034=FACE_BOUND ( 'NONE', #15170, .T. ) ;
#1035=CIRCLE ( 'NONE', #5506, 10.50000000000000178 ) ;
#1036=CARTESIAN_POINT ( 'NONE',  ( -80.52077156573417938, 110.1741184958670061, -15.85886927678779834 ) ) ;
#1037=DIRECTION ( 'NONE',  ( -1.000000000000000000, 0.000000000000000000, 0.000000000000000000 ) ) ;
#1039=CARTESIAN_POINT ( 'NONE',  ( -90.85838362644000199, 65.17411849586700612, -147.9984795835769944 ) ) ;
#1040=ORIENTED_EDGE ( 'NONE', *, *, #12700, .T. ) ;
#1048=AXIS2_PLACEMENT_3D ( 'NONE', #7609, #8905, #462 ) ;
#1050=DIRECTION ( 'NONE',  ( 1.000000000000000000, 0.000000000000000000, 0.000000000000000000 ) ) ;
#1053=CARTESIAN_POINT ( 'NONE',  ( -59.02799568714584666, 59.67411849586701322, -152.4984795835769944 ) ) ;
#1055=CARTESIAN_POINT ( 'NONE',  ( -52.77438362644000591, 99.17411849586700612, -145.4984795835769660 ) ) ;
#1056=LINE ( 'NONE', #11850, #4509 ) ;
#1058=VERTEX_POINT ( 'NONE', #10992 ) ;
#1060=ORIENTED_EDGE ( 'NONE', *, *, #10858, .T. ) ;
#1063=ORIENTED_EDGE ( 'NONE', *, *, #10334, .F. ) ;
#1066=ADVANCED_FACE ( 'NONE', ( #2532, #8734 ), #13253, .T. ) ;
#1067=VERTEX_POINT ( 'NONE', #2845 ) ;
#1074=DIRECTION ( 'NONE',  ( -1.000000000000000000, 0.000000000000000000, 0.000000000000000000 ) ) ;
#1079=CIRCLE ( 'NONE', #3812, 1.250000000000001110 ) ;
#1083=LINE ( 'NONE', #4580, #13952 ) ;
#1084=ADVANCED_FACE ( 'NONE', ( #12232 ), #7593, .F. ) ;
#1086=EDGE_CURVE ( 'NONE', #8835, #6563, #8583, .T. ) ;
#1087=CARTESIAN_POINT ( 'NONE',  ( -79.02077156573416516, 60.67411849586702743, -79.59847958357700293 ) ) ;
#1090=ORIENTED_EDGE ( 'NONE', *, *, #6419, .T. ) ;
#1092=DIRECTION ( 'NONE',  ( -0.8660254037844387076, -0.4999999999999998890, 0.000000000000000000 ) ) ;
#1096=EDGE_CURVE ( 'NONE', #1293, #13867, #5378, .T. ) ;
#1100=DIRECTION ( 'NONE',  ( 1.000000000000000000, 0.000000000000000000, 0.000000000000000000 ) ) ;
#1105=ORIENTED_EDGE ( 'NONE', *, *, #13994, .F. ) ;
#1106=CARTESIAN_POINT ( 'NONE',  ( -84.73238362643999722, 66.35306774555222376, -150.4984795835770228 ) ) ;
#1113=DIRECTION ( 'NONE',  ( -1.000000000000000000, 0.000000000000000000, 0.000000000000000000 ) ) ;
#1117=LINE ( 'NONE', #1036, #6362 ) ;
#1124=PLANE ( 'NONE',  #4523 ) ;
#1125=VECTOR ( 'NONE', #12355, 1000.000000000000000 ) ;
#1126=ORIENTED_EDGE ( 'NONE', *, *, #331, .T. ) ;
#1130=EDGE_LOOP ( 'NONE', ( #13827, #11841, #4280 ) ) ;
#1133=CARTESIAN_POINT ( 'NONE',  ( -48.27438362644000591, 99.17411849586700612, -86.49847958357699440 ) ) ;
#1134=VECTOR ( 'NONE', #11888, 1000.000000000000000 ) ;
#1139=CIRCLE ( 'NONE', #5618, 5.499999999999998224 ) ;
#1140=DIRECTION ( 'NONE',  ( 0.000000000000000000, 1.000000000000000000, 0.000000000000000000 ) ) ;
#1142=ORIENTED_EDGE ( 'NONE', *, *, #4184, .T. ) ;
#1143=DIRECTION ( 'NONE',  ( 0.000000000000000000, -4.130293990420970006E-17, 1.000000000000000000 ) ) ;
#1144=EDGE_CURVE ( 'NONE', #12791, #11036, #7466, .T. ) ;
#1148=EDGE_LOOP ( 'NONE', ( #12567, #12427, #8900, #13200 ) ) ;
#1151=ORIENTED_EDGE ( 'NONE', *, *, #12378, .T. ) ;
#1154=DIRECTION ( 'NONE',  ( 0.000000000000000000, 0.000000000000000000, -1.000000000000000000 ) ) ;
#1160=DIRECTION ( 'NONE',  ( 0.000000000000000000, 0.000000000000000000, -1.000000000000000000 ) ) ;
#1164=AXIS2_PLACEMENT_3D ( 'NONE', #3408, #11789, #1074 ) ;
#1165=EDGE_LOOP ( 'NONE', ( #2623, #10956, #13964, #3494 ) ) ;
#1172=CONICAL_SURFACE ( 'NONE', #7125, 3.749999999999996447, 0.7853981633974476129 ) ;
#1175=CARTESIAN_POINT ( 'NONE',  ( -49.02438362644100067, 99.17411849586700612, -150.4984795835770228 ) ) ;
#1178=CARTESIAN_POINT ( 'NONE',  ( -52.77438362644100067, 99.17411849586700612, -147.9984795835769944 ) ) ;
#1181=ADVANCED_FACE ( 'NONE', ( #1910 ), #14700, .F. ) ;
#1182=CARTESIAN_POINT ( 'NONE',  ( -37.27438362644000591, 104.6741184958670061, -15.85886927678779834 ) ) ;
#1183=LINE ( 'NONE', #12897, #3792 ) ;
#1186=ADVANCED_FACE ( 'NONE', ( #4239, #585 ), #8893, .T. ) ;
#1188=AXIS2_PLACEMENT_3D ( 'NONE', #5400, #14833, #9016 ) ;
#1189=EDGE_CURVE ( 'NONE', #6732, #7286, #13704, .T. ) ;
#1190=VERTEX_POINT ( 'NONE', #13851 ) ;
#1195=CARTESIAN_POINT ( 'NONE',  ( -86.77438362644100778, 99.17411849586700612, -182.2484795835770228 ) ) ;
#1197=AXIS2_PLACEMENT_3D ( 'NONE', #622, #3895, #8620 ) ;
#1198=PLANE ( 'NONE',  #9735 ) ;
#1199=ADVANCED_FACE ( 'NONE', ( #4087, #8814 ), #3074, .T. ) ;
#1201=VERTEX_POINT ( 'NONE', #12464 ) ;
#1202=CARTESIAN_POINT ( 'NONE',  ( -58.27438362644001302, 82.17411849586700612, -83.44847958357698303 ) ) ;
#1204=ORIENTED_EDGE ( 'NONE', *, *, #11026, .T. ) ;
#1205=AXIS2_PLACEMENT_3D ( 'NONE', #290, #11235, #14791 ) ;
#1209=CYLINDRICAL_SURFACE ( 'NONE', #13169, 8.000000000000007105 ) ;
#1210=CARTESIAN_POINT ( 'NONE',  ( -86.77438362643999881, 65.17411849586700612, -145.4984795835769944 ) ) ;
#1212=PLANE ( 'NONE',  #10583 ) ;
#1213=CARTESIAN_POINT ( 'NONE',  ( -69.77438362644001302, 82.17411849586700612, -85.04847958357699156 ) ) ;
#1214=CARTESIAN_POINT ( 'NONE',  ( -66.41143315690761995, 66.60412428008086749, -83.44847958357698303 ) ) ;
#1215=CARTESIAN_POINT ( 'NONE',  ( -55.47438362644000165, 65.17411849586700612, -145.4984795835769944 ) ) ;
#1216=CARTESIAN_POINT ( 'NONE',  ( -72.92551479769302603, 94.57411849586699759, -93.49847958357699440 ) ) ;
#1218=ORIENTED_EDGE ( 'NONE', *, *, #10001, .F. ) ;
#1220=VERTEX_POINT ( 'NONE', #6661 ) ;
#1221=PLANE ( 'NONE',  #3828 ) ;
#1223=ORIENTED_EDGE ( 'NONE', *, *, #2209, .T. ) ;
#1224=ORIENTED_EDGE ( 'NONE', *, *, #9575, .F. ) ;
#1225=VERTEX_POINT ( 'NONE', #11371 ) ;
#1230=EDGE_CURVE ( 'NONE', #10445, #7422, #3149, .T. ) ;
#1232=FACE_OUTER_BOUND ( 'NONE', #12141, .T. ) ;
#1233=CARTESIAN_POINT ( 'NONE',  ( -86.77438362644001302, 110.1741184958670061, -15.85886927678779834 ) ) ;
#1235=DIRECTION ( 'NONE',  ( -1.000000000000000000, 0.000000000000000000, 0.000000000000000000 ) ) ;
#1236=ORIENTED_EDGE ( 'NONE', *, *, #10242, .T. ) ;
#1237=FACE_OUTER_BOUND ( 'NONE', #7306, .T. ) ;
#1244=DIRECTION ( 'NONE',  ( 0.000000000000000000, 0.000000000000000000, -1.000000000000000000 ) ) ;
#1247=EDGE_CURVE ( 'NONE', #12468, #4454, #13924, .T. ) ;
#1249=LINE ( 'NONE', #7699, #11092 ) ;
#1250=CARTESIAN_POINT ( 'NONE',  ( -69.77438362644001302, 82.17411849586700612, -112.9984795835769944 ) ) ;
#1251=CARTESIAN_POINT ( 'NONE',  ( -84.27438362643998460, 65.17411849586700612, -182.2484795835770228 ) ) ;
#1252=CARTESIAN_POINT ( 'NONE',  ( -52.77438362644100067, 101.5320169952374414, -147.9984795835769944 ) ) ;
#1253=CARTESIAN_POINT ( 'NONE',  ( -85.75338362643999801, 66.94254237039483257, -147.9984795835769944 ) ) ;
#1256=ORIENTED_EDGE ( 'NONE', *, *, #12725, .T. ) ;
#1257=EDGE_LOOP ( 'NONE', ( #13800, #5512, #2573, #2575 ) ) ;
#1258=EDGE_LOOP ( 'NONE', ( #8908, #11095, #11894 ) ) ;
#1261=EDGE_CURVE ( 'NONE', #9847, #1912, #11911, .T. ) ;
#1265=EDGE_CURVE ( 'NONE', #6718, #14328, #8183, .T. ) ;
#1268=DIRECTION ( 'NONE',  ( 1.000000000000000000, 0.000000000000000000, 0.000000000000000000 ) ) ;
#1270=ORIENTED_EDGE ( 'NONE', *, *, #2619, .T. ) ;
#1272=CARTESIAN_POINT ( 'NONE',  ( -86.77438362644100778, 99.17411849586700612, -145.2984795835770058 ) ) ;
#1274=EDGE_CURVE ( 'NONE', #2616, #5168, #11835, .T. ) ;
#1277=AXIS2_PLACEMENT_3D ( 'NONE', #954, #12606, #12752 ) ;
#1283=LINE ( 'NONE', #9500, #11918 ) ;
#1285=DIRECTION ( 'NONE',  ( -1.000000000000000000, 0.000000000000000000, 0.000000000000000000 ) ) ;
#1286=AXIS2_PLACEMENT_3D ( 'NONE', #784, #5541, #10396 ) ;
#1288=CARTESIAN_POINT ( 'NONE',  ( -86.77438362644001302, 99.17411849586700612, -145.4984795835769660 ) ) ;
#1291=DIRECTION ( 'NONE',  ( 0.000000000000000000, -0.000000000000000000, 1.000000000000000000 ) ) ;
#1293=VERTEX_POINT ( 'NONE', #1202 ) ;
#1294=CARTESIAN_POINT ( 'NONE',  ( -52.77438362644100067, 99.17411849586700612, -182.2484795835770228 ) ) ;
#1304=FACE_OUTER_BOUND ( 'NONE', #9267, .T. ) ;
#1305=LINE ( 'NONE', #10691, #9080 ) ;
#1307=CIRCLE ( 'NONE', #9731, 1.250000000000001110 ) ;
#1312=DIRECTION ( 'NONE',  ( 0.000000000000000000, 0.000000000000000000, -1.000000000000000000 ) ) ;
#1313=VERTEX_POINT ( 'NONE', #3611 ) ;
#1315=AXIS2_PLACEMENT_3D ( 'NONE', #14886, #4276, #9004 ) ;
#1317=EDGE_LOOP ( 'NONE', ( #5440, #5241, #14278, #9761 ) ) ;
#1320=DIRECTION ( 'NONE',  ( 0.000000000000000000, 0.000000000000000000, -1.000000000000000000 ) ) ;
#1323=PLANE ( 'NONE',  #4014 ) ;
#1326=VECTOR ( 'NONE', #14944, 1000.000000000000000 ) ;
#1328=CARTESIAN_POINT ( 'NONE',  ( -86.77438362644001302, 59.67411849586700612, -152.4984795835769944 ) ) ;
#1329=CARTESIAN_POINT ( 'NONE',  ( -90.52438362643999881, 65.17411849586700612, -150.4984795835770228 ) ) ;
#1334=PLANE ( 'NONE',  #1426 ) ;
#1336=ORIENTED_EDGE ( 'NONE', *, *, #3538, .F. ) ;
#1341=CIRCLE ( 'NONE', #1600, 10.20000000000000107 ) ;
#1348=CARTESIAN_POINT ( 'NONE',  ( -50.73238362643999722, 63.99516924618178848, -147.9984795835769944 ) ) ;
#1349=CARTESIAN_POINT ( 'NONE',  ( -35.27438362644000591, 0.000000000000000000, 0.000000000000000000 ) ) ;
#1355=CYLINDRICAL_SURFACE ( 'NONE', #8095, 4.500000000000003553 ) ;
#1356=EDGE_CURVE ( 'NONE', #12262, #8420, #14084, .T. ) ;
#1363=VECTOR ( 'NONE', #4751, 1000.000000000000000 ) ;
#1364=FACE_OUTER_BOUND ( 'NONE', #13451, .T. ) ;
#1365=CARTESIAN_POINT ( 'NONE',  ( -69.77438362644001302, 82.17411849586700612, -81.84847958357698872 ) ) ;
#1367=ADVANCED_FACE ( 'NONE', ( #4701 ), #5720, .T. ) ;
#1369=LINE ( 'NONE', #14320, #3433 ) ;
#1370=PLANE ( 'NONE',  #9719 ) ;
#1377=CIRCLE ( 'NONE', #3620, 2.750000000000002665 ) ;
#1378=CYLINDRICAL_SURFACE ( 'NONE', #12228, 4.249999999999996447 ) ;
#1382=CARTESIAN_POINT ( 'NONE',  ( -86.77438362644001302, 65.17411849586700612, -145.4984795835769660 ) ) ;
#1383=ADVANCED_FACE ( 'NONE', ( #3380 ), #12847, .F. ) ;
#1388=AXIS2_PLACEMENT_3D ( 'NONE', #1252, #10721, #2571 ) ;
#1389=CARTESIAN_POINT ( 'NONE',  ( -52.77438362643999881, 65.17411849586700612, -150.4984795835770228 ) ) ;
#1390=AXIS2_PLACEMENT_3D ( 'NONE', #5956, #5789, #10653 ) ;
#1391=ADVANCED_FACE ( 'NONE', ( #7342, #6036 ), #7420, .T. ) ;
#1397=LINE ( 'NONE', #7454, #10039 ) ;
#1398=EDGE_CURVE ( 'NONE', #8134, #15237, #9879, .T. ) ;
#1400=DIRECTION ( 'NONE',  ( -2.065146995210485003E-17, -4.130293990420970006E-17, -1.000000000000000000 ) ) ;
#1401=VERTEX_POINT ( 'NONE', #5006 ) ;
#1402=CARTESIAN_POINT ( 'NONE',  ( -86.77438362643999881, 65.17411849586700612, -145.2984795835770058 ) ) ;
#1403=VECTOR ( 'NONE', #11031, 1000.000000000000000 ) ;
#1405=VERTEX_POINT ( 'NONE', #12142 ) ;
#1406=VERTEX_POINT ( 'NONE', #7262 ) ;
#1407=VECTOR ( 'NONE', #2415, 1000.000000000000000 ) ;
#1409=DIRECTION ( 'NONE',  ( 1.000000000000000000, 0.000000000000000000, 0.000000000000000000 ) ) ;
#1411=DIRECTION ( 'NONE',  ( 0.000000000000000000, 0.000000000000000000, -1.000000000000000000 ) ) ;
#1413=FACE_OUTER_BOUND ( 'NONE', #9244, .T. ) ;
#1415=CARTESIAN_POINT ( 'NONE',  ( -52.77438362644100067, 99.17411849586700612, -182.2484795835770228 ) ) ;
#1420=LINE ( 'NONE', #14435, #807 ) ;
#1421=VERTEX_POINT ( 'NONE', #107 ) ;
#1426=AXIS2_PLACEMENT_3D ( 'NONE', #9631, #6324, #7323 ) ;
#1427=VECTOR ( 'NONE', #13016, 1000.000000000000000 ) ;
#1431=DIRECTION ( 'NONE',  ( 0.000000000000000000, 0.000000000000000000, -1.000000000000000000 ) ) ;
#1437=DIRECTION ( 'NONE',  ( 0.000000000000000000, 0.000000000000000000, -1.000000000000000000 ) ) ;
#1441=ORIENTED_EDGE ( 'NONE', *, *, #862, .T. ) ;
#1444=CIRCLE ( 'NONE', #6664, 4.500000000000003553 ) ;
#1445=CARTESIAN_POINT ( 'NONE',  ( -69.77438362644001302, 82.17411849586700612, -29.37106258560738681 ) ) ;
#1448=PLANE ( 'NONE',  #10022 ) ;
#1451=DIRECTION ( 'NONE',  ( -1.287488025362404182E-15, -1.000000000000000000, 0.000000000000000000 ) ) ;
#1452=CARTESIAN_POINT ( 'NONE',  ( -88.81638362644100937, 97.99516924618178848, -150.4984795835770228 ) ) ;
#1455=CIRCLE ( 'NONE', #3194, 2.042000000000002036 ) ;
#1459=VERTEX_POINT ( 'NONE', #7579 ) ;
#1462=ORIENTED_EDGE ( 'NONE', *, *, #8859, .F. ) ;
#1466=EDGE_CURVE ( 'NONE', #4666, #6139, #13389, .T. ) ;
#1468=CARTESIAN_POINT ( 'NONE',  ( -52.77438362643999881, 65.17411849586700612, -147.9984795835769944 ) ) ;
#1469=LINE ( 'NONE', #3713, #11498 ) ;
#1474=DIRECTION ( 'NONE',  ( 0.000000000000000000, 0.000000000000000000, 1.000000000000000000 ) ) ;
#1477=CARTESIAN_POINT ( 'NONE',  ( -57.27438362644000591, 99.17411849586700612, -79.59847958357700293 ) ) ;
#1480=ORIENTED_EDGE ( 'NONE', *, *, #8476, .F. ) ;
#1481=VERTEX_POINT ( 'NONE', #13233 ) ;
#1482=ORIENTED_EDGE ( 'NONE', *, *, #10428, .T. ) ;
#1483=CARTESIAN_POINT ( 'NONE',  ( -76.48108760497456160, 68.65632084656354550, -83.44847958357698303 ) ) ;
#1491=ADVANCED_FACE ( 'NONE', ( #10826 ), #1355, .F. ) ;
#1492=DIRECTION ( 'NONE',  ( 1.000000000000000000, 0.000000000000000000, 0.000000000000000000 ) ) ;
#1493=CARTESIAN_POINT ( 'NONE',  ( -80.52077156573417938, 59.67411849586701322, -79.59847958357700293 ) ) ;
#1494=DIRECTION ( 'NONE',  ( 0.5000000000000003331, 0.8660254037844384856, 0.000000000000000000 ) ) ;
#1496=CARTESIAN_POINT ( 'NONE',  ( -69.77438362643999881, 89.17411849586052597, -43.99847958364157563 ) ) ;
#1497=VERTEX_POINT ( 'NONE', #10976 ) ;
#1498=CARTESIAN_POINT ( 'NONE',  ( -88.81638362644000040, 63.99516924618178848, -150.4984795835770228 ) ) ;
#1499=ORIENTED_EDGE ( 'NONE', *, *, #5654, .F. ) ;
#1502=LINE ( 'NONE', #5308, #8712 ) ;
#1505=DIRECTION ( 'NONE',  ( -1.000000000000000000, 0.000000000000000000, 0.000000000000000000 ) ) ;
#1509=ORIENTED_EDGE ( 'NONE', *, *, #6408, .T. ) ;
#1510=DIRECTION ( 'NONE',  ( 0.000000000000000000, 0.000000000000000000, 1.000000000000000000 ) ) ;
#1516=VECTOR ( 'NONE', #12476, 1000.000000000000000 ) ;
#1520=CARTESIAN_POINT ( 'NONE',  ( -61.64938362644000591, 82.17411849586700612, -150.4984795835769944 ) ) ;
#1521=VECTOR ( 'NONE', #9793, 1000.000000000000000 ) ;
#1524=CARTESIAN_POINT ( 'NONE',  ( -50.02438362644000591, 99.17411849586700612, -86.49847958357699440 ) ) ;
#1526=AXIS2_PLACEMENT_3D ( 'NONE', #6553, #1657, #14598 ) ;
#1529=EDGE_CURVE ( 'NONE', #12869, #11817, #5089, .T. ) ;
#1530=ORIENTED_EDGE ( 'NONE', *, *, #6128, .T. ) ;
#1531=CARTESIAN_POINT ( 'NONE',  ( -69.77438362644001302, 79.67411849586700612, -67.69567958357700377 ) ) ;
#1534=ORIENTED_EDGE ( 'NONE', *, *, #15085, .T. ) ;
#1535=EDGE_CURVE ( 'NONE', #4454, #9228, #7870, .T. ) ;
#1537=DIRECTION ( 'NONE',  ( 0.000000000000000000, 0.000000000000000000, -1.000000000000000000 ) ) ;
#1541=DIRECTION ( 'NONE',  ( 0.000000000000000000, 0.000000000000000000, 1.000000000000000000 ) ) ;
#1543=DIRECTION ( 'NONE',  ( 0.000000000000000000, -1.000000000000000000, 0.000000000000000000 ) ) ;
#1544=CYLINDRICAL_SURFACE ( 'NONE', #15213, 8.050000000000000711 ) ;
#1545=ORIENTED_EDGE ( 'NONE', *, *, #10949, .F. ) ;
#1546=DIRECTION ( 'NONE',  ( -1.000000000000000000, 0.000000000000000000, 0.000000000000000000 ) ) ;
#1547=ADVANCED_FACE ( 'NONE', ( #12529 ), #1893, .F. ) ;
#1549=ORIENTED_EDGE ( 'NONE', *, *, #14757, .F. ) ;
#1552=AXIS2_PLACEMENT_3D ( 'NONE', #5721, #8030, #9413 ) ;
#1554=LINE ( 'NONE', #9921, #3084 ) ;
#1556=VECTOR ( 'NONE', #12230, 1000.000000000000000 ) ;
#1561=DIRECTION ( 'NONE',  ( 0.000000000000000000, 0.000000000000000000, 1.000000000000000000 ) ) ;
#1563=DIRECTION ( 'NONE',  ( 0.000000000000000000, 0.000000000000000000, -1.000000000000000000 ) ) ;
#1566=AXIS2_PLACEMENT_3D ( 'NONE', #4357, #8153, #15274 ) ;
#1567=DIRECTION ( 'NONE',  ( 0.000000000000000000, 0.000000000000000000, -1.000000000000000000 ) ) ;
#1570=EDGE_CURVE ( 'NONE', #3974, #1792, #10312, .T. ) ;
#1571=ORIENTED_EDGE ( 'NONE', *, *, #45, .T. ) ;
#1572=VECTOR ( 'NONE', #13214, 1000.000000000000000 ) ;
#1574=VERTEX_POINT ( 'NONE', #12604 ) ;
#1578=ADVANCED_FACE ( 'NONE', ( #13617 ), #3136, .F. ) ;
#1579=CIRCLE ( 'NONE', #11228, 6.999999999974082954 ) ;
#1581=DIRECTION ( 'NONE',  ( -1.000000000000000000, 0.000000000000000000, 0.000000000000000000 ) ) ;
#1582=CARTESIAN_POINT ( 'NONE',  ( -57.27438362644000591, 65.17411849586700612, -145.4984795835769660 ) ) ;
#1584=VECTOR ( 'NONE', #13522, 1000.000000000000000 ) ;
#1585=CARTESIAN_POINT ( 'NONE',  ( -69.77438362644001302, 82.17411849586700612, -79.49847958357700861 ) ) ;
#1586=DIRECTION ( 'NONE',  ( 0.000000000000000000, 0.000000000000000000, -1.000000000000000000 ) ) ;
#1588=VERTEX_POINT ( 'NONE', #11428 ) ;
#1590=CIRCLE ( 'NONE', #15189, 16.06499999999999773 ) ;
#1591=AXIS2_PLACEMENT_3D ( 'NONE', #4880, #4950, #11853 ) ;
#1594=LINE ( 'NONE', #14688, #2872 ) ;
#1596=ORIENTED_EDGE ( 'NONE', *, *, #3761, .T. ) ;
#1598=AXIS2_PLACEMENT_3D ( 'NONE', #279, #13111, #10771 ) ;
#1599=DIRECTION ( 'NONE',  ( 0.8660254037844383745, -0.5000000000000003331, 0.000000000000000000 ) ) ;
#1600=AXIS2_PLACEMENT_3D ( 'NONE', #3479, #3643, #10613 ) ;
#1601=VECTOR ( 'NONE', #2527, 1000.000000000000000 ) ;
#1603=PLANE ( 'NONE',  #5084 ) ;
#1604=LINE ( 'NONE', #11213, #2951 ) ;
#1606=CARTESIAN_POINT ( 'NONE',  ( -82.27438362643999881, 99.17411849586700612, -79.59847958357700293 ) ) ;
#1608=ORIENTED_EDGE ( 'NONE', *, *, #3942, .F. ) ;
#1611=DIRECTION ( 'NONE',  ( 0.000000000000000000, 0.000000000000000000, -1.000000000000000000 ) ) ;
#1613=ORIENTED_EDGE ( 'NONE', *, *, #3658, .F. ) ;
#1615=PLANE ( 'NONE',  #3743 ) ;
#1617=DIRECTION ( 'NONE',  ( 1.000000000000000000, 0.000000000000000000, 0.000000000000000000 ) ) ;
#1618=VECTOR ( 'NONE', #7431, 1000.000000000000000 ) ;
#1621=AXIS2_PLACEMENT_3D ( 'NONE', #10436, #14020, #5901 ) ;
#1623=EDGE_CURVE ( 'NONE', #4755, #14843, #9568, .T. ) ;
#1624=DIRECTION ( 'NONE',  ( 0.000000000000000000, 0.000000000000000000, 1.000000000000000000 ) ) ;
#1626=DIRECTION ( 'NONE',  ( -1.000000000000000000, 0.000000000000000000, 0.000000000000000000 ) ) ;
#1629=ORIENTED_EDGE ( 'NONE', *, *, #1265, .T. ) ;
#1630=AXIS2_PLACEMENT_3D ( 'NONE', #8697, #5453, #7701 ) ;
#1631=ORIENTED_EDGE ( 'NONE', *, *, #13248, .F. ) ;
#1632=EDGE_LOOP ( 'NONE', ( #12709, #14728 ) ) ;
#1634=DIRECTION ( 'NONE',  ( 0.000000000000000000, 0.000000000000000000, -1.000000000000000000 ) ) ;
#1639=DIRECTION ( 'NONE',  ( -0.000000000000000000, -0.000000000000000000, -1.000000000000000000 ) ) ;
#1640=EDGE_CURVE ( 'NONE', #1459, #11930, #5235, .T. ) ;
#1641=CARTESIAN_POINT ( 'NONE',  ( -80.52077156573417938, 110.1741184958670061, -152.4984795835769944 ) ) ;
#1642=DIRECTION ( 'NONE',  ( 0.000000000000000000, 0.000000000000000000, -1.000000000000000000 ) ) ;
#1643=CARTESIAN_POINT ( 'NONE',  ( -77.82438362644001018, 82.17411849586700612, -80.14847958357698587 ) ) ;
#1645=DIRECTION ( 'NONE',  ( 0.000000000000000000, 1.000000000000000000, 0.000000000000000000 ) ) ;
#1646=EDGE_CURVE ( 'NONE', #13582, #558, #4646, .T. ) ;
#1648=VECTOR ( 'NONE', #1960, 1000.000000000000000 ) ;
#1650=VECTOR ( 'NONE', #4516, 1000.000000000000114 ) ;
#1653=ORIENTED_EDGE ( 'NONE', *, *, #12485, .F. ) ;
#1656=EDGE_CURVE ( 'NONE', #3101, #11082, #1671, .T. ) ;
#1657=DIRECTION ( 'NONE',  ( 0.000000000000000000, 0.000000000000000000, 1.000000000000000000 ) ) ;
#1658=AXIS2_PLACEMENT_3D ( 'NONE', #14905, #12446, #6648 ) ;
#1660=DIRECTION ( 'NONE',  ( 0.000000000000000000, 0.000000000000000000, -1.000000000000000000 ) ) ;
#1664=LINE ( 'NONE', #8793, #9089 ) ;
#1665=CARTESIAN_POINT ( 'NONE',  ( -69.77438362644100778, 82.17411849586699191, -79.49847958357700861 ) ) ;
#1666=EDGE_CURVE ( 'NONE', #506, #877, #569, .T. ) ;
#1667=CARTESIAN_POINT ( 'NONE',  ( -77.52077156573416516, 59.67411849586701322, -152.4984795835769944 ) ) ;
#1668=EDGE_CURVE ( 'NONE', #15237, #1406, #14768, .T. ) ;
#1670=VECTOR ( 'NONE', #10957, 1000.000000000000000 ) ;
#1671=LINE ( 'NONE', #11358, #13323 ) ;
#1672=VECTOR ( 'NONE', #12373, 1000.000000000000000 ) ;
#1673=ORIENTED_EDGE ( 'NONE', *, *, #13413, .T. ) ;
#1677=ORIENTED_EDGE ( 'NONE', *, *, #12378, .F. ) ;
#1679=ADVANCED_FACE ( 'NONE', ( #12747 ), #9399, .F. ) ;
#1682=CARTESIAN_POINT ( 'NONE',  ( -69.77438362644001302, 90.17411849586700612, -79.49847958357700861 ) ) ;
#1685=DIRECTION ( 'NONE',  ( -0.000000000000000000, 1.000000000000000000, 0.000000000000000000 ) ) ;
#1689=VECTOR ( 'NONE', #7984, 1000.000000000000000 ) ;
#1692=ORIENTED_EDGE ( 'NONE', *, *, #11601, .T. ) ;
#1693=LINE ( 'NONE', #14485, #8282 ) ;
#1701=CARTESIAN_POINT ( 'NONE',  ( -101.2743836264399988, 57.67411849586700612, -79.49847958357700861 ) ) ;
#1702=ORIENTED_EDGE ( 'NONE', *, *, #11480, .T. ) ;
#1703=ORIENTED_EDGE ( 'NONE', *, *, #6023, .F. ) ;
#1710=CARTESIAN_POINT ( 'NONE',  ( -65.78565528768382364, 67.29799558322736175, -83.44847958357698303 ) ) ;
#1714=DIRECTION ( 'NONE',  ( -1.000000000000000000, 0.000000000000000000, 0.000000000000000000 ) ) ;
#1718=LINE ( 'NONE', #405, #1584 ) ;
#1719=ORIENTED_EDGE ( 'NONE', *, *, #2228, .T. ) ;
#1720=DIRECTION ( 'NONE',  ( 0.000000000000000000, 0.000000000000000000, -1.000000000000000000 ) ) ;
#1721=EDGE_LOOP ( 'NONE', ( #15325, #9614, #7601, #1653, #1702 ) ) ;
#1723=ORIENTED_EDGE ( 'NONE', *, *, #11348, .T. ) ;
#1724=UNCERTAINTY_MEASURE_WITH_UNIT (LENGTH_MEASURE( 1.000000000000000082E-05 ), #10709, 'distance_accuracy_value', 'NONE');
#1727=CARTESIAN_POINT ( 'NONE',  ( -69.77438362644001302, 90.17411849586700612, -58.99847958357700151 ) ) ;
#1729=DIRECTION ( 'NONE',  ( 0.000000000000000000, 0.000000000000000000, 1.000000000000000000 ) ) ;
#1730=DIRECTION ( 'NONE',  ( 0.000000000000000000, 0.000000000000000000, 1.000000000000000000 ) ) ;
#1735=CARTESIAN_POINT ( 'NONE',  ( -69.77438362644100778, 82.17411849586699191, -67.49847958357700861 ) ) ;
#1737=ADVANCED_FACE ( 'NONE', ( #12669 ), #8168, .F. ) ;
#1738=ORIENTED_EDGE ( 'NONE', *, *, #2710, .T. ) ;
#1743=DIRECTION ( 'NONE',  ( -1.000000000000000000, 0.000000000000000000, 0.000000000000000000 ) ) ;
#1746=EDGE_CURVE ( 'NONE', #12096, #14091, #2664, .T. ) ;
#1748=CARTESIAN_POINT ( 'NONE',  ( -52.77438362643999881, 65.17411849586700612, -145.4984795835769944 ) ) ;
#1749=ADVANCED_FACE ( 'NONE', ( #8009 ), #2911, .F. ) ;
#1751=CARTESIAN_POINT ( 'NONE',  ( -69.77438362644001302, 110.1741184958670061, -152.4984795835769944 ) ) ;
#1753=VERTEX_POINT ( 'NONE', #14134 ) ;
#1755=EDGE_CURVE ( 'NONE', #8497, #5254, #8091, .T. ) ;
#1757=AXIS2_PLACEMENT_3D ( 'NONE', #13264, #3946, #2774 ) ;
#1758=CARTESIAN_POINT ( 'NONE',  ( -54.81638362644000040, 63.99516924618178848, -147.9984795835769944 ) ) ;
#1760=EDGE_LOOP ( 'NONE', ( #9418, #4584, #11504, #11247, #110, #7784 ) ) ;
#1761=ADVANCED_FACE ( 'NONE', ( #10643, #2117 ), #8245, .F. ) ;
#1762=EDGE_CURVE ( 'NONE', #4888, #4114, #15061, .T. ) ;
#1766=FACE_OUTER_BOUND ( 'NONE', #14367, .T. ) ;
#1770=ORIENTED_EDGE ( 'NONE', *, *, #2864, .T. ) ;
#1772=ORIENTED_EDGE ( 'NONE', *, *, #13010, .F. ) ;
#1774=VERTEX_POINT ( 'NONE', #4756 ) ;
#1776=ORIENTED_EDGE ( 'NONE', *, *, #6424, .F. ) ;
#1777=ORIENTED_EDGE ( 'NONE', *, *, #12434, .T. ) ;
#1778=AXIS2_PLACEMENT_3D ( 'NONE', #10159, #14891, #7310 ) ;
#1780=CIRCLE ( 'NONE', #9948, 1.250000000000001110 ) ;
#1786=CIRCLE ( 'NONE', #8475, 2.500000000000002220 ) ;
#1787=DIRECTION ( 'NONE',  ( -0.000000000000000000, -0.000000000000000000, 1.000000000000000000 ) ) ;
#1789=CARTESIAN_POINT ( 'NONE',  ( -88.81638362644100937, 97.99516924618178848, -147.9984795835769944 ) ) ;
#1790=DIRECTION ( 'NONE',  ( 0.000000000000000000, -1.000000000000000000, 0.000000000000000000 ) ) ;
#1792=VERTEX_POINT ( 'NONE', #11655 ) ;
#1794=CIRCLE ( 'NONE', #10202, 16.06499999999999773 ) ;
#1795=VERTEX_POINT ( 'NONE', #12899 ) ;
#1800=FACE_OUTER_BOUND ( 'NONE', #11038, .T. ) ;
#1801=CIRCLE ( 'NONE', #10466, 1.250000000000001110 ) ;
#1803=LINE ( 'NONE', #5314, #5906 ) ;
#1804=DIRECTION ( 'NONE',  ( 0.000000000000000000, 0.000000000000000000, 1.000000000000000000 ) ) ;
#1806=AXIS2_PLACEMENT_3D ( 'NONE', #6432, #13562, #2759 ) ;
#1808=ORIENTED_EDGE ( 'NONE', *, *, #243, .T. ) ;
#1811=EDGE_LOOP ( 'NONE', ( #11659, #8970, #5653 ) ) ;
#1813=VERTEX_POINT ( 'NONE', #6788 ) ;
#1816=ORIENTED_EDGE ( 'NONE', *, *, #1656, .F. ) ;
#1818=FACE_OUTER_BOUND ( 'NONE', #14215, .T. ) ;
#1819=DIRECTION ( 'NONE',  ( 1.000000000000000000, 0.000000000000000000, 0.000000000000000000 ) ) ;
#1820=CARTESIAN_POINT ( 'NONE',  ( -57.27438362644000591, 99.17411849586700612, -145.4984795835769660 ) ) ;
#1822=AXIS2_PLACEMENT_3D ( 'NONE', #9717, #12067, #7575 ) ;
#1827=DIRECTION ( 'NONE',  ( 0.000000000000000000, 0.000000000000000000, -1.000000000000000000 ) ) ;
#1828=CARTESIAN_POINT ( 'NONE',  ( -69.77438362644001302, 82.17411849586700612, -79.59847958357700293 ) ) ;
#1832=ORIENTED_EDGE ( 'NONE', *, *, #9595, .T. ) ;
#1835=ORIENTED_EDGE ( 'NONE', *, *, #143, .T. ) ;
#1839=CARTESIAN_POINT ( 'NONE',  ( -88.81638362644000040, 66.35306774555222376, -150.4984795835770228 ) ) ;
#1840=ADVANCED_FACE ( 'NONE', ( #8330 ), #3823, .T. ) ;
#1841=DIRECTION ( 'NONE',  ( -1.287488025362404182E-15, -1.000000000000000000, 0.000000000000000000 ) ) ;
#1842=DIRECTION ( 'NONE',  ( 0.000000000000000000, 0.000000000000000000, 1.000000000000000000 ) ) ;
#1846=AXIS2_PLACEMENT_3D ( 'NONE', #12744, #2113, #3999 ) ;
#1848=DIRECTION ( 'NONE',  ( 1.000000000000000000, 0.000000000000000000, 0.000000000000000000 ) ) ;
#1849=ADVANCED_FACE ( 'NONE', ( #3740 ), #1334, .F. ) ;
#1851=CARTESIAN_POINT ( 'NONE',  ( -88.81638362644100937, 100.3530677455522238, -150.4984795835770228 ) ) ;
#1856=VERTEX_POINT ( 'NONE', #13298 ) ;
#1860=VECTOR ( 'NONE', #5540, 1000.000000000000000 ) ;
#1861=DIRECTION ( 'NONE',  ( 0.000000000000000000, -0.000000000000000000, 1.000000000000000000 ) ) ;
#1864=LINE ( 'NONE', #13738, #14193 ) ;
#1865=EDGE_CURVE ( 'NONE', #12872, #13910, #10889, .T. ) ;
#1867=DIRECTION ( 'NONE',  ( -1.000000000000000000, 0.000000000000000000, 0.000000000000000000 ) ) ;
#1869=DIRECTION ( 'NONE',  ( 0.000000000000000000, 0.000000000000000000, -1.000000000000000000 ) ) ;
#1870=CARTESIAN_POINT ( 'NONE',  ( -104.2743836264399988, 101.6741184958670061, -79.49847958357700861 ) ) ;
#1872=ORIENTED_EDGE ( 'NONE', *, *, #5140, .T. ) ;
#1876=VECTOR ( 'NONE', #9651, 1000.000000000000000 ) ;
#1879=AXIS2_PLACEMENT_3D ( 'NONE', #1991, #14862, #4332 ) ;
#1880=FACE_OUTER_BOUND ( 'NONE', #11161, .T. ) ;
#1882=PLANE ( 'NONE',  #893 ) ;
#1883=DIRECTION ( 'NONE',  ( 0.000000000000000000, 0.000000000000000000, -1.000000000000000000 ) ) ;
#1884=LINE ( 'NONE', #12741, #5887 ) ;
#1886=AXIS2_PLACEMENT_3D ( 'NONE', #8104, #8023, #806 ) ;
#1887=DIRECTION ( 'NONE',  ( -0.000000000000000000, -0.000000000000000000, 1.000000000000000000 ) ) ;
#1890=FACE_OUTER_BOUND ( 'NONE', #3846, .T. ) ;
#1891=CARTESIAN_POINT ( 'NONE',  ( -42.77438362644000591, 104.6741184958670061, -15.85886927678779834 ) ) ;
#1892=ORIENTED_EDGE ( 'NONE', *, *, #9615, .T. ) ;
#1893=CYLINDRICAL_SURFACE ( 'NONE', #1658, 4.499999999999997335 ) ;
#1895=DIRECTION ( 'NONE',  ( 0.000000000000000000, -1.000000000000000000, 0.000000000000000000 ) ) ;
#1897=ORIENTED_EDGE ( 'NONE', *, *, #2710, .F. ) ;
#1898=CIRCLE ( 'NONE', #12793, 4.500000000000003553 ) ;
#1900=ORIENTED_EDGE ( 'NONE', *, *, #15000, .T. ) ;
#1902=ADVANCED_FACE ( 'NONE', ( #3673 ), #911, .F. ) ;
#1903=DIRECTION ( 'NONE',  ( 0.000000000000000000, 0.000000000000000000, 1.000000000000000000 ) ) ;
#1906=VECTOR ( 'NONE', #3184, 1000.000000000000000 ) ;
#1909=DIRECTION ( 'NONE',  ( 0.8660254037844387076, 0.4999999999999998890, 0.000000000000000000 ) ) ;
#1910=FACE_OUTER_BOUND ( 'NONE', #9957, .T. ) ;
#1911=CARTESIAN_POINT ( 'NONE',  ( -86.77438362644001302, 99.17411849586700612, -86.49847958357699440 ) ) ;
#1912=VERTEX_POINT ( 'NONE', #14593 ) ;
#1913=DIRECTION ( 'NONE',  ( 0.000000000000000000, -1.000000000000000000, 0.000000000000000000 ) ) ;
#1918=DIRECTION ( 'NONE',  ( -1.000000000000000000, 0.000000000000000000, 0.000000000000000000 ) ) ;
#1919=EDGE_CURVE ( 'NONE', #13427, #12323, #4840, .T. ) ;
#1920=CARTESIAN_POINT ( 'NONE',  ( -64.53565528768383786, 67.29799558322736175, -83.44847958357698303 ) ) ;
#1925=CARTESIAN_POINT ( 'NONE',  ( -52.77438362644000591, 65.17411849586700612, -145.4984795835769660 ) ) ;
#1926=CIRCLE ( 'NONE', #12335, 8.000000000000007105 ) ;
#1928=DIRECTION ( 'NONE',  ( 0.000000000000000000, 0.000000000000000000, 1.000000000000000000 ) ) ;
#1929=ORIENTED_EDGE ( 'NONE', *, *, #7103, .F. ) ;
#1932=ORIENTED_EDGE ( 'NONE', *, *, #2223, .T. ) ;
#1938=VECTOR ( 'NONE', #4896, 1000.000000000000000 ) ;
#1941=LINE ( 'NONE', #7628, #5786 ) ;
#1943=CARTESIAN_POINT ( 'NONE',  ( -47.27438362644100778, 114.1741184958670061, -67.49847958357700861 ) ) ;
#1947=DIRECTION ( 'NONE',  ( -0.000000000000000000, -0.000000000000000000, 1.000000000000000000 ) ) ;
#1948=EDGE_CURVE ( 'NONE', #15131, #14575, #12129, .T. ) ;
#1949=ORIENTED_EDGE ( 'NONE', *, *, #7451, .F. ) ;
#1951=VECTOR ( 'NONE', #15321, 1000.000000000000114 ) ;
#1952=VERTEX_POINT ( 'NONE', #5151 ) ;
#1954=EDGE_CURVE ( 'NONE', #11451, #10071, #9980, .T. ) ;
#1955=CYLINDRICAL_SURFACE ( 'NONE', #9456, 16.00000000000000000 ) ;
#1957=ADVANCED_FACE ( 'NONE', ( #9552 ), #14296, .F. ) ;
#1958=PLANE ( 'NONE',  #13997 ) ;
#1959=CARTESIAN_POINT ( 'NONE',  ( -84.02438362643999881, 99.17411849586700612, -152.4984795835769944 ) ) ;
#1960=DIRECTION ( 'NONE',  ( -1.000000000000000000, 0.000000000000000000, 0.000000000000000000 ) ) ;
#1963=CARTESIAN_POINT ( 'NONE',  ( -73.64736697264743270, 75.17411849586699191, -44.99847958359794120 ) ) ;
#1965=DIRECTION ( 'NONE',  ( -1.000000000000000000, 0.000000000000000000, 0.000000000000000000 ) ) ;
#1970=EDGE_LOOP ( 'NONE', ( #6035, #5031, #9706, #12276 ) ) ;
#1971=ORIENTED_EDGE ( 'NONE', *, *, #2292, .T. ) ;
#1973=DIRECTION ( 'NONE',  ( 0.000000000000000000, 0.000000000000000000, 1.000000000000000000 ) ) ;
#1976=CARTESIAN_POINT ( 'NONE',  ( -73.01311196519618818, 67.29799558322736175, -83.44847958357698303 ) ) ;
#1977=DIRECTION ( 'NONE',  ( -1.000000000000000000, 0.000000000000000000, 0.000000000000000000 ) ) ;
#1982=ORIENTED_EDGE ( 'NONE', *, *, #15000, .F. ) ;
#1983=CARTESIAN_POINT ( 'NONE',  ( -69.77438362644001302, 82.17411849586700612, -80.14847958357698587 ) ) ;
#1985=ORIENTED_EDGE ( 'NONE', *, *, #4142, .T. ) ;
#1986=CARTESIAN_POINT ( 'NONE',  ( -86.77438362644100778, 99.17411849586700612, -182.2484795835770228 ) ) ;
#1987=LINE ( 'NONE', #744, #2404 ) ;
#1989=DIRECTION ( 'NONE',  ( -1.000000000000000000, 0.000000000000000000, 0.000000000000000000 ) ) ;
#1991=CARTESIAN_POINT ( 'NONE',  ( -52.77438362643999881, 65.17411849586700612, -147.9984795835769944 ) ) ;
#1993=DIRECTION ( 'NONE',  ( 1.000000000000000000, 0.000000000000000000, 0.000000000000000000 ) ) ;
#1994=ORIENTED_EDGE ( 'NONE', *, *, #14565, .F. ) ;
#1995=CARTESIAN_POINT ( 'NONE',  ( -104.2743836264399988, 111.1741184958670061, -79.49847958357700861 ) ) ;
#1997=ORIENTED_EDGE ( 'NONE', *, *, #6881, .T. ) ;
#1998=ORIENTED_EDGE ( 'NONE', *, *, #2383, .T. ) ;
#2000=ORIENTED_EDGE ( 'NONE', *, *, #7459, .T. ) ;
#2002=AXIS2_PLACEMENT_3D ( 'NONE', #14613, #10183, #11207 ) ;
#2005=AXIS2_PLACEMENT_3D ( 'NONE', #14400, #11005, #6369 ) ;
#2009=PLANE ( 'NONE',  #10070 ) ;
#2010=CARTESIAN_POINT ( 'NONE',  ( -69.77438362644001302, 82.17411849586700612, -150.4984795835769944 ) ) ;
#2012=CARTESIAN_POINT ( 'NONE',  ( -102.2743836264399988, 99.17411849586700612, -152.4984795835769944 ) ) ;
#2015=CARTESIAN_POINT ( 'NONE',  ( -50.27438362644099357, 99.17411849586700612, -79.59847958357700293 ) ) ;
#2016=AXIS2_PLACEMENT_3D ( 'NONE', #14304, #14222, #1505 ) ;
#2018=CARTESIAN_POINT ( 'NONE',  ( -77.52077156573416516, 60.67411849586702743, -79.59847958357700293 ) ) ;
#2020=EDGE_CURVE ( 'NONE', #10091, #4114, #10233, .T. ) ;
#2022=AXIS2_PLACEMENT_3D ( 'NONE', #12202, #14674, #13532 ) ;
#2023=VERTEX_POINT ( 'NONE', #8930 ) ;
#2024=EDGE_LOOP ( 'NONE', ( #13150, #5457, #12095, #8818 ) ) ;
#2026=AXIS2_PLACEMENT_3D ( 'NONE', #6583, #8815, #12467 ) ;
#2029=EDGE_CURVE ( 'NONE', #12869, #8331, #13747, .T. ) ;
#2031=EDGE_CURVE ( 'NONE', #7017, #12917, #7705, .T. ) ;
#2032=CARTESIAN_POINT ( 'NONE',  ( -69.09337542095325091, 75.17411849586699191, -44.02377680093032097 ) ) ;
#2033=DIRECTION ( 'NONE',  ( 0.000000000000000000, 0.000000000000000000, 1.000000000000000000 ) ) ;
#2034=AXIS2_PLACEMENT_3D ( 'NONE', #9158, #11644, #6704 ) ;
#2037=LINE ( 'NONE', #1020, #12517 ) ;
#2043=ORIENTED_EDGE ( 'NONE', *, *, #2020, .T. ) ;
#2044=EDGE_CURVE ( 'NONE', #10133, #13729, #2806, .T. ) ;
#2046=CYLINDRICAL_SURFACE ( 'NONE', #13670, 1.500000000000001332 ) ;
#2047=ORIENTED_EDGE ( 'NONE', *, *, #12073, .T. ) ;
#2049=ORIENTED_EDGE ( 'NONE', *, *, #13972, .F. ) ;
#2050=CIRCLE ( 'NONE', #813, 3.000000000000002665 ) ;
#2057=CYLINDRICAL_SURFACE ( 'NONE', #13482, 2.750000000000002665 ) ;
#2062=VERTEX_POINT ( 'NONE', #13668 ) ;
#2063=VECTOR ( 'NONE', #3488, 1000.000000000000000 ) ;
#2065=EDGE_LOOP ( 'NONE', ( #2140, #3233, #8362, #2049 ) ) ;
#2067=VECTOR ( 'NONE', #2260, 1000.000000000000000 ) ;
#2068=CARTESIAN_POINT ( 'NONE',  ( -52.77438362643999881, 62.81621999649657084, -150.4984795835770228 ) ) ;
#2069=AXIS2_PLACEMENT_3D ( 'NONE', #8203, #5589, #5671 ) ;
#2071=FACE_OUTER_BOUND ( 'NONE', #12830, .T. ) ;
#2073=ORIENTED_EDGE ( 'NONE', *, *, #4785, .T. ) ;
#2074=CARTESIAN_POINT ( 'NONE',  ( -86.77438362643999881, 65.17411849586700612, -150.4984795835770228 ) ) ;
#2078=VERTEX_POINT ( 'NONE', #5386 ) ;
#2080=ORIENTED_EDGE ( 'NONE', *, *, #607, .F. ) ;
#2081=ORIENTED_EDGE ( 'NONE', *, *, #2104, .F. ) ;
#2088=EDGE_CURVE ( 'NONE', #9247, #7059, #485, .T. ) ;
#2091=LINE ( 'NONE', #1943, #6900 ) ;
#2093=DIRECTION ( 'NONE',  ( 0.000000000000000000, 0.000000000000000000, -1.000000000000000000 ) ) ;
#2094=CARTESIAN_POINT ( 'NONE',  ( -42.77438362644000591, 104.6741184958670061, -152.4984795835769944 ) ) ;
#2096=CARTESIAN_POINT ( 'NONE',  ( -69.77438362644001302, 94.57411849586699759, -89.99847958357699440 ) ) ;
#2097=EDGE_LOOP ( 'NONE', ( #13143, #668, #3903, #9455 ) ) ;
#2100=TOROIDAL_SURFACE ( 'NONE', #3594, 2.700000000000000178, 0.2000000000000000111 ) ;
#2101=VECTOR ( 'NONE', #5397, 1000.000000000000000 ) ;
#2102=LINE ( 'NONE', #6852, #3272 ) ;
#2103=VECTOR ( 'NONE', #14131, 1000.000000000000000 ) ;
#2104=EDGE_CURVE ( 'NONE', #9860, #10234, #9737, .T. ) ;
#2107=DIRECTION ( 'NONE',  ( -0.000000000000000000, -0.000000000000000000, 1.000000000000000000 ) ) ;
#2109=DIRECTION ( 'NONE',  ( -0.000000000000000000, -0.000000000000000000, 1.000000000000000000 ) ) ;
#2113=DIRECTION ( 'NONE',  ( 0.000000000000000000, 0.000000000000000000, -1.000000000000000000 ) ) ;
#2114=VECTOR ( 'NONE', #10222, 1000.000000000000000 ) ;
#2115=ORIENTED_EDGE ( 'NONE', *, *, #5726, .T. ) ;
#2117=FACE_BOUND ( 'NONE', #14397, .T. ) ;
#2118=ORIENTED_EDGE ( 'NONE', *, *, #10917, .F. ) ;
#2120=DIRECTION ( 'NONE',  ( -1.000000000000000000, 0.000000000000000000, 0.000000000000000000 ) ) ;
#2123=VERTEX_POINT ( 'NONE', #5455 ) ;
#2127=AXIS2_PLACEMENT_3D ( 'NONE', #13772, #3147, #7880 ) ;
#2131=EDGE_CURVE ( 'NONE', #4691, #4583, #814, .T. ) ;
#2133=CARTESIAN_POINT ( 'NONE',  ( -52.77438362644000591, 82.17411849586700612, -79.59847958357700293 ) ) ;
#2139=AXIS2_PLACEMENT_3D ( 'NONE', #2254, #5931, #14125 ) ;
#2140=ORIENTED_EDGE ( 'NONE', *, *, #11227, .T. ) ;
#2146=FACE_BOUND ( 'NONE', #573, .T. ) ;
#2147=EDGE_CURVE ( 'NONE', #7923, #11451, #6921, .T. ) ;
#2149=FACE_OUTER_BOUND ( 'NONE', #13147, .T. ) ;
#2152=CARTESIAN_POINT ( 'NONE',  ( -54.81638362644100226, 100.3530677455522238, -147.9984795835769944 ) ) ;
#2155=ORIENTED_EDGE ( 'NONE', *, *, #10470, .F. ) ;
#2157=ORIENTED_EDGE ( 'NONE', *, *, #4679, .F. ) ;
#2158=EDGE_LOOP ( 'NONE', ( #8629, #9535, #10726, #7373 ) ) ;
#2166=AXIS2_PLACEMENT_3D ( 'NONE', #11885, #12122, #1492 ) ;
#2167=FACE_OUTER_BOUND ( 'NONE', #6971, .T. ) ;
#2169=DIRECTION ( 'NONE',  ( 0.000000000000000000, 0.000000000000000000, -1.000000000000000000 ) ) ;
#2171=DIRECTION ( 'NONE',  ( 0.000000000000000000, 0.000000000000000000, 1.000000000000000000 ) ) ;
#2172=ORIENTED_EDGE ( 'NONE', *, *, #13987, .F. ) ;
#2173=CARTESIAN_POINT ( 'NONE',  ( -89.27438362643999881, 65.17411849586700612, -145.2984795835770058 ) ) ;
#2176=ORIENTED_EDGE ( 'NONE', *, *, #6800, .F. ) ;
#2179=AXIS2_PLACEMENT_3D ( 'NONE', #14406, #11791, #8379 ) ;
#2180=DIRECTION ( 'NONE',  ( 0.000000000000000000, 0.000000000000000000, 1.000000000000000000 ) ) ;
#2183=DIRECTION ( 'NONE',  ( -1.000000000000000000, 0.000000000000000000, 0.000000000000000000 ) ) ;
#2184=CARTESIAN_POINT ( 'NONE',  ( -69.77438362644001302, 82.17411849586700612, -80.44847958357698303 ) ) ;
#2186=CARTESIAN_POINT ( 'NONE',  ( -52.77438362644000591, 99.17411849586700612, -86.49847958357699440 ) ) ;
#2187=DIRECTION ( 'NONE',  ( -1.000000000000000000, 0.000000000000000000, -0.000000000000000000 ) ) ;
#2188=DIRECTION ( 'NONE',  ( 0.000000000000000000, 0.000000000000000000, -1.000000000000000000 ) ) ;
#2189=CARTESIAN_POINT ( 'NONE',  ( -69.77438362644001302, 82.17411849586700612, -80.14847958357698587 ) ) ;
#2196=CARTESIAN_POINT ( 'NONE',  ( -75.01311196519617397, 67.29799558322736175, -83.44847958357698303 ) ) ;
#2198=EDGE_CURVE ( 'NONE', #15131, #10091, #10388, .T. ) ;
#2202=CIRCLE ( 'NONE', #15069, 2.500000000000002220 ) ;
#2203=CYLINDRICAL_SURFACE ( 'NONE', #2757, 2.000000000000001776 ) ;
#2204=CARTESIAN_POINT ( 'NONE',  ( -104.2743836264399988, 60.67411849586700612, -67.49847958357700861 ) ) ;
#2205=DIRECTION ( 'NONE',  ( 1.000000000000000000, 0.000000000000000000, 0.000000000000000000 ) ) ;
#2207=ORIENTED_EDGE ( 'NONE', *, *, #14548, .F. ) ;
#2209=EDGE_CURVE ( 'NONE', #6162, #6907, #7280, .T. ) ;
#2210=CARTESIAN_POINT ( 'NONE',  ( -50.73238362644099197, 97.99516924618178848, -150.4984795835770228 ) ) ;
#2212=ADVANCED_FACE ( 'NONE', ( #3338, #3256 ), #2328, .T. ) ;
#2214=VERTEX_POINT ( 'NONE', #2018 ) ;
#2217=ADVANCED_FACE ( 'NONE', ( #11797 ), #12651, .F. ) ;
#2218=ADVANCED_FACE ( 'NONE', ( #7990 ), #1006, .T. ) ;
#2219=CARTESIAN_POINT ( 'NONE',  ( -50.73238362643999722, 66.35306774555222376, -147.9984795835769944 ) ) ;
#2223=EDGE_CURVE ( 'NONE', #4691, #4583, #8070, .T. ) ;
#2226=DIRECTION ( 'NONE',  ( 0.000000000000000000, 0.000000000000000000, -1.000000000000000000 ) ) ;
#2228=EDGE_CURVE ( 'NONE', #1792, #11018, #6049, .T. ) ;
#2231=ORIENTED_EDGE ( 'NONE', *, *, #3280, .F. ) ;
#2232=ORIENTED_EDGE ( 'NONE', *, *, #7566, .T. ) ;
#2242=DIRECTION ( 'NONE',  ( 0.000000000000000000, 0.000000000000000000, -1.000000000000000000 ) ) ;
#2243=ADVANCED_FACE ( 'NONE', ( #7920 ), #6769, .F. ) ;
#2245=LINE ( 'NONE', #4819, #14938 ) ;
#2246=ORIENTED_EDGE ( 'NONE', *, *, #1948, .T. ) ;
#2249=CIRCLE ( 'NONE', #12908, 5.500000000000005329 ) ;
#2251=VERTEX_POINT ( 'NONE', #2173 ) ;
#2254=CARTESIAN_POINT ( 'NONE',  ( -69.77438362644001302, 82.17411849586700612, -82.44847958357698303 ) ) ;
#2255=DIRECTION ( 'NONE',  ( -1.000000000000000000, 0.000000000000000000, 0.000000000000000000 ) ) ;
#2260=DIRECTION ( 'NONE',  ( 0.8660254037844387076, 0.4999999999999998890, 0.000000000000000000 ) ) ;
#2262=LINE ( 'NONE', #5778, #11970 ) ;
#2264=EDGE_LOOP ( 'NONE', ( #2000, #5533, #4670, #12676 ) ) ;
#2265=CARTESIAN_POINT ( 'NONE',  ( -86.77438362644100778, 96.81621999649657084, -147.9984795835769944 ) ) ;
#2267=ORIENTED_EDGE ( 'NONE', *, *, #2486, .T. ) ;
#2277=DIRECTION ( 'NONE',  ( -1.000000000000000000, 0.000000000000000000, 0.000000000000000000 ) ) ;
#2280=DIRECTION ( 'NONE',  ( 0.000000000000000000, 0.000000000000000000, 1.000000000000000000 ) ) ;
#2281=ORIENTED_EDGE ( 'NONE', *, *, #13625, .F. ) ;
#2283=DIRECTION ( 'NONE',  ( 0.000000000000000000, 0.000000000000000000, 1.000000000000000000 ) ) ;
#2286=ORIENTED_EDGE ( 'NONE', *, *, #2428, .T. ) ;
#2291=LINE ( 'NONE', #7042, #13893 ) ;
#2292=EDGE_CURVE ( 'NONE', #9398, #2214, #13224, .T. ) ;
#2295=CARTESIAN_POINT ( 'NONE',  ( -77.52077156573416516, 110.1741184958670061, -15.85886927678779834 ) ) ;
#2299=CARTESIAN_POINT ( 'NONE',  ( -52.77438362644000591, 99.17411849586700612, -152.4984795835769944 ) ) ;
#2303=VERTEX_POINT ( 'NONE', #6995 ) ;
#2309=VECTOR ( 'NONE', #4461, 1000.000000000000114 ) ;
#2310=AXIS2_PLACEMENT_3D ( 'NONE', #6451, #11014, #13724 ) ;
#2313=DIRECTION ( 'NONE',  ( -0.000000000000000000, -0.000000000000000000, 1.000000000000000000 ) ) ;
#2314=EDGE_CURVE ( 'NONE', #5254, #877, #14414, .T. ) ;
#2318=DIRECTION ( 'NONE',  ( 0.000000000000000000, 1.000000000000000000, 0.000000000000000000 ) ) ;
#2319=ADVANCED_FACE ( 'NONE', ( #11948 ), #11732, .F. ) ;
#2320=EDGE_CURVE ( 'NONE', #9847, #9368, #13948, .T. ) ;
#2324=CIRCLE ( 'NONE', #11004, 8.050000000000000711 ) ;
#2326=DIRECTION ( 'NONE',  ( 0.000000000000000000, 0.000000000000000000, -1.000000000000000000 ) ) ;
#2328=PLANE ( 'NONE',  #5036 ) ;
#2329=EDGE_CURVE ( 'NONE', #469, #6326, #8530, .T. ) ;
#2330=ORIENTED_EDGE ( 'NONE', *, *, #15085, .F. ) ;
#2331=ORIENTED_EDGE ( 'NONE', *, *, #7272, .T. ) ;
#2336=CIRCLE ( 'NONE', #6566, 2.500000000000002220 ) ;
#2340=DIRECTION ( 'NONE',  ( 1.000000000000000000, 1.727704675731647582E-15, 0.000000000000000000 ) ) ;
#2345=DIRECTION ( 'NONE',  ( 0.000000000000000000, 0.000000000000000000, -1.000000000000000000 ) ) ;
#2348=CONICAL_SURFACE ( 'NONE', #8283, 10.49999999999999467, 0.7853981633974497223 ) ;
#2349=ORIENTED_EDGE ( 'NONE', *, *, #811, .F. ) ;
#2350=ORIENTED_EDGE ( 'NONE', *, *, #7668, .T. ) ;
#2351=CARTESIAN_POINT ( 'NONE',  ( -88.81638362644000040, 63.99516924618178848, -147.9984795835769944 ) ) ;
#2354=CIRCLE ( 'NONE', #4612, 1.500000000000001332 ) ;
#2359=AXIS2_PLACEMENT_3D ( 'NONE', #12424, #1563, #2962 ) ;
#2360=LINE ( 'NONE', #10655, #12731 ) ;
#2361=VERTEX_POINT ( 'NONE', #1477 ) ;
#2362=DIRECTION ( 'NONE',  ( 0.000000000000000000, 0.000000000000000000, -1.000000000000000000 ) ) ;
#2363=DIRECTION ( 'NONE',  ( -0.000000000000000000, -0.000000000000000000, -1.000000000000000000 ) ) ;
#2364=MECHANICAL_DESIGN_GEOMETRIC_PRESENTATION_REPRESENTATION('',(#9545),#388);
#2365=VERTEX_POINT ( 'NONE', #10934 ) ;
#2368=ORIENTED_EDGE ( 'NONE', *, *, #322, .T. ) ;
#2373=AXIS2_PLACEMENT_3D ( 'NONE', #2761, #361, #7515 ) ;
#2377=PLANE ( 'NONE',  #5028 ) ;
#2379=FACE_OUTER_BOUND ( 'NONE', #213, .T. ) ;
#2383=EDGE_CURVE ( 'NONE', #9574, #1401, #10980, .T. ) ;
#2388=VERTEX_POINT ( 'NONE', #8450 ) ;
#2390=EDGE_LOOP ( 'NONE', ( #14213, #2461 ) ) ;
#2391=ADVANCED_FACE ( 'NONE', ( #10703 ), #7387, .F. ) ;
#2392=ORIENTED_EDGE ( 'NONE', *, *, #8193, .T. ) ;
#2395=DIRECTION ( 'NONE',  ( -1.000000000000000000, 0.000000000000000000, 0.000000000000000000 ) ) ;
#2397=DIRECTION ( 'NONE',  ( 0.000000000000000000, 0.000000000000000000, -1.000000000000000000 ) ) ;
#2404=VECTOR ( 'NONE', #12479, 1000.000000000000000 ) ;
#2407=EDGE_CURVE ( 'NONE', #2251, #8280, #5544, .T. ) ;
#2410=ORIENTED_EDGE ( 'NONE', *, *, #13056, .T. ) ;
#2411=EDGE_CURVE ( 'NONE', #4210, #1912, #14194, .T. ) ;
#2414=VECTOR ( 'NONE', #8003, 1000.000000000000000 ) ;
#2415=DIRECTION ( 'NONE',  ( 0.000000000000000000, 0.000000000000000000, 1.000000000000000000 ) ) ;
#2418=DIRECTION ( 'NONE',  ( 0.000000000000000000, -1.000000000000000000, 0.000000000000000000 ) ) ;
#2421=CARTESIAN_POINT ( 'NONE',  ( -52.77438362643999881, 67.53201699523744139, -147.9984795835769944 ) ) ;
#2426=ORIENTED_EDGE ( 'NONE', *, *, #5920, .T. ) ;
#2428=EDGE_CURVE ( 'NONE', #12810, #14328, #5808, .T. ) ;
#2429=ORIENTED_EDGE ( 'NONE', *, *, #13010, .T. ) ;
#2432=EDGE_CURVE ( 'NONE', #8073, #14575, #8306, .T. ) ;
#2434=ADVANCED_FACE ( 'NONE', ( #1237 ), #10625, .T. ) ;
#2438=DIRECTION ( 'NONE',  ( -1.000000000000000000, 0.000000000000000000, 0.000000000000000000 ) ) ;
#2443=DIRECTION ( 'NONE',  ( 0.000000000000000000, 0.000000000000000000, 1.000000000000000000 ) ) ;
#2450=DIRECTION ( 'NONE',  ( -1.287488025362404182E-15, -1.000000000000000000, 0.000000000000000000 ) ) ;
#2452=CYLINDRICAL_SURFACE ( 'NONE', #14580, 16.00000000000000000 ) ;
#2453=FACE_OUTER_BOUND ( 'NONE', #5115, .T. ) ;
#2455=VERTEX_POINT ( 'NONE', #493 ) ;
#2456=CYLINDRICAL_SURFACE ( 'NONE', #8274, 2.500000000000002220 ) ;
#2459=CARTESIAN_POINT ( 'NONE',  ( -84.27438362644100778, 99.17411849586700612, -182.2484795835770228 ) ) ;
#2461=ORIENTED_EDGE ( 'NONE', *, *, #6878, .T. ) ;
#2463=EDGE_LOOP ( 'NONE', ( #4360, #3971, #246, #11952 ) ) ;
#2469=DIRECTION ( 'NONE',  ( 0.000000000000000000, 0.000000000000000000, -1.000000000000000000 ) ) ;
#2474=FACE_OUTER_BOUND ( 'NONE', #10176, .T. ) ;
#2480=ORIENTED_EDGE ( 'NONE', *, *, #4140, .T. ) ;
#2481=PLANE ( 'NONE',  #13926 ) ;
#2484=DIRECTION ( 'NONE',  ( 0.000000000000000000, 0.000000000000000000, -1.000000000000000000 ) ) ;
#2485=DIRECTION ( 'NONE',  ( 1.000000000000000000, 0.000000000000000000, 0.000000000000000000 ) ) ;
#2486=EDGE_CURVE ( 'NONE', #4841, #686, #9842, .T. ) ;
#2491=DIRECTION ( 'NONE',  ( -0.000000000000000000, -0.000000000000000000, 1.000000000000000000 ) ) ;
#2493=ORIENTED_EDGE ( 'NONE', *, *, #6418, .F. ) ;
#2495=ORIENTED_EDGE ( 'NONE', *, *, #13972, .T. ) ;
#2496=VECTOR ( 'NONE', #1895, 1000.000000000000000 ) ;
#2497=ORIENTED_EDGE ( 'NONE', *, *, #4111, .T. ) ;
#2499=EDGE_CURVE ( 'NONE', #13840, #8420, #3070, .T. ) ;
#2504=LINE ( 'NONE', #12065, #4501 ) ;
#2509=EDGE_CURVE ( 'NONE', #14684, #1190, #11094, .T. ) ;
#2512=EDGE_CURVE ( 'NONE', #6403, #10071, #4109, .T. ) ;
#2513=ORIENTED_EDGE ( 'NONE', *, *, #615, .F. ) ;
#2514=DIRECTION ( 'NONE',  ( 0.000000000000000000, 0.000000000000000000, -1.000000000000000000 ) ) ;
#2516=PRODUCT_CONTEXT ( 'NONE', #4069, 'mechanical' ) ;
#2517=EDGE_LOOP ( 'NONE', ( #10301, #2950, #8307, #8615, #2732 ) ) ;
#2518=DIRECTION ( 'NONE',  ( -1.000000000000000000, 0.000000000000000000, 0.000000000000000000 ) ) ;
#2521=ORIENTED_EDGE ( 'NONE', *, *, #14653, .T. ) ;
#2522=AXIS2_PLACEMENT_3D ( 'NONE', #5733, #10674, #8044 ) ;
#2527=DIRECTION ( 'NONE',  ( -1.000000000000000000, 0.000000000000000000, 0.000000000000000000 ) ) ;
#2532=FACE_BOUND ( 'NONE', #13254, .T. ) ;
#2533=AXIS2_PLACEMENT_3D ( 'NONE', #15204, #3585, #14204 ) ;
#2534=EDGE_LOOP ( 'NONE', ( #2349, #8405, #14864, #11949 ) ) ;
#2535=CARTESIAN_POINT ( 'NONE',  ( -52.77438362644100067, 99.17411849586700612, -182.2484795835770228 ) ) ;
#2539=CYLINDRICAL_SURFACE ( 'NONE', #7797, 4.499999999999997335 ) ;
#2541=ORIENTED_EDGE ( 'NONE', *, *, #4236, .F. ) ;
#2543=ORIENTED_EDGE ( 'NONE', *, *, #6202, .T. ) ;
#2546=CARTESIAN_POINT ( 'NONE',  ( -77.52077156573416516, 59.67411849586701322, -79.59847958357700293 ) ) ;
#2547=CARTESIAN_POINT ( 'NONE',  ( -75.01311196519617397, 67.29799558322736175, -83.44847958357698303 ) ) ;
#2548=AXIS2_PLACEMENT_3D ( 'NONE', #1748, #8655, #6498 ) ;
#2551=CARTESIAN_POINT ( 'NONE',  ( -79.11147769456633227, 68.38713492810558137, -81.84847958357697451 ) ) ;
#2554=ORIENTED_EDGE ( 'NONE', *, *, #4854, .T. ) ;
#2555=CIRCLE ( 'NONE', #2804, 16.50000000000000000 ) ;
#2556=VECTOR ( 'NONE', #3416, 1000.000000000000114 ) ;
#2557=ORIENTED_EDGE ( 'NONE', *, *, #9893, .F. ) ;
#2558=EDGE_LOOP ( 'NONE', ( #11468, #1985 ) ) ;
#2559=ORIENTED_EDGE ( 'NONE', *, *, #12932, .F. ) ;
#2560=VERTEX_POINT ( 'NONE', #1851 ) ;
#2561=VECTOR ( 'NONE', #9529, 1000.000000000000114 ) ;
#2568=DIRECTION ( 'NONE',  ( 0.000000000000000000, 0.000000000000000000, -1.000000000000000000 ) ) ;
#2570=CARTESIAN_POINT ( 'NONE',  ( -69.77438362644001302, 82.17411849586700612, -79.49847958357700861 ) ) ;
#2571=DIRECTION ( 'NONE',  ( 0.000000000000000000, 0.000000000000000000, -1.000000000000000000 ) ) ;
#2573=ORIENTED_EDGE ( 'NONE', *, *, #12019, .F. ) ;
#2575=ORIENTED_EDGE ( 'NONE', *, *, #764, .F. ) ;
#2584=EDGE_CURVE ( 'NONE', #14784, #9846, #13962, .T. ) ;
#2585=DIRECTION ( 'NONE',  ( 0.000000000000000000, 0.000000000000000000, -1.000000000000000000 ) ) ;
#2586=DIRECTION ( 'NONE',  ( -1.000000000000000000, 0.000000000000000000, 0.000000000000000000 ) ) ;
#2589=CIRCLE ( 'NONE', #8536, 9.999999999999994671 ) ;
#2592=ORIENTED_EDGE ( 'NONE', *, *, #12952, .T. ) ;
#2595=ORIENTED_EDGE ( 'NONE', *, *, #4854, .F. ) ;
#2598=ORIENTED_EDGE ( 'NONE', *, *, #12571, .F. ) ;
#2599=VECTOR ( 'NONE', #7816, 1000.000000000000114 ) ;
#2601=AXIS2_PLACEMENT_3D ( 'NONE', #9462, #14201, #3582 ) ;
#2602=ADVANCED_FACE ( 'NONE', ( #605 ), #5358, .T. ) ;
#2606=DIRECTION ( 'NONE',  ( -0.000000000000000000, -0.000000000000000000, 1.000000000000000000 ) ) ;
#2611=( GEOMETRIC_REPRESENTATION_CONTEXT ( 3 ) GLOBAL_UNCERTAINTY_ASSIGNED_CONTEXT ( ( #6552 ) ) GLOBAL_UNIT_ASSIGNED_CONTEXT ( ( #10749, #10661, #9727 ) ) REPRESENTATION_CONTEXT ( 'NONE', 'WORKASPACE' ) );
#2616=VERTEX_POINT ( 'NONE', #11546 ) ;
#2619=EDGE_CURVE ( 'NONE', #10610, #4759, #12726, .T. ) ;
#2621=DIRECTION ( 'NONE',  ( 0.000000000000000000, 0.000000000000000000, 1.000000000000000000 ) ) ;
#2623=ORIENTED_EDGE ( 'NONE', *, *, #6779, .F. ) ;
#2624=VERTEX_POINT ( 'NONE', #1995 ) ;
#2626=VERTEX_POINT ( 'NONE', #3470 ) ;
#2627=EDGE_CURVE ( 'NONE', #2455, #2744, #14205, .T. ) ;
#2629=CARTESIAN_POINT ( 'NONE',  ( -82.27438362643999881, 99.17411849586700612, -86.49847958357699440 ) ) ;
#2630=VECTOR ( 'NONE', #4851, 1000.000000000000000 ) ;
#2631=CIRCLE ( 'NONE', #12783, 2.042000000000002036 ) ;
#2633=LINE ( 'NONE', #8441, #14219 ) ;
#2634=CARTESIAN_POINT ( 'NONE',  ( -85.77438362644001302, 82.17411849586700612, -117.9984795835769944 ) ) ;
#2635=DIRECTION ( 'NONE',  ( 0.000000000000000000, 0.000000000000000000, -1.000000000000000000 ) ) ;
#2636=DIRECTION ( 'NONE',  ( 1.287488025362404182E-15, 1.000000000000000000, 0.000000000000000000 ) ) ;
#2637=CARTESIAN_POINT ( 'NONE',  ( -57.02438362644099357, 99.17411849586700612, -182.2484795835770228 ) ) ;
#2638=ORIENTED_EDGE ( 'NONE', *, *, #3185, .F. ) ;
#2639=CARTESIAN_POINT ( 'NONE',  ( -52.77438362643999881, 65.17411849586700612, -145.2984795835770058 ) ) ;
#2640=VERTEX_POINT ( 'NONE', #13801 ) ;
#2641=AXIS2_PLACEMENT_3D ( 'NONE', #15205, #12893, #3428 ) ;
#2644=VECTOR ( 'NONE', #2720, 1000.000000000000000 ) ;
#2645=ORIENTED_EDGE ( 'NONE', *, *, #2783, .T. ) ;
#2648=SURFACE_STYLE_USAGE ( .BOTH. , #9689 ) ;
#2651=DIRECTION ( 'NONE',  ( -1.000000000000000000, 0.000000000000000000, 0.000000000000000000 ) ) ;
#2652=AXIS2_PLACEMENT_3D ( 'NONE', #15036, #3250, #5375 ) ;
#2655=CARTESIAN_POINT ( 'NONE',  ( -57.27438362644000591, 65.17411849586700612, -86.49847958357699440 ) ) ;
#2657=FACE_BOUND ( 'NONE', #4847, .T. ) ;
#2658=VERTEX_POINT ( 'NONE', #910 ) ;
#2660=ORIENTED_EDGE ( 'NONE', *, *, #13338, .F. ) ;
#2662=ORIENTED_EDGE ( 'NONE', *, *, #11510, .T. ) ;
#2664=CIRCLE ( 'NONE', #8847, 2.750000000000002665 ) ;
#2668=LINE ( 'NONE', #2903, #7842 ) ;
#2669=CYLINDRICAL_SURFACE ( 'NONE', #2016, 16.50000000000000000 ) ;
#2670=DIRECTION ( 'NONE',  ( 0.000000000000000000, -4.130293990420970006E-17, 1.000000000000000000 ) ) ;
#2671=CARTESIAN_POINT ( 'NONE',  ( -52.77438362644100067, 101.5320169952374414, -147.9984795835769944 ) ) ;
#2672=EDGE_CURVE ( 'NONE', #12055, #2078, #11623, .T. ) ;
#2673=AXIS2_PLACEMENT_3D ( 'NONE', #7166, #9543, #7237 ) ;
#2674=PLANE ( 'NONE',  #10421 ) ;
#2675=ORIENTED_EDGE ( 'NONE', *, *, #13598, .F. ) ;
#2677=EDGE_CURVE ( 'NONE', #4603, #3159, #6063, .T. ) ;
#2681=ORIENTED_EDGE ( 'NONE', *, *, #14758, .F. ) ;
#2685=DIRECTION ( 'NONE',  ( 0.8660254037844381525, 1.060575238724905436E-16, -0.5000000000000007772 ) ) ;
#2687=ADVANCED_FACE ( 'NONE', ( #12630 ), #3234, .T. ) ;
#2689=CARTESIAN_POINT ( 'NONE',  ( -86.77438362644100778, 99.17411849586700612, -147.9984795835769944 ) ) ;
#2691=DIRECTION ( 'NONE',  ( -0.000000000000000000, -0.000000000000000000, 1.000000000000000000 ) ) ;
#2693=EDGE_CURVE ( 'NONE', #9916, #15330, #9251, .T. ) ;
#2696=ORIENTED_EDGE ( 'NONE', *, *, #8538, .T. ) ;
#2697=ORIENTED_EDGE ( 'NONE', *, *, #1954, .F. ) ;
#2698=EDGE_LOOP ( 'NONE', ( #11113, #11513, #935, #14785, #1040 ) ) ;
#2701=ORIENTED_EDGE ( 'NONE', *, *, #13036, .F. ) ;
#2703=EDGE_CURVE ( 'NONE', #13582, #8436, #10210, .T. ) ;
#2704=DIRECTION ( 'NONE',  ( 0.000000000000000000, 0.000000000000000000, 1.000000000000000000 ) ) ;
#2707=DIRECTION ( 'NONE',  ( 0.000000000000000000, -1.000000000000000000, 0.000000000000000000 ) ) ;
#2710=EDGE_CURVE ( 'NONE', #8436, #14943, #3306, .T. ) ;
#2713=ORIENTED_EDGE ( 'NONE', *, *, #6884, .T. ) ;
#2714=DIRECTION ( 'NONE',  ( 0.000000000000000000, 0.000000000000000000, -1.000000000000000000 ) ) ;
#2715=ORIENTED_EDGE ( 'NONE', *, *, #13140, .T. ) ;
#2716=ORIENTED_EDGE ( 'NONE', *, *, #1096, .T. ) ;
#2718=ORIENTED_EDGE ( 'NONE', *, *, #13441, .F. ) ;
#2720=DIRECTION ( 'NONE',  ( -1.287488025362404182E-15, -1.000000000000000000, 0.000000000000000000 ) ) ;
#2724=CARTESIAN_POINT ( 'NONE',  ( -96.77438362643999881, 65.17411849586700612, -79.59847958357700293 ) ) ;
#2725=LINE ( 'NONE', #12046, #4560 ) ;
#2726=DIRECTION ( 'NONE',  ( 0.000000000000000000, 0.000000000000000000, -1.000000000000000000 ) ) ;
#2730=CARTESIAN_POINT ( 'NONE',  ( -82.52438362643998460, 65.17411849586700612, -182.2484795835770228 ) ) ;
#2731=EDGE_LOOP ( 'NONE', ( #8430, #13992, #7902, #2554 ) ) ;
#2732=ORIENTED_EDGE ( 'NONE', *, *, #11605, .F. ) ;
#2733=ORIENTED_EDGE ( 'NONE', *, *, #12834, .T. ) ;
#2737=DIRECTION ( 'NONE',  ( 0.000000000000000000, 0.000000000000000000, -1.000000000000000000 ) ) ;
#2738=FACE_BOUND ( 'NONE', #10888, .T. ) ;
#2741=DIRECTION ( 'NONE',  ( 1.000000000000000000, 0.000000000000000000, 0.000000000000000000 ) ) ;
#2742=ORIENTED_EDGE ( 'NONE', *, *, #9043, .F. ) ;
#2744=VERTEX_POINT ( 'NONE', #4412 ) ;
#2746=( NAMED_UNIT ( * ) PLANE_ANGLE_UNIT ( ) SI_UNIT ( $, .RADIAN. ) );
#2748=VERTEX_POINT ( 'NONE', #12704 ) ;
#2750=AXIS2_PLACEMENT_3D ( 'NONE', #13412, #3789, #4098 ) ;
#2751=CYLINDRICAL_SURFACE ( 'NONE', #3501, 2.750000000000002665 ) ;
#2754=LINE ( 'NONE', #2993, #1618 ) ;
#2755=CARTESIAN_POINT ( 'NONE',  ( -77.82438362644001018, 82.17411849586700612, -85.04847958357699156 ) ) ;
#2756=CARTESIAN_POINT ( 'NONE',  ( -48.52438362644100067, 99.17411849586700612, -149.9984795835770228 ) ) ;
#2757=AXIS2_PLACEMENT_3D ( 'NONE', #6945, #5788, #10496 ) ;
#2758=CARTESIAN_POINT ( 'NONE',  ( -52.77438362644100067, 99.17411849586700612, -147.9984795835769944 ) ) ;
#2759=DIRECTION ( 'NONE',  ( -1.000000000000000000, 0.000000000000000000, 0.000000000000000000 ) ) ;
#2761=CARTESIAN_POINT ( 'NONE',  ( -86.77438362644100778, 99.17411849586700612, -150.4984795835770228 ) ) ;
#2762=CARTESIAN_POINT ( 'NONE',  ( -91.02438362643999881, 65.17411849586700612, -149.9984795835770228 ) ) ;
#2764=VERTEX_POINT ( 'NONE', #9285 ) ;
#2766=CIRCLE ( 'NONE', #9702, 4.499999999999997335 ) ;
#2768=APPLICATION_CONTEXT ( 'automotive_design' ) ;
#2769=LINE ( 'NONE', #9975, #10766 ) ;
#2771=ORIENTED_EDGE ( 'NONE', *, *, #7665, .F. ) ;
#2774=DIRECTION ( 'NONE',  ( 1.000000000000000000, 0.000000000000000000, 0.000000000000000000 ) ) ;
#2776=VECTOR ( 'NONE', #10658, 1000.000000000000000 ) ;
#2777=CARTESIAN_POINT ( 'NONE',  ( -59.02799568714584666, 0.000000000000000000, -79.59847958357700293 ) ) ;
#2781=DIRECTION ( 'NONE',  ( 1.000000000000000000, 0.000000000000000000, 0.000000000000000000 ) ) ;
#2783=EDGE_CURVE ( 'NONE', #11570, #11860, #8363, .T. ) ;
#2784=VERTEX_POINT ( 'NONE', #11929 ) ;
#2786=ORIENTED_EDGE ( 'NONE', *, *, #10162, .T. ) ;
#2788=EDGE_LOOP ( 'NONE', ( #7966, #6101, #4257, #9700, #13915 ) ) ;
#2790=VECTOR ( 'NONE', #14472, 1000.000000000000000 ) ;
#2791=EDGE_CURVE ( 'NONE', #7742, #5220, #3703, .T. ) ;
#2795=EDGE_CURVE ( 'NONE', #13765, #13261, #12010, .T. ) ;
#2799=FACE_OUTER_BOUND ( 'NONE', #11571, .T. ) ;
#2801=CARTESIAN_POINT ( 'NONE',  ( -86.77438362644001302, 99.17411849586700612, -79.59847958357700293 ) ) ;
#2802=CARTESIAN_POINT ( 'NONE',  ( -81.27438362643999881, 82.17411849586700612, -83.44847958357698303 ) ) ;
#2804=AXIS2_PLACEMENT_3D ( 'NONE', #12999, #14081, #2277 ) ;
#2805=DIRECTION ( 'NONE',  ( -1.000000000000000000, 0.000000000000000000, 0.000000000000000000 ) ) ;
#2806=CIRCLE ( 'NONE', #8504, 2.750000000000002665 ) ;
#2807=CARTESIAN_POINT ( 'NONE',  ( -69.09337542095276774, 89.17411849586704875, -44.02377680093037071 ) ) ;
#2808=ADVANCED_FACE ( 'NONE', ( #6210 ), #1378, .T. ) ;
#2809=ORIENTED_EDGE ( 'NONE', *, *, #3062, .T. ) ;
#2810=CARTESIAN_POINT ( 'NONE',  ( -52.77438362644000591, 99.17411849586700612, -145.4984795835769660 ) ) ;
#2812=CIRCLE ( 'NONE', #8007, 2.000000000000001776 ) ;
#2813=ORIENTED_EDGE ( 'NONE', *, *, #5660, .F. ) ;
#2820=CIRCLE ( 'NONE', #11487, 2.042000000000002036 ) ;
#2822=CARTESIAN_POINT ( 'NONE',  ( -69.77438362644001302, 81.46011849586699327, -81.84847958357697451 ) ) ;
#2823=AXIS2_PLACEMENT_3D ( 'NONE', #7947, #6806, #887 ) ;
#2830=AXIS2_PLACEMENT_3D ( 'NONE', #4796, #3633, #12102 ) ;
#2834=VERTEX_POINT ( 'NONE', #14325 ) ;
#2835=AXIS2_PLACEMENT_3D ( 'NONE', #13711, #5422, #7675 ) ;
#2836=DIRECTION ( 'NONE',  ( 1.000000000000000000, 0.000000000000000000, 0.000000000000000000 ) ) ;
#2837=VECTOR ( 'NONE', #9687, 1000.000000000000000 ) ;
#2841=LINE ( 'NONE', #13905, #8539 ) ;
#2842=CARTESIAN_POINT ( 'NONE',  ( -102.2743836264399988, 104.6741184958670061, -15.85886927678779834 ) ) ;
#2845=CARTESIAN_POINT ( 'NONE',  ( -84.27438362644100778, 99.17411849586700612, -145.2984795835770058 ) ) ;
#2846=LINE ( 'NONE', #5334, #38 ) ;
#2848=EDGE_CURVE ( 'NONE', #4755, #3140, #10765, .T. ) ;
#2849=CIRCLE ( 'NONE', #861, 8.124999999999992895 ) ;
#2853=ORIENTED_EDGE ( 'NONE', *, *, #10839, .F. ) ;
#2854=AXIS2_PLACEMENT_3D ( 'NONE', #4129, #1494, #8696 ) ;
#2855=CARTESIAN_POINT ( 'NONE',  ( -73.80978675135780520, 64.78624853950366003, -81.84847958357697451 ) ) ;
#2858=VECTOR ( 'NONE', #14855, 1000.000000000000000 ) ;
#2859=DIRECTION ( 'NONE',  ( 0.000000000000000000, 0.000000000000000000, 1.000000000000000000 ) ) ;
#2864=EDGE_CURVE ( 'NONE', #8823, #7562, #2820, .T. ) ;
#2866=ORIENTED_EDGE ( 'NONE', *, *, #27, .F. ) ;
#2868=ADVANCED_FACE ( 'NONE', ( #13176 ), #2456, .T. ) ;
#2869=ORIENTED_EDGE ( 'NONE', *, *, #8012, .T. ) ;
#2871=ORIENTED_EDGE ( 'NONE', *, *, #7538, .F. ) ;
#2872=VECTOR ( 'NONE', #10035, 1000.000000000000114 ) ;
#2873=ORIENTED_EDGE ( 'NONE', *, *, #7651, .F. ) ;
#2875=AXIS2_PLACEMENT_3D ( 'NONE', #3754, #15225, #7186 ) ;
#2876=CARTESIAN_POINT ( 'NONE',  ( -59.02799568714584666, 103.6741184958669919, -152.4984795835769944 ) ) ;
#2883=CARTESIAN_POINT ( 'NONE',  ( -52.77438362644100067, 99.17411849586700612, -147.9984795835769944 ) ) ;
#2886=DIRECTION ( 'NONE',  ( 0.5000000000000003331, 0.8660254037844384856, 0.000000000000000000 ) ) ;
#2887=EDGE_CURVE ( 'NONE', #6165, #8182, #834, .T. ) ;
#2888=CARTESIAN_POINT ( 'NONE',  ( -102.2743836264399988, 99.17411849586700612, -15.85886927678779834 ) ) ;
#2889=CARTESIAN_POINT ( 'NONE',  ( -66.51083064278755330, 89.17411849586699191, -44.70344037800860804 ) ) ;
#2896=ORIENTED_EDGE ( 'NONE', *, *, #4184, .F. ) ;
#2898=DIRECTION ( 'NONE',  ( 0.000000000000000000, 1.000000000000000000, 0.000000000000000000 ) ) ;
#2899=VECTOR ( 'NONE', #13780, 1000.000000000000000 ) ;
#2903=CARTESIAN_POINT ( 'NONE',  ( -88.81638362644000040, 63.99516924618178848, -147.9984795835769944 ) ) ;
#2908=EDGE_CURVE ( 'NONE', #13232, #11184, #4074, .T. ) ;
#2911=CONICAL_SURFACE ( 'NONE', #6155, 2.500000000000002220, 1.029744258676651425 ) ;
#2914=AXIS2_PLACEMENT_3D ( 'NONE', #9835, #11006, #4962 ) ;
#2919=ORIENTED_EDGE ( 'NONE', *, *, #764, .T. ) ;
#2920=DIRECTION ( 'NONE',  ( -0.000000000000000000, 0.000000000000000000, -1.000000000000000000 ) ) ;
#2922=AXIS2_PLACEMENT_3D ( 'NONE', #2186, #15056, #10480 ) ;
#2923=DIRECTION ( 'NONE',  ( 1.000000000000000000, 0.000000000000000000, 0.000000000000000000 ) ) ;
#2924=DIRECTION ( 'NONE',  ( 0.000000000000000000, 0.000000000000000000, -1.000000000000000000 ) ) ;
#2927=DIRECTION ( 'NONE',  ( 0.000000000000000000, 0.000000000000000000, -1.000000000000000000 ) ) ;
#2932=VERTEX_POINT ( 'NONE', #5904 ) ;
#2934=LINE ( 'NONE', #8821, #7053 ) ;
#2938=CARTESIAN_POINT ( 'NONE',  ( -91.27438362643999881, 99.17411849586700612, -152.4984795835769944 ) ) ;
#2943=CARTESIAN_POINT ( 'NONE',  ( -73.80978675135780520, 64.78624853950366003, -83.44847958357698303 ) ) ;
#2944=ORIENTED_EDGE ( 'NONE', *, *, #2383, .F. ) ;
#2950=ORIENTED_EDGE ( 'NONE', *, *, #13815, .F. ) ;
#2951=VECTOR ( 'NONE', #269, 1000.000000000000000 ) ;
#2958=ADVANCED_FACE ( 'NONE', ( #52 ), #6804, .T. ) ;
#2960=DIRECTION ( 'NONE',  ( 0.8660254037844383745, -0.5000000000000003331, 0.000000000000000000 ) ) ;
#2962=DIRECTION ( 'NONE',  ( -1.000000000000000000, 0.000000000000000000, 0.000000000000000000 ) ) ;
#2963=DIRECTION ( 'NONE',  ( 0.000000000000000000, 0.000000000000000000, 1.000000000000000000 ) ) ;
#2964=CARTESIAN_POINT ( 'NONE',  ( -86.77438362644001302, 99.17411849586700612, -145.4984795835769660 ) ) ;
#2971=CARTESIAN_POINT ( 'NONE',  ( -73.64736697264537213, 89.17411849586700612, -57.99847958357699440 ) ) ;
#2976=CARTESIAN_POINT ( 'NONE',  ( -84.73238362644100619, 97.99516924618178848, -147.9984795835769944 ) ) ;
#2977=DIRECTION ( 'NONE',  ( 0.000000000000000000, 1.000000000000000000, 0.000000000000000000 ) ) ;
#2979=CARTESIAN_POINT ( 'NONE',  ( -35.27438362644000591, 111.1741184958670061, -67.49847958357700861 ) ) ;
#2980=CARTESIAN_POINT ( 'NONE',  ( -70.11249870063934964, 75.17411849586699191, -43.99847958365485567 ) ) ;
#2984=ADVANCED_FACE ( 'NONE', ( #218 ), #5125, .F. ) ;
#2986=EDGE_LOOP ( 'NONE', ( #9007, #1571, #801, #730 ) ) ;
#2989=EDGE_CURVE ( 'NONE', #1813, #12412, #1469, .T. ) ;
#2992=EDGE_CURVE ( 'NONE', #6604, #469, #8522, .T. ) ;
#2993=CARTESIAN_POINT ( 'NONE',  ( -53.70938362644000819, 81.46011849586699327, -83.44847958357698303 ) ) ;
#2994=EDGE_CURVE ( 'NONE', #4969, #1406, #2633, .T. ) ;
#2995=CARTESIAN_POINT ( 'NONE',  ( -69.77438362644001302, 79.67411849586700612, -43.99847958357699440 ) ) ;
#2997=DIRECTION ( 'NONE',  ( -1.000000000000000000, 0.000000000000000000, 0.000000000000000000 ) ) ;
#2999=CARTESIAN_POINT ( 'NONE',  ( -66.62325245518700001, 97.86074886511960358, -93.49847958357699440 ) ) ;
#3000=FACE_OUTER_BOUND ( 'NONE', #7098, .T. ) ;
#3001=EDGE_CURVE ( 'NONE', #558, #13582, #7551, .T. ) ;
#3004=ORIENTED_EDGE ( 'NONE', *, *, #12279, .F. ) ;
#3005=AXIS2_PLACEMENT_3D ( 'NONE', #10201, #15010, #13715 ) ;
#3009=EDGE_CURVE ( 'NONE', #2748, #486, #13348, .T. ) ;
#3010=CARTESIAN_POINT ( 'NONE',  ( -69.77438362644001302, 110.1741184958670061, -152.4984795835769944 ) ) ;
#3011=AXIS2_PLACEMENT_3D ( 'NONE', #14683, #4070, #13231 ) ;
#3012=CIRCLE ( 'NONE', #12430, 2.000000000000001776 ) ;
#3013=FACE_OUTER_BOUND ( 'NONE', #176, .T. ) ;
#3018=EDGE_LOOP ( 'NONE', ( #5761, #12487, #9475, #757 ) ) ;
#3020=ORIENTED_EDGE ( 'NONE', *, *, #11996, .F. ) ;
#3030=CARTESIAN_POINT ( 'NONE',  ( -72.92551479769302603, 94.57411849586699759, -93.49847958357699440 ) ) ;
#3031=VECTOR ( 'NONE', #7789, 1000.000000000000000 ) ;
#3034=DIRECTION ( 'NONE',  ( 0.8660254037844383745, -0.5000000000000003331, 0.000000000000000000 ) ) ;
#3038=DIRECTION ( 'NONE',  ( 0.000000000000000000, 0.000000000000000000, -1.000000000000000000 ) ) ;
#3040=ORIENTED_EDGE ( 'NONE', *, *, #6334, .T. ) ;
#3043=ADVANCED_FACE ( 'NONE', ( #6068 ), #10928, .F. ) ;
#3044=VECTOR ( 'NONE', #14550, 1000.000000000000114 ) ;
#3049=AXIS2_PLACEMENT_3D ( 'NONE', #15035, #10616, #4424 ) ;
#3050=DIRECTION ( 'NONE',  ( 0.000000000000000000, 0.000000000000000000, -1.000000000000000000 ) ) ;
#3051=DIRECTION ( 'NONE',  ( 0.000000000000000000, 0.000000000000000000, -1.000000000000000000 ) ) ;
#3053=CIRCLE ( 'NONE', #9231, 4.499999999999997335 ) ;
#3057=ADVANCED_FACE ( 'NONE', ( #3949 ), #8673, .F. ) ;
#3058=ORIENTED_EDGE ( 'NONE', *, *, #9595, .F. ) ;
#3060=VECTOR ( 'NONE', #6262, 1000.000000000000114 ) ;
#3061=ORIENTED_EDGE ( 'NONE', *, *, #224, .T. ) ;
#3062=EDGE_CURVE ( 'NONE', #3615, #7225, #13415, .T. ) ;
#3063=AXIS2_PLACEMENT_3D ( 'NONE', #14966, #9082, #13824 ) ;
#3068=DIRECTION ( 'NONE',  ( 0.000000000000000000, 1.000000000000000000, 0.000000000000000000 ) ) ;
#3070=CIRCLE ( 'NONE', #15190, 2.042000000000002036 ) ;
#3071=DIRECTION ( 'NONE',  ( -1.287488025362404182E-15, -1.000000000000000000, 0.000000000000000000 ) ) ;
#3072=CARTESIAN_POINT ( 'NONE',  ( -52.77438362643999881, 65.17411849586700612, -145.2984795835770058 ) ) ;
#3073=CARTESIAN_POINT ( 'NONE',  ( -78.12438362644000733, 82.17411849586700612, -80.14847958357698587 ) ) ;
#3074=PLANE ( 'NONE',  #3638 ) ;
#3075=ADVANCED_FACE ( 'NONE', ( #459 ), #6152, .F. ) ;
#3076=CARTESIAN_POINT ( 'NONE',  ( -69.77438362644001302, 82.17411849586700612, -81.84847958357698872 ) ) ;
#3078=ORIENTED_EDGE ( 'NONE', *, *, #4326, .T. ) ;
#3080=CARTESIAN_POINT ( 'NONE',  ( -52.77438362644100067, 99.17411849586700612, -145.2984795835770058 ) ) ;
#3084=VECTOR ( 'NONE', #14729, 1000.000000000000000 ) ;
#3085=EDGE_CURVE ( 'NONE', #1067, #11758, #2336, .T. ) ;
#3086=DIRECTION ( 'NONE',  ( 0.000000000000000000, 0.000000000000000000, 1.000000000000000000 ) ) ;
#3091=EDGE_CURVE ( 'NONE', #6403, #7923, #9012, .T. ) ;
#3092=CARTESIAN_POINT ( 'NONE',  ( -52.77438362644000591, 99.17411849586700612, -86.49847958357699440 ) ) ;
#3095=VERTEX_POINT ( 'NONE', #9123 ) ;
#3098=EDGE_CURVE ( 'NONE', #5984, #9369, #6594, .T. ) ;
#3101=VERTEX_POINT ( 'NONE', #10203 ) ;
#3103=STYLED_ITEM ( 'NONE', ( #3532 ), #357 ) ;
#3107=AXIS2_PLACEMENT_3D ( 'NONE', #13596, #2726, #3897 ) ;
#3109=LINE ( 'NONE', #546, #7766 ) ;
#3110=CARTESIAN_POINT ( 'NONE',  ( -86.77438362644001302, 59.67411849586700612, -15.85886927678779834 ) ) ;
#3113=FACE_OUTER_BOUND ( 'NONE', #15171, .T. ) ;
#3114=CARTESIAN_POINT ( 'NONE',  ( -101.2743836264399988, 57.67411849586699901, -79.49847958357700861 ) ) ;
#3115=CARTESIAN_POINT ( 'NONE',  ( -91.02438362644100778, 99.17411849586700612, -145.4984795835769660 ) ) ;
#3117=CARTESIAN_POINT ( 'NONE',  ( -62.02799568714584666, 164.3482369917340122, -152.4984795835769944 ) ) ;
#3119=AXIS2_PLACEMENT_3D ( 'NONE', #11137, #6576, #11291 ) ;
#3120=ORIENTED_EDGE ( 'NONE', *, *, #12195, .T. ) ;
#3121=ORIENTED_EDGE ( 'NONE', *, *, #12172, .T. ) ;
#3128=CARTESIAN_POINT ( 'NONE',  ( -50.27438362644100067, 59.67411849586700612, -79.59847958357700293 ) ) ;
#3129=AXIS2_PLACEMENT_3D ( 'NONE', #4519, #2109, #10246 ) ;
#3130=PLANE ( 'NONE',  #9851 ) ;
#3133=LINE ( 'NONE', #4683, #9272 ) ;
#3135=ORIENTED_EDGE ( 'NONE', *, *, #7997, .F. ) ;
#3136=PLANE ( 'NONE',  #14285 ) ;
#3139=AXIS2_PLACEMENT_3D ( 'NONE', #8657, #7438, #14552 ) ;
#3140=VERTEX_POINT ( 'NONE', #677 ) ;
#3141=AXIS2_PLACEMENT_3D ( 'NONE', #5752, #10454, #10618 ) ;
#3143=ORIENTED_EDGE ( 'NONE', *, *, #1189, .F. ) ;
#3147=DIRECTION ( 'NONE',  ( 0.000000000000000000, 0.000000000000000000, -1.000000000000000000 ) ) ;
#3148=CARTESIAN_POINT ( 'NONE',  ( -50.73238362644099197, 97.99516924618178848, -147.9984795835769944 ) ) ;
#3149=CIRCLE ( 'NONE', #5131, 8.000000000000007105 ) ;
#3150=ADVANCED_FACE ( 'NONE', ( #1766 ), #12330, .F. ) ;
#3151=VECTOR ( 'NONE', #14959, 1000.000000000000000 ) ;
#3152=DIRECTION ( 'NONE',  ( 0.000000000000000000, 0.000000000000000000, -1.000000000000000000 ) ) ;
#3154=CARTESIAN_POINT ( 'NONE',  ( -71.73429801879703405, 98.05590563058170517, -94.29040204287990434 ) ) ;
#3157=EDGE_LOOP ( 'NONE', ( #14083, #3657 ) ) ;
#3159=VERTEX_POINT ( 'NONE', #12404 ) ;
#3160=CIRCLE ( 'NONE', #13804, 4.250000000000003553 ) ;
#3161=ADVANCED_FACE ( 'NONE', ( #12559 ), #8903, .F. ) ;
#3163=CARTESIAN_POINT ( 'NONE',  ( -57.27438362644000591, 65.17411849586700612, -86.49847958357699440 ) ) ;
#3165=CYLINDRICAL_SURFACE ( 'NONE', #5325, 17.85000000000000497 ) ;
#3166=AXIS2_PLACEMENT_3D ( 'NONE', #4916, #3502, #4981 ) ;
#3167=EDGE_LOOP ( 'NONE', ( #9997, #3866, #4139, #11739 ) ) ;
#3169=ORIENTED_EDGE ( 'NONE', *, *, #6418, .T. ) ;
#3171=ORIENTED_EDGE ( 'NONE', *, *, #7647, .T. ) ;
#3173=ORIENTED_EDGE ( 'NONE', *, *, #7761, .F. ) ;
#3176=VERTEX_POINT ( 'NONE', #11308 ) ;
#3179=ADVANCED_FACE ( 'NONE', ( #9051 ), #12993, .F. ) ;
#3180=CIRCLE ( 'NONE', #1197, 2.000000000000001776 ) ;
#3181=DIRECTION ( 'NONE',  ( 0.000000000000000000, 0.000000000000000000, -1.000000000000000000 ) ) ;
#3184=DIRECTION ( 'NONE',  ( 0.000000000000000000, 0.000000000000000000, -1.000000000000000000 ) ) ;
#3185=EDGE_CURVE ( 'NONE', #8073, #4888, #4404, .T. ) ;
#3186=EDGE_CURVE ( 'NONE', #8760, #5254, #14713, .T. ) ;
#3187=DIRECTION ( 'NONE',  ( -1.000000000000000000, 0.000000000000000000, 0.000000000000000000 ) ) ;
#3188=DIRECTION ( 'NONE',  ( 1.000000000000000000, 1.541976423090494894E-16, 0.000000000000000000 ) ) ;
#3193=ORIENTED_EDGE ( 'NONE', *, *, #11871, .T. ) ;
#3194=AXIS2_PLACEMENT_3D ( 'NONE', #9053, #13794, #1989 ) ;
#3196=ORIENTED_EDGE ( 'NONE', *, *, #10348, .F. ) ;
#3201=DIRECTION ( 'NONE',  ( 1.000000000000000000, 0.000000000000000000, 0.000000000000000000 ) ) ;
#3202=CARTESIAN_POINT ( 'NONE',  ( -86.77438362644001302, 65.17411849586700612, -86.49847958357699440 ) ) ;
#3203=CARTESIAN_POINT ( 'NONE',  ( -86.77438362643999881, 65.17411849586700612, -145.4984795835769944 ) ) ;
#3204=DIRECTION ( 'NONE',  ( 0.000000000000000000, 0.000000000000000000, -1.000000000000000000 ) ) ;
#3205=CARTESIAN_POINT ( 'NONE',  ( -102.2743836264399988, 65.17411849586700612, -15.85886927678779834 ) ) ;
#3209=ORIENTED_EDGE ( 'NONE', *, *, #14709, .T. ) ;
#3210=DIRECTION ( 'NONE',  ( 1.000000000000000000, 0.000000000000000000, 0.000000000000000000 ) ) ;
#3212=EDGE_LOOP ( 'NONE', ( #10829, #3241 ) ) ;
#3215=DIRECTION ( 'NONE',  ( 0.000000000000000000, -1.000000000000000000, 0.000000000000000000 ) ) ;
#3218=CARTESIAN_POINT ( 'NONE',  ( -71.99490031521868616, 98.02122612623958275, -94.16161080865532540 ) ) ;
#3224=ORIENTED_EDGE ( 'NONE', *, *, #13873, .T. ) ;
#3232=CARTESIAN_POINT ( 'NONE',  ( -102.2743836264264132, 104.6741184958692088, -79.59847958357700293 ) ) ;
#3233=ORIENTED_EDGE ( 'NONE', *, *, #13222, .T. ) ;
#3234=CYLINDRICAL_SURFACE ( 'NONE', #10744, 2.500000000000002220 ) ;
#3237=VERTEX_POINT ( 'NONE', #9423 ) ;
#3241=ORIENTED_EDGE ( 'NONE', *, *, #8769, .T. ) ;
#3250=DIRECTION ( 'NONE',  ( 0.000000000000000000, 0.000000000000000000, -1.000000000000000000 ) ) ;
#3251=LINE ( 'NONE', #12880, #1689 ) ;
#3255=ORIENTED_EDGE ( 'NONE', *, *, #1865, .F. ) ;
#3256=FACE_OUTER_BOUND ( 'NONE', #11408, .T. ) ;
#3258=AXIS2_PLACEMENT_3D ( 'NONE', #2196, #9100, #10257 ) ;
#3260=ORIENTED_EDGE ( 'NONE', *, *, #13886, .T. ) ;
#3264=DIRECTION ( 'NONE',  ( 0.7071067811865474617, 0.000000000000000000, 0.7071067811865474617 ) ) ;
#3267=CIRCLE ( 'NONE', #548, 2.042000000000002036 ) ;
#3268=DIRECTION ( 'NONE',  ( 0.000000000000000000, 0.000000000000000000, 1.000000000000000000 ) ) ;
#3269=CARTESIAN_POINT ( 'NONE',  ( -50.02438362644000591, 99.17411849586700612, -145.4984795835769944 ) ) ;
#3271=CYLINDRICAL_SURFACE ( 'NONE', #10302, 2.750000000000002665 ) ;
#3272=VECTOR ( 'NONE', #11574, 1000.000000000000000 ) ;
#3273=EDGE_CURVE ( 'NONE', #6326, #957, #11846, .T. ) ;
#3275=CARTESIAN_POINT ( 'NONE',  ( -69.77438362644002723, 75.17411849587348627, -43.99847958364158984 ) ) ;
#3276=DIRECTION ( 'NONE',  ( -1.287488025362404182E-15, -1.000000000000000000, 0.000000000000000000 ) ) ;
#3277=CONICAL_SURFACE ( 'NONE', #14421, 3.750000000000003553, 0.7853981633974476129 ) ;
#3278=ORIENTED_EDGE ( 'NONE', *, *, #14074, .F. ) ;
#3280=EDGE_CURVE ( 'NONE', #12826, #12970, #2324, .T. ) ;
#3281=VERTEX_POINT ( 'NONE', #8126 ) ;
#3282=VECTOR ( 'NONE', #4331, 1000.000000000000000 ) ;
#3284=DIRECTION ( 'NONE',  ( 0.000000000000000000, -0.000000000000000000, 1.000000000000000000 ) ) ;
#3287=ORIENTED_EDGE ( 'NONE', *, *, #10080, .T. ) ;
#3288=AXIS2_PLACEMENT_3D ( 'NONE', #9143, #8061, #10308 ) ;
#3291=CARTESIAN_POINT ( 'NONE',  ( -82.27438362643999881, 65.17411849586700612, -145.4984795835769660 ) ) ;
#3297=AXIS2_PLACEMENT_3D ( 'NONE', #1087, #14047, #12887 ) ;
#3298=DIRECTION ( 'NONE',  ( -1.000000000000000000, 0.000000000000000000, 0.000000000000000000 ) ) ;
#3300=CIRCLE ( 'NONE', #11738, 4.250000000000003553 ) ;
#3305=CARTESIAN_POINT ( 'NONE',  ( -66.62325245518700001, 94.57411849586699759, -93.49847958357699440 ) ) ;
#3306=CIRCLE ( 'NONE', #4805, 16.00000000000000000 ) ;
#3307=DIRECTION ( 'NONE',  ( 0.000000000000000000, 0.000000000000000000, -1.000000000000000000 ) ) ;
#3308=PLANE ( 'NONE',  #5327 ) ;
#3311=DIRECTION ( 'NONE',  ( 0.000000000000000000, -0.000000000000000000, 1.000000000000000000 ) ) ;
#3312=EDGE_CURVE ( 'NONE', #3902, #3610, #6819, .T. ) ;
#3314=ORIENTED_EDGE ( 'NONE', *, *, #3098, .T. ) ;
#3321=ORIENTED_EDGE ( 'NONE', *, *, #12384, .T. ) ;
#3323=EDGE_LOOP ( 'NONE', ( #14803, #9020, #9557, #8069 ) ) ;
#3326=DIRECTION ( 'NONE',  ( 0.000000000000000000, 1.000000000000000000, 0.000000000000000000 ) ) ;
#3328=CIRCLE ( 'NONE', #8294, 2.700000000000001066 ) ;
#3330=ADVANCED_FACE ( 'NONE', ( #10670 ), #3308, .T. ) ;
#3336=CARTESIAN_POINT ( 'NONE',  ( -69.77438362644001302, 82.17411849586700612, -80.44847958357698303 ) ) ;
#3337=EDGE_LOOP ( 'NONE', ( #300, #6266, #10072, #13106, #9826 ) ) ;
#3338=FACE_BOUND ( 'NONE', #7783, .T. ) ;
#3339=EDGE_LOOP ( 'NONE', ( #990, #2733, #3004, #13618 ) ) ;
#3342=CIRCLE ( 'NONE', #7605, 4.250000000000003553 ) ;
#3343=CARTESIAN_POINT ( 'NONE',  ( -86.77438362644100778, 99.17411849586700612, -147.9984795835769944 ) ) ;
#3344=CIRCLE ( 'NONE', #12028, 2.500000000000002220 ) ;
#3348=DIRECTION ( 'NONE',  ( -0.3469356515732558988, -0.9378889346118975956, 0.000000000000000000 ) ) ;
#3349=EDGE_CURVE ( 'NONE', #4841, #9681, #44, .T. ) ;
#3351=LINE ( 'NONE', #945, #10594 ) ;
#3352=VECTOR ( 'NONE', #15153, 1000.000000000000000 ) ;
#3356=DIRECTION ( 'NONE',  ( 0.000000000000000000, -1.000000000000000000, 0.000000000000000000 ) ) ;
#3359=DIRECTION ( 'NONE',  ( 1.000000000000000000, 0.000000000000000000, 0.000000000000000000 ) ) ;
#3362=CARTESIAN_POINT ( 'NONE',  ( -86.77438362643999881, 62.81621999649657084, -147.9984795835769944 ) ) ;
#3363=VERTEX_POINT ( 'NONE', #5662 ) ;
#3364=ADVANCED_FACE ( 'NONE', ( #2149 ), #2348, .T. ) ;
#3370=AXIS2_PLACEMENT_3D ( 'NONE', #10192, #6660, #11446 ) ;
#3372=EDGE_CURVE ( 'NONE', #9550, #10808, #12933, .T. ) ;
#3376=CYLINDRICAL_SURFACE ( 'NONE', #10164, 4.250000000000003553 ) ;
#3380=FACE_OUTER_BOUND ( 'NONE', #4823, .T. ) ;
#3382=AXIS2_PLACEMENT_3D ( 'NONE', #6463, #10879, #9773 ) ;
#3383=ORIENTED_EDGE ( 'NONE', *, *, #12083, .F. ) ;
#3389=TOROIDAL_SURFACE ( 'NONE', #14045, 2.700000000000000178, 0.2000000000000000111 ) ;
#3390=DIRECTION ( 'NONE',  ( 0.000000000000000000, 0.000000000000000000, 1.000000000000000000 ) ) ;
#3392=CARTESIAN_POINT ( 'NONE',  ( -89.47438362644099641, 99.17411849586700612, -145.4984795835769944 ) ) ;
#3393=CARTESIAN_POINT ( 'NONE',  ( -86.77438362644001302, 82.17411849586700612, -3.496191900462991775 ) ) ;
#3394=ORIENTED_EDGE ( 'NONE', *, *, #2029, .F. ) ;
#3395=CARTESIAN_POINT ( 'NONE',  ( -69.77438362644001302, 82.17411849586700612, -117.9984795835769944 ) ) ;
#3398=CIRCLE ( 'NONE', #10837, 1.000000000000000888 ) ;
#3403=ORIENTED_EDGE ( 'NONE', *, *, #10051, .T. ) ;
#3405=CARTESIAN_POINT ( 'NONE',  ( -86.77438362644001302, 65.17411849586700612, -86.49847958357699440 ) ) ;
#3406=DIRECTION ( 'NONE',  ( 0.000000000000000000, 0.000000000000000000, -1.000000000000000000 ) ) ;
#3407=CARTESIAN_POINT ( 'NONE',  ( -89.47438362644099641, 99.17411849586700612, -145.2984795835770058 ) ) ;
#3408=CARTESIAN_POINT ( 'NONE',  ( -42.77438362644000591, 104.6741184958670061, -79.59847958357700293 ) ) ;
#3411=PLANE ( 'NONE',  #116 ) ;
#3412=FACE_OUTER_BOUND ( 'NONE', #14216, .T. ) ;
#3415=EDGE_LOOP ( 'NONE', ( #299, #92, #8912 ) ) ;
#3416=DIRECTION ( 'NONE',  ( 0.8660254037844383745, -0.5000000000000003331, 0.000000000000000000 ) ) ;
#3418=( BOUNDED_CURVE ( )  B_SPLINE_CURVE ( 3, ( #2971, #8631, #7410, #1727 ),
 .UNSPECIFIED., .F., .F. ) 
 B_SPLINE_CURVE_WITH_KNOTS ( ( 4, 4 ),
 ( 5.777824796895650650, 6.283185307179590673 ),
 .UNSPECIFIED. ) 
 CURVE ( )  GEOMETRIC_REPRESENTATION_ITEM ( )  RATIONAL_B_SPLINE_CURVE ( ( 1.000000000000000000, 0.9788305577012550440, 0.9788305577012550440, 1.000000000000000000 ) ) 
 REPRESENTATION_ITEM ( '' )  );
#3420=ORIENTED_EDGE ( 'NONE', *, *, #9575, .T. ) ;
#3421=EDGE_CURVE ( 'NONE', #12869, #9247, #13168, .T. ) ;
#3422=AXIS2_PLACEMENT_3D ( 'NONE', #530, #7681, #13350 ) ;
#3423=CARTESIAN_POINT ( 'NONE',  ( 0.000000000000000000, 0.000000000000000000, 0.000000000000000000 ) ) ;
#3428=DIRECTION ( 'NONE',  ( 1.000000000000000000, 0.000000000000000000, 0.000000000000000000 ) ) ;
#3429=FACE_OUTER_BOUND ( 'NONE', #6924, .T. ) ;
#3430=CARTESIAN_POINT ( 'NONE',  ( -70.11249870063895173, 89.17411849586699191, -43.99847958365485567 ) ) ;
#3431=DIRECTION ( 'NONE',  ( -0.000000000000000000, -0.000000000000000000, 1.000000000000000000 ) ) ;
#3432=DIRECTION ( 'NONE',  ( 0.000000000000000000, 0.000000000000000000, 1.000000000000000000 ) ) ;
#3433=VECTOR ( 'NONE', #9504, 1000.000000000000000 ) ;
#3436=ORIENTED_EDGE ( 'NONE', *, *, #14642, .T. ) ;
#3443=EDGE_LOOP ( 'NONE', ( #6400, #8612, #14866 ) ) ;
#3445=AXIS2_PLACEMENT_3D ( 'NONE', #13700, #12684, #3071 ) ;
#3449=FACE_OUTER_BOUND ( 'NONE', #15256, .T. ) ;
#3452=CARTESIAN_POINT ( 'NONE',  ( -90.85838362644000199, 65.17411849586700612, -147.9984795835769944 ) ) ;
#3455=CYLINDRICAL_SURFACE ( 'NONE', #15233, 10.49999999999999467 ) ;
#3457=ORIENTED_EDGE ( 'NONE', *, *, #6136, .F. ) ;
#3458=EDGE_CURVE ( 'NONE', #15330, #13910, #6129, .T. ) ;
#3461=LINE ( 'NONE', #8191, #8943 ) ;
#3463=DIRECTION ( 'NONE',  ( 0.000000000000000000, 0.000000000000000000, 1.000000000000000000 ) ) ;
#3464=ADVANCED_FACE ( 'NONE', ( #3626, #3857 ), #1603, .T. ) ;
#3469=EDGE_LOOP ( 'NONE', ( #10073, #12787, #12414, #152 ) ) ;
#3470=CARTESIAN_POINT ( 'NONE',  ( -53.79538362644100147, 97.40569462133919387, -147.9984795835769944 ) ) ;
#3471=ADVANCED_FACE ( 'NONE', ( #8503 ), #1448, .F. ) ;
#3472=ORIENTED_EDGE ( 'NONE', *, *, #3091, .T. ) ;
#3473=VERTEX_POINT ( 'NONE', #1520 ) ;
#3476=ORIENTED_EDGE ( 'NONE', *, *, #8867, .T. ) ;
#3477=ORIENTED_EDGE ( 'NONE', *, *, #3185, .T. ) ;
#3479=CARTESIAN_POINT ( 'NONE',  ( -69.77438362644001302, 82.17411849586700612, -80.14847958357698587 ) ) ;
#3481=CARTESIAN_POINT ( 'NONE',  ( -50.73238362644099197, 100.3530677455522238, -147.9984795835769944 ) ) ;
#3483=DIRECTION ( 'NONE',  ( 1.000000000000000000, 0.000000000000000000, 0.000000000000000000 ) ) ;
#3484=CARTESIAN_POINT ( 'NONE',  ( -86.77438362643999881, 65.17411849586700612, -145.4984795835769944 ) ) ;
#3486=DIRECTION ( 'NONE',  ( 0.000000000000000000, 0.000000000000000000, -1.000000000000000000 ) ) ;
#3488=DIRECTION ( 'NONE',  ( 0.000000000000000000, 0.000000000000000000, -1.000000000000000000 ) ) ;
#3490=CARTESIAN_POINT ( 'NONE',  ( -53.77438362644000591, 82.17411849586700612, -183.7533135795160320 ) ) ;
#3491=VERTEX_POINT ( 'NONE', #2756 ) ;
#3493=ORIENTED_EDGE ( 'NONE', *, *, #10855, .F. ) ;
#3494=ORIENTED_EDGE ( 'NONE', *, *, #13886, .F. ) ;
#3495=AXIS2_PLACEMENT_3D ( 'NONE', #5580, #4783, #1050 ) ;
#3496=DIRECTION ( 'NONE',  ( 0.000000000000000000, 0.000000000000000000, 1.000000000000000000 ) ) ;
#3501=AXIS2_PLACEMENT_3D ( 'NONE', #10113, #8956, #7506 ) ;
#3502=DIRECTION ( 'NONE',  ( 1.000000000000000000, -1.287488025362404182E-15, 0.000000000000000000 ) ) ;
#3506=VECTOR ( 'NONE', #6254, 1000.000000000000000 ) ;
#3508=DIRECTION ( 'NONE',  ( 0.000000000000000000, 0.000000000000000000, 1.000000000000000000 ) ) ;
#3510=EDGE_CURVE ( 'NONE', #632, #7802, #9768, .T. ) ;
#3512=ORIENTED_EDGE ( 'NONE', *, *, #4710, .F. ) ;
#3516=VERTEX_POINT ( 'NONE', #10759 ) ;
#3519=DIRECTION ( 'NONE',  ( 0.000000000000000000, 0.000000000000000000, 1.000000000000000000 ) ) ;
#3521=FACE_OUTER_BOUND ( 'NONE', #13096, .T. ) ;
#3524=DIRECTION ( 'NONE',  ( 0.000000000000000000, 0.000000000000000000, -1.000000000000000000 ) ) ;
#3528=CARTESIAN_POINT ( 'NONE',  ( -62.02799568714584666, 103.6741184958669919, -79.59847958357700293 ) ) ;
#3532=PRESENTATION_STYLE_ASSIGNMENT (( #9647 ) ) ;
#3537=AXIS2_PLACEMENT_3D ( 'NONE', #14957, #10145, #4350 ) ;
#3538=EDGE_CURVE ( 'NONE', #1459, #3615, #6086, .T. ) ;
#3540=AXIS2_PLACEMENT_3D ( 'NONE', #1402, #3574, #295 ) ;
#3543=DIRECTION ( 'NONE',  ( 0.000000000000000000, -1.000000000000000000, 0.000000000000000000 ) ) ;
#3546=TOROIDAL_SURFACE ( 'NONE', #12986, 11.50000000000000000, 1.000000000000000000 ) ;
#3547=ORIENTED_EDGE ( 'NONE', *, *, #11519, .T. ) ;
#3555=ORIENTED_EDGE ( 'NONE', *, *, #9402, .F. ) ;
#3559=CIRCLE ( 'NONE', #7285, 5.499999999999998224 ) ;
#3560=PLANE ( 'NONE',  #5640 ) ;
#3561=DIRECTION ( 'NONE',  ( -1.000000000000000000, 0.000000000000000000, 0.000000000000000000 ) ) ;
#3564=CARTESIAN_POINT ( 'NONE',  ( -69.77438362644001302, 82.17411849586700612, -44.99847958359070788 ) ) ;
#3565=DIRECTION ( 'NONE',  ( 1.000000000000000000, 0.000000000000000000, 0.000000000000000000 ) ) ;
#3566=CARTESIAN_POINT ( 'NONE',  ( -38.27438362644000591, 114.1741184958670061, -79.49847958357700861 ) ) ;
#3573=VERTEX_POINT ( 'NONE', #7935 ) ;
#3574=DIRECTION ( 'NONE',  ( 0.000000000000000000, 0.000000000000000000, 1.000000000000000000 ) ) ;
#3575=ORIENTED_EDGE ( 'NONE', *, *, #8103, .F. ) ;
#3576=ORIENTED_EDGE ( 'NONE', *, *, #1865, .T. ) ;
#3577=VERTEX_POINT ( 'NONE', #11355 ) ;
#3579=VECTOR ( 'NONE', #759, 1000.000000000000000 ) ;
#3582=DIRECTION ( 'NONE',  ( 0.000000000000000000, 0.000000000000000000, 1.000000000000000000 ) ) ;
#3583=B_SPLINE_CURVE_WITH_KNOTS ( 'NONE', 3,
 ( #13446, #2889, #7636, #12356, #10886, #2807, #4920, #1496 ),
 .UNSPECIFIED., .F., .F.,
 ( 4, 2, 2, 4 ),
 ( 0.04105254269951062740, 0.04300721795512758849, 0.04398455558293606904, 0.04496189321074454959 ),
 .UNSPECIFIED. ) ;
#3585=DIRECTION ( 'NONE',  ( 1.000000000000000000, 0.000000000000000000, 0.000000000000000000 ) ) ;
#3589=DIRECTION ( 'NONE',  ( 0.8660254037844383745, -0.5000000000000003331, 0.000000000000000000 ) ) ;
#3590=DIRECTION ( 'NONE',  ( 0.000000000000000000, 0.000000000000000000, -1.000000000000000000 ) ) ;
#3592=ORIENTED_EDGE ( 'NONE', *, *, #1668, .T. ) ;
#3594=AXIS2_PLACEMENT_3D ( 'NONE', #3080, #8740, #4174 ) ;
#3596=EDGE_LOOP ( 'NONE', ( #6060, #11134 ) ) ;
#3597=VERTEX_POINT ( 'NONE', #7588 ) ;
#3598=AXIS2_PLACEMENT_3D ( 'NONE', #5688, #9078, #7915 ) ;
#3601=ORIENTED_EDGE ( 'NONE', *, *, #1535, .T. ) ;
#3609=CYLINDRICAL_SURFACE ( 'NONE', #9682, 2.000000000000001776 ) ;
#3610=VERTEX_POINT ( 'NONE', #6862 ) ;
#3611=CARTESIAN_POINT ( 'NONE',  ( -84.73238362643999722, 66.35306774555222376, -147.9984795835769944 ) ) ;
#3615=VERTEX_POINT ( 'NONE', #790 ) ;
#3616=CIRCLE ( 'NONE', #653, 4.499999999999997335 ) ;
#3619=VERTEX_POINT ( 'NONE', #14979 ) ;
#3620=AXIS2_PLACEMENT_3D ( 'NONE', #1055, #9359, #8278 ) ;
#3621=ADVANCED_FACE ( 'NONE', ( #9095 ), #947, .T. ) ;
#3623=EDGE_CURVE ( 'NONE', #13986, #8154, #2037, .T. ) ;
#3624=LINE ( 'NONE', #267, #7083 ) ;
#3625=CARTESIAN_POINT ( 'NONE',  ( -84.02438362643999881, 99.17411849586700612, -86.49847958357699440 ) ) ;
#3626=FACE_BOUND ( 'NONE', #11532, .T. ) ;
#3627=AXIS2_PLACEMENT_3D ( 'NONE', #3203, #6641, #6559 ) ;
#3628=DIRECTION ( 'NONE',  ( 0.8660254037844383745, -0.5000000000000003331, 0.000000000000000000 ) ) ;
#3629=CARTESIAN_POINT ( 'NONE',  ( -84.73238362644100619, 100.3530677455522238, -150.4984795835770228 ) ) ;
#3633=DIRECTION ( 'NONE',  ( 0.000000000000000000, 0.000000000000000000, 1.000000000000000000 ) ) ;
#3635=FACE_OUTER_BOUND ( 'NONE', #7157, .T. ) ;
#3637=ORIENTED_EDGE ( 'NONE', *, *, #2031, .T. ) ;
#3638=AXIS2_PLACEMENT_3D ( 'NONE', #13564, #6500, #7812 ) ;
#3641=EDGE_LOOP ( 'NONE', ( #11917, #6041, #5187, #570, #2592, #2713 ) ) ;
#3643=DIRECTION ( 'NONE',  ( 2.065146995210485003E-17, 4.251773225433349175E-17, 1.000000000000000000 ) ) ;
#3644=CARTESIAN_POINT ( 'NONE',  ( -69.77438362644001302, 82.17411849586700612, -79.49847958357700861 ) ) ;
#3650=LINE ( 'NONE', #11566, #2063 ) ;
#3653=EDGE_CURVE ( 'NONE', #840, #10550, #2841, .T. ) ;
#3657=ORIENTED_EDGE ( 'NONE', *, *, #12344, .T. ) ;
#3658=EDGE_CURVE ( 'NONE', #11018, #5594, #8088, .T. ) ;
#3661=AXIS2_PLACEMENT_3D ( 'NONE', #6010, #3817, #8543 ) ;
#3664=DIRECTION ( 'NONE',  ( -0.8660254037844387076, -0.4999999999999998890, 0.000000000000000000 ) ) ;
#3668=DIRECTION ( 'NONE',  ( 0.000000000000000000, 0.000000000000000000, -1.000000000000000000 ) ) ;
#3671=ADVANCED_FACE ( 'NONE', ( #1890 ), #366, .F. ) ;
#3672=EDGE_LOOP ( 'NONE', ( #4415, #5112, #13654, #8594 ) ) ;
#3673=FACE_OUTER_BOUND ( 'NONE', #8685, .T. ) ;
#3674=ORIENTED_EDGE ( 'NONE', *, *, #2407, .F. ) ;
#3675=CIRCLE ( 'NONE', #937, 16.50000000000000000 ) ;
#3676=ORIENTED_EDGE ( 'NONE', *, *, #12273, .F. ) ;
#3682=CARTESIAN_POINT ( 'NONE',  ( -88.81638362644000040, 65.17411849586700612, -147.9984795835769944 ) ) ;
#3683=CONICAL_SURFACE ( 'NONE', #6912, 2.042000000000002036, 1.047197551196596965 ) ;
#3684=DIRECTION ( 'NONE',  ( -0.000000000000000000, -0.000000000000000000, 1.000000000000000000 ) ) ;
#3685=DIRECTION ( 'NONE',  ( -1.000000000000000000, 0.000000000000000000, 0.000000000000000000 ) ) ;
#3686=EDGE_LOOP ( 'NONE', ( #7969, #12358, #14648, #14494 ) ) ;
#3687=CARTESIAN_POINT ( 'NONE',  ( -69.77438362644001302, 82.17411849586700612, -83.44847958357698303 ) ) ;
#3688=DIRECTION ( 'NONE',  ( 0.000000000000000000, 0.000000000000000000, 1.000000000000000000 ) ) ;
#3698=DIRECTION ( 'NONE',  ( 0.000000000000000000, 0.000000000000000000, -1.000000000000000000 ) ) ;
#3700=DIRECTION ( 'NONE',  ( 0.000000000000000000, 0.000000000000000000, -1.000000000000000000 ) ) ;
#3703=LINE ( 'NONE', #8281, #9001 ) ;
#3704=ADVANCED_FACE ( 'NONE', ( #6644 ), #14719, .T. ) ;
#3708=VERTEX_POINT ( 'NONE', #13759 ) ;
#3709=ORIENTED_EDGE ( 'NONE', *, *, #706, .F. ) ;
#3710=ORIENTED_EDGE ( 'NONE', *, *, #319, .F. ) ;
#3711=DIRECTION ( 'NONE',  ( 0.000000000000000000, 1.000000000000000000, 0.000000000000000000 ) ) ;
#3712=CARTESIAN_POINT ( 'NONE',  ( -61.72438362644000165, 82.17411849586700612, -80.14847958357698587 ) ) ;
#3713=CARTESIAN_POINT ( 'NONE',  ( -60.43728955831367955, 68.38713492810558137, -83.44847958357698303 ) ) ;
#3714=PLANE ( 'NONE',  #10859 ) ;
#3715=CARTESIAN_POINT ( 'NONE',  ( -86.77438362643999881, 67.53201699523744139, -147.9984795835769944 ) ) ;
#3716=FACE_BOUND ( 'NONE', #10938, .T. ) ;
#3720=ORIENTED_EDGE ( 'NONE', *, *, #10881, .F. ) ;
#3722=EDGE_CURVE ( 'NONE', #11099, #1313, #3133, .T. ) ;
#3724=EDGE_LOOP ( 'NONE', ( #12199, #13746, #6746, #13199 ) ) ;
#3726=ORIENTED_EDGE ( 'NONE', *, *, #10777, .T. ) ;
#3729=LINE ( 'NONE', #8689, #2644 ) ;
#3734=DIRECTION ( 'NONE',  ( 0.000000000000000000, 0.000000000000000000, -1.000000000000000000 ) ) ;
#3735=LINE ( 'NONE', #9625, #5096 ) ;
#3736=EDGE_CURVE ( 'NONE', #1497, #913, #7565, .T. ) ;
#3737=LINE ( 'NONE', #8467, #8569 ) ;
#3738=CARTESIAN_POINT ( 'NONE',  ( -86.77438362644001302, 114.1741184958670061, -15.85886927678779834 ) ) ;
#3740=FACE_OUTER_BOUND ( 'NONE', #9188, .T. ) ;
#3741=EDGE_CURVE ( 'NONE', #8134, #3619, #7010, .T. ) ;
#3743=AXIS2_PLACEMENT_3D ( 'NONE', #11085, #457, #13492 ) ;
#3745=ORIENTED_EDGE ( 'NONE', *, *, #15097, .T. ) ;
#3753=DIRECTION ( 'NONE',  ( 1.287488025362404182E-15, 1.000000000000000000, 0.000000000000000000 ) ) ;
#3754=CARTESIAN_POINT ( 'NONE',  ( -52.77438362644000591, 65.17411849586700612, -145.4984795835769660 ) ) ;
#3757=EDGE_CURVE ( 'NONE', #13652, #4260, #3735, .T. ) ;
#3759=ORIENTED_EDGE ( 'NONE', *, *, #10451, .T. ) ;
#3761=EDGE_CURVE ( 'NONE', #2932, #3473, #2849, .T. ) ;
#3767=ORIENTED_EDGE ( 'NONE', *, *, #10977, .F. ) ;
#3771=CARTESIAN_POINT ( 'NONE',  ( -77.52077156573416516, 164.3482369917340122, -79.59847958357700293 ) ) ;
#3772=CIRCLE ( 'NONE', #43, 8.124999999999992895 ) ;
#3775=DIRECTION ( 'NONE',  ( 0.000000000000000000, 0.000000000000000000, 1.000000000000000000 ) ) ;
#3776=DIRECTION ( 'NONE',  ( 1.000000000000000000, 0.000000000000000000, 0.000000000000000000 ) ) ;
#3777=LINE ( 'NONE', #1452, #8329 ) ;
#3778=PLANE ( 'NONE',  #3139 ) ;
#3780=DIRECTION ( 'NONE',  ( 0.000000000000000000, 0.000000000000000000, -1.000000000000000000 ) ) ;
#3785=EDGE_LOOP ( 'NONE', ( #10845, #13823 ) ) ;
#3786=ORIENTED_EDGE ( 'NONE', *, *, #7761, .T. ) ;
#3788=VECTOR ( 'NONE', #7067, 1000.000000000000000 ) ;
#3789=DIRECTION ( 'NONE',  ( -0.000000000000000000, -0.000000000000000000, 1.000000000000000000 ) ) ;
#3791=DIRECTION ( 'NONE',  ( 0.000000000000000000, 0.000000000000000000, 1.000000000000000000 ) ) ;
#3792=VECTOR ( 'NONE', #3432, 1000.000000000000000 ) ;
#3799=DIRECTION ( 'NONE',  ( -1.000000000000000000, 0.000000000000000000, 0.000000000000000000 ) ) ;
#3802=ORIENTED_EDGE ( 'NONE', *, *, #2703, .F. ) ;
#3803=ORIENTED_EDGE ( 'NONE', *, *, #14520, .T. ) ;
#3804=ORIENTED_EDGE ( 'NONE', *, *, #7928, .T. ) ;
#3806=AXIS2_PLACEMENT_3D ( 'NONE', #11178, #5300, #10015 ) ;
#3808=ADVANCED_FACE ( 'NONE', ( #7168 ), #5938, .F. ) ;
#3812=AXIS2_PLACEMENT_3D ( 'NONE', #5401, #6561, #13835 ) ;
#3813=FACE_OUTER_BOUND ( 'NONE', #7190, .T. ) ;
#3814=EDGE_CURVE ( 'NONE', #14332, #8449, #14063, .T. ) ;
#3815=AXIS2_PLACEMENT_3D ( 'NONE', #2074, #4645, #9363 ) ;
#3817=DIRECTION ( 'NONE',  ( -0.000000000000000000, -0.000000000000000000, 1.000000000000000000 ) ) ;
#3818=CARTESIAN_POINT ( 'NONE',  ( -69.77438362644001302, 82.17411849586700612, -44.99847958358509459 ) ) ;
#3823=PLANE ( 'NONE',  #13802 ) ;
#3826=ORIENTED_EDGE ( 'NONE', *, *, #7188, .T. ) ;
#3828=AXIS2_PLACEMENT_3D ( 'NONE', #9746, #4954, #9590 ) ;
#3830=VECTOR ( 'NONE', #288, 1000.000000000000000 ) ;
#3832=EDGE_CURVE ( 'NONE', #9574, #8280, #13069, .T. ) ;
#3835=CARTESIAN_POINT ( 'NONE',  ( -101.2743836264399988, 114.1741184958669777, -67.49847958357700861 ) ) ;
#3836=ADVANCED_FACE ( 'NONE', ( #13211 ), #10719, .F. ) ;
#3839=VECTOR ( 'NONE', #8398, 1000.000000000000114 ) ;
#3840=CARTESIAN_POINT ( 'NONE',  ( -69.77438362644001302, 82.17411849586700612, -81.84847958357698872 ) ) ;
#3841=EDGE_LOOP ( 'NONE', ( #14195, #8684, #5909, #5050 ) ) ;
#3846=EDGE_LOOP ( 'NONE', ( #11493, #11515, #9934, #2047, #8092 ) ) ;
#3848=EDGE_LOOP ( 'NONE', ( #8410, #15043, #12445, #609 ) ) ;
#3849=EDGE_CURVE ( 'NONE', #1190, #14746, #10032, .T. ) ;
#3855=ADVANCED_FACE ( 'NONE', ( #15288 ), #5063, .F. ) ;
#3856=CYLINDRICAL_SURFACE ( 'NONE', #13705, 2.500000000000002220 ) ;
#3857=FACE_OUTER_BOUND ( 'NONE', #12807, .T. ) ;
#3862=( GEOMETRIC_REPRESENTATION_CONTEXT ( 3 ) GLOBAL_UNCERTAINTY_ASSIGNED_CONTEXT ( ( #6702 ) ) GLOBAL_UNIT_ASSIGNED_CONTEXT ( ( #6237, #8616, #11022 ) ) REPRESENTATION_CONTEXT ( 'NONE', 'WORKASPACE' ) );
#3863=ORIENTED_EDGE ( 'NONE', *, *, #2198, .F. ) ;
#3865=CARTESIAN_POINT ( 'NONE',  ( -69.77438362644100778, 72.17411849586700612, -67.49847958357700861 ) ) ;
#3866=ORIENTED_EDGE ( 'NONE', *, *, #2627, .T. ) ;
#3870=ORIENTED_EDGE ( 'NONE', *, *, #526, .F. ) ;
#3872=EDGE_CURVE ( 'NONE', #704, #9228, #9696, .T. ) ;
#3875=DIRECTION ( 'NONE',  ( 0.000000000000000000, 1.000000000000000000, 0.000000000000000000 ) ) ;
#3876=DIRECTION ( 'NONE',  ( 0.000000000000000000, 0.000000000000000000, -1.000000000000000000 ) ) ;
#3878=CARTESIAN_POINT ( 'NONE',  ( -69.77438362644001302, 82.17411849586700612, -67.69567958357700377 ) ) ;
#3879=DIRECTION ( 'NONE',  ( 0.000000000000000000, 0.000000000000000000, -1.000000000000000000 ) ) ;
#3880=EDGE_LOOP ( 'NONE', ( #12020, #11164, #135 ) ) ;
#3884=VECTOR ( 'NONE', #9163, 1000.000000000000000 ) ;
#3885=ORIENTED_EDGE ( 'NONE', *, *, #10881, .T. ) ;
#3886=EDGE_LOOP ( 'NONE', ( #7390, #11373, #12242, #6872, #174 ) ) ;
#3887=ORIENTED_EDGE ( 'NONE', *, *, #6800, .T. ) ;
#3888=LINE ( 'NONE', #1483, #6565 ) ;
#3894=CIRCLE ( 'NONE', #12806, 2.750000000000002665 ) ;
#3895=DIRECTION ( 'NONE',  ( 0.000000000000000000, 0.000000000000000000, -1.000000000000000000 ) ) ;
#3896=CYLINDRICAL_SURFACE ( 'NONE', #6814, 3.000000000000002665 ) ;
#3897=DIRECTION ( 'NONE',  ( -1.000000000000000000, 0.000000000000000000, 0.000000000000000000 ) ) ;
#3898=CARTESIAN_POINT ( 'NONE',  ( -55.27438362644100067, 99.17411849586700612, -79.59847958357700293 ) ) ;
#3902=VERTEX_POINT ( 'NONE', #14741 ) ;
#3903=ORIENTED_EDGE ( 'NONE', *, *, #4317, .T. ) ;
#3906=VECTOR ( 'NONE', #10971, 1000.000000000000114 ) ;
#3907=DIRECTION ( 'NONE',  ( 0.000000000000000000, 0.000000000000000000, 1.000000000000000000 ) ) ;
#3913=CIRCLE ( 'NONE', #2922, 4.499999999999997335 ) ;
#3916=CARTESIAN_POINT ( 'NONE',  ( -86.77438362644001302, 65.17411849586700612, -86.49847958357699440 ) ) ;
#3919=VERTEX_POINT ( 'NONE', #9857 ) ;
#3922=ORIENTED_EDGE ( 'NONE', *, *, #9993, .T. ) ;
#3926=CARTESIAN_POINT ( 'NONE',  ( -84.73238362643999722, 65.17411849586700612, -147.9984795835769944 ) ) ;
#3927=ADVANCED_FACE ( 'NONE', ( #9776 ), #11176, .T. ) ;
#3930=CARTESIAN_POINT ( 'NONE',  ( -54.81638362644100226, 99.17411849586700612, -147.9984795835769944 ) ) ;
#3933=DIRECTION ( 'NONE',  ( 0.000000000000000000, 0.000000000000000000, 1.000000000000000000 ) ) ;
#3934=ADVANCED_FACE ( 'NONE', ( #7401 ), #6319, .F. ) ;
#3935=DIRECTION ( 'NONE',  ( 0.000000000000000000, 0.000000000000000000, 1.000000000000000000 ) ) ;
#3942=EDGE_CURVE ( 'NONE', #7562, #8783, #10012, .T. ) ;
#3946=DIRECTION ( 'NONE',  ( 0.000000000000000000, 0.000000000000000000, -1.000000000000000000 ) ) ;
#3947=EDGE_CURVE ( 'NONE', #6550, #8981, #6102, .T. ) ;
#3948=CARTESIAN_POINT ( 'NONE',  ( -80.52077156573417938, 164.3482369917340122, -152.4984795835769944 ) ) ;
#3949=FACE_OUTER_BOUND ( 'NONE', #8737, .T. ) ;
#3951=CARTESIAN_POINT ( 'NONE',  ( -54.81638362644100226, 97.99516924618178848, -147.9984795835769944 ) ) ;
#3952=EDGE_CURVE ( 'NONE', #3619, #4969, #12272, .T. ) ;
#3953=PLANE ( 'NONE',  #8788 ) ;
#3954=EDGE_LOOP ( 'NONE', ( #12650, #12360, #10606, #10463, #14346 ) ) ;
#3956=ORIENTED_EDGE ( 'NONE', *, *, #136, .T. ) ;
#3957=ORIENTED_EDGE ( 'NONE', *, *, #14074, .T. ) ;
#3958=VERTEX_POINT ( 'NONE', #403 ) ;
#3959=VERTEX_POINT ( 'NONE', #5216 ) ;
#3964=DIRECTION ( 'NONE',  ( 0.000000000000000000, 0.000000000000000000, 1.000000000000000000 ) ) ;
#3967=CARTESIAN_POINT ( 'NONE',  ( -73.64736697264332577, 89.17411849586700612, -44.99847958359595168 ) ) ;
#3969=CARTESIAN_POINT ( 'NONE',  ( -81.27438362643999881, 82.17411849586700612, -82.44847958357698303 ) ) ;
#3970=FACE_OUTER_BOUND ( 'NONE', #7906, .T. ) ;
#3971=ORIENTED_EDGE ( 'NONE', *, *, #8199, .F. ) ;
#3974=VERTEX_POINT ( 'NONE', #311 ) ;
#3979=FACE_OUTER_BOUND ( 'NONE', #12692, .T. ) ;
#3980=LINE ( 'NONE', #8709, #6738 ) ;
#3981=DIRECTION ( 'NONE',  ( 1.000000000000000000, 0.000000000000000000, 0.000000000000000000 ) ) ;
#3982=FACE_OUTER_BOUND ( 'NONE', #5983, .T. ) ;
#3985=PLANE ( 'NONE',  #8699 ) ;
#3986=VERTEX_POINT ( 'NONE', #2655 ) ;
#3989=CIRCLE ( 'NONE', #3011, 3.000000000000002665 ) ;
#3990=CARTESIAN_POINT ( 'NONE',  ( -86.77438362643999881, 65.17411849586700612, -146.8195303338917768 ) ) ;
#3992=ORIENTED_EDGE ( 'NONE', *, *, #8743, .T. ) ;
#3994=AXIS2_PLACEMENT_3D ( 'NONE', #10126, #10281, #1918 ) ;
#3995=CYLINDRICAL_SURFACE ( 'NONE', #4739, 4.499999999999997335 ) ;
#3999=DIRECTION ( 'NONE',  ( -1.000000000000000000, 0.000000000000000000, 0.000000000000000000 ) ) ;
#4002=DIRECTION ( 'NONE',  ( -1.000000000000000000, 0.000000000000000000, 0.000000000000000000 ) ) ;
#4006=DIRECTION ( 'NONE',  ( 0.000000000000000000, 0.000000000000000000, -1.000000000000000000 ) ) ;
#4008=ORIENTED_EDGE ( 'NONE', *, *, #10092, .T. ) ;
#4011=CARTESIAN_POINT ( 'NONE',  ( -50.07438362643999596, 65.17411849586700612, -145.2984795835770058 ) ) ;
#4013=VERTEX_POINT ( 'NONE', #14432 ) ;
#4014=AXIS2_PLACEMENT_3D ( 'NONE', #7163, #9690, #14426 ) ;
#4018=CARTESIAN_POINT ( 'NONE',  ( -86.77438362643999881, 65.17411849586700612, -145.2984795835770058 ) ) ;
#4019=AXIS2_PLACEMENT_3D ( 'NONE', #5651, #2363, #3298 ) ;
#4020=CARTESIAN_POINT ( 'NONE',  ( -86.77438362644100778, 99.17411849586700612, -145.2984795835770058 ) ) ;
#4022=CARTESIAN_POINT ( 'NONE',  ( -86.77438362644001302, 65.17411849586700612, -86.49847958357699440 ) ) ;
#4033=ORIENTED_EDGE ( 'NONE', *, *, #2509, .F. ) ;
#4035=VECTOR ( 'NONE', #355, 1000.000000000000000 ) ;
#4039=ADVANCED_FACE ( 'NONE', ( #3113 ), #6693, .T. ) ;
#4040=VECTOR ( 'NONE', #1451, 1000.000000000000000 ) ;
#4046=EDGE_CURVE ( 'NONE', #15273, #13375, #14735, .T. ) ;
#4050=AXIS2_PLACEMENT_3D ( 'NONE', #13698, #5716, #10186 ) ;
#4052=VECTOR ( 'NONE', #13888, 1000.000000000000000 ) ;
#4053=FACE_OUTER_BOUND ( 'NONE', #10055, .T. ) ;
#4054=ORIENTED_EDGE ( 'NONE', *, *, #11063, .F. ) ;
#4057=AXIS2_PLACEMENT_3D ( 'NONE', #6322, #5066, #483 ) ;
#4059=ORIENTED_EDGE ( 'NONE', *, *, #10132, .F. ) ;
#4061=FACE_OUTER_BOUND ( 'NONE', #14888, .T. ) ;
#4063=CARTESIAN_POINT ( 'NONE',  ( -86.77438362643999881, 65.17411849586700612, -149.9984795835770228 ) ) ;
#4064=DIRECTION ( 'NONE',  ( -1.000000000000000000, 0.000000000000000000, 0.000000000000000000 ) ) ;
#4065=DIRECTION ( 'NONE',  ( 0.000000000000000000, 0.000000000000000000, -1.000000000000000000 ) ) ;
#4066=TOROIDAL_SURFACE ( 'NONE', #2823, 2.700000000000000178, 0.2000000000000000111 ) ;
#4067=CARTESIAN_POINT ( 'NONE',  ( -88.81638362644100937, 99.17411849586700612, -147.9984795835769944 ) ) ;
#4069=APPLICATION_CONTEXT ( 'automotive_design' ) ;
#4070=DIRECTION ( 'NONE',  ( -0.000000000000000000, -0.000000000000000000, -1.000000000000000000 ) ) ;
#4071=ORIENTED_EDGE ( 'NONE', *, *, #9703, .T. ) ;
#4072=CARTESIAN_POINT ( 'NONE',  ( -52.77438362644100067, 101.5320169952374414, -150.4984795835770228 ) ) ;
#4074=CIRCLE ( 'NONE', #1591, 2.000000000000001776 ) ;
#4079=VECTOR ( 'NONE', #6507, 1000.000000000000000 ) ;
#4080=CARTESIAN_POINT ( 'NONE',  ( -96.77438362643999881, 65.17411849586700612, -152.4984795835769944 ) ) ;
#4081=AXIS2_PLACEMENT_3D ( 'NONE', #12408, #603, #1993 ) ;
#4085=DIRECTION ( 'NONE',  ( 0.000000000000000000, 0.000000000000000000, -1.000000000000000000 ) ) ;
#4087=FACE_BOUND ( 'NONE', #8202, .T. ) ;
#4089=ORIENTED_EDGE ( 'NONE', *, *, #5193, .F. ) ;
#4090=EDGE_CURVE ( 'NONE', #13263, #6604, #851, .T. ) ;
#4092=ORIENTED_EDGE ( 'NONE', *, *, #11601, .F. ) ;
#4093=CARTESIAN_POINT ( 'NONE',  ( -69.77438362644001302, 74.17411849586699191, -58.99847958357700151 ) ) ;
#4095=VERTEX_POINT ( 'NONE', #7985 ) ;
#4096=AXIS2_PLACEMENT_3D ( 'NONE', #4598, #3431, #8165 ) ;
#4098=DIRECTION ( 'NONE',  ( -1.000000000000000000, 0.000000000000000000, 0.000000000000000000 ) ) ;
#4102=CIRCLE ( 'NONE', #12770, 17.00000000000000000 ) ;
#4109=LINE ( 'NONE', #4187, #6794 ) ;
#4110=EDGE_CURVE ( 'NONE', #2784, #13871, #768, .T. ) ;
#4111=EDGE_CURVE ( 'NONE', #5237, #3237, #4498, .T. ) ;
#4112=ORIENTED_EDGE ( 'NONE', *, *, #15156, .T. ) ;
#4114=VERTEX_POINT ( 'NONE', #701 ) ;
#4115=AXIS2_PLACEMENT_3D ( 'NONE', #8325, #2491, #14361 ) ;
#4116=ORIENTED_EDGE ( 'NONE', *, *, #2131, .T. ) ;
#4117=ORIENTED_EDGE ( 'NONE', *, *, #10758, .T. ) ;
#4119=CARTESIAN_POINT ( 'NONE',  ( -89.52438362644001302, 99.17411849586700612, -145.4984795835769660 ) ) ;
#4124=EDGE_CURVE ( 'NONE', #11097, #840, #11260, .T. ) ;
#4125=DIRECTION ( 'NONE',  ( -1.000000000000000000, 0.000000000000000000, 0.000000000000000000 ) ) ;
#4127=EDGE_CURVE ( 'NONE', #2251, #4356, #5588, .T. ) ;
#4129=CARTESIAN_POINT ( 'NONE',  ( -54.81638362644000040, 63.99516924618178848, -147.9984795835769944 ) ) ;
#4130=DIRECTION ( 'NONE',  ( -1.287488025362404182E-15, -1.000000000000000000, 0.000000000000000000 ) ) ;
#4133=ORIENTED_EDGE ( 'NONE', *, *, #13793, .T. ) ;
#4135=DIRECTION ( 'NONE',  ( 0.000000000000000000, 0.000000000000000000, 1.000000000000000000 ) ) ;
#4137=EDGE_LOOP ( 'NONE', ( #3726, #13114, #9782, #10790, #10405 ) ) ;
#4139=ORIENTED_EDGE ( 'NONE', *, *, #4376, .T. ) ;
#4140=EDGE_CURVE ( 'NONE', #469, #840, #12647, .T. ) ;
#4142=EDGE_CURVE ( 'NONE', #587, #11316, #3344, .T. ) ;
#4143=VECTOR ( 'NONE', #5794, 1000.000000000000000 ) ;
#4145=AXIS2_PLACEMENT_3D ( 'NONE', #12879, #15105, #5831 ) ;
#4146=DIRECTION ( 'NONE',  ( 1.000000000000000000, 0.000000000000000000, 0.000000000000000000 ) ) ;
#4147=DIRECTION ( 'NONE',  ( 0.000000000000000000, -4.130293990420970006E-17, 1.000000000000000000 ) ) ;
#4150=CARTESIAN_POINT ( 'NONE',  ( -80.27438362643999881, 82.17411849586700612, -82.44847958357698303 ) ) ;
#4151=CARTESIAN_POINT ( 'NONE',  ( -73.03793661009240168, 75.17411849586699191, -44.70344037800862225 ) ) ;
#4154=VECTOR ( 'NONE', #1024, 1000.000000000000000 ) ;
#4155=DIRECTION ( 'NONE',  ( 0.8660254037844383745, -0.5000000000000003331, 0.000000000000000000 ) ) ;
#4156=EDGE_CURVE ( 'NONE', #3473, #2932, #5848, .T. ) ;
#4157=VECTOR ( 'NONE', #13934, 1000.000000000000000 ) ;
#4160=ORIENTED_EDGE ( 'NONE', *, *, #5326, .F. ) ;
#4162=DIRECTION ( 'NONE',  ( 0.000000000000000000, 0.000000000000000000, -1.000000000000000000 ) ) ;
#4163=DIRECTION ( 'NONE',  ( 0.000000000000000000, -0.000000000000000000, 1.000000000000000000 ) ) ;
#4165=CARTESIAN_POINT ( 'NONE',  ( -42.77438362644000591, 59.67411849586700612, -152.4984795835769944 ) ) ;
#4166=CARTESIAN_POINT ( 'NONE',  ( -77.52077156573416516, 60.67411849586702743, -152.4984795835769944 ) ) ;
#4169=CARTESIAN_POINT ( 'NONE',  ( -67.06350624369862601, 97.94473565475263399, -93.86023119279390414 ) ) ;
#4170=DIRECTION ( 'NONE',  ( -0.000000000000000000, -0.000000000000000000, 1.000000000000000000 ) ) ;
#4171=ORIENTED_EDGE ( 'NONE', *, *, #10051, .F. ) ;
#4174=DIRECTION ( 'NONE',  ( 1.000000000000000000, 0.000000000000000000, 0.000000000000000000 ) ) ;
#4176=VERTEX_POINT ( 'NONE', #9148 ) ;
#4178=CARTESIAN_POINT ( 'NONE',  ( -86.77438362643999881, 65.17411849586700612, -182.2484795835770228 ) ) ;
#4179=DIRECTION ( 'NONE',  ( 0.8660254037844383745, -0.5000000000000003331, 0.000000000000000000 ) ) ;
#4180=AXIS2_PLACEMENT_3D ( 'NONE', #4022, #8750, #377 ) ;
#4184=EDGE_CURVE ( 'NONE', #11099, #9860, #7328, .T. ) ;
#4185=CARTESIAN_POINT ( 'NONE',  ( -64.53565528768383786, 67.29799558322736175, -81.84847958357697451 ) ) ;
#4187=CARTESIAN_POINT ( 'NONE',  ( -85.77438362644001302, 82.17411849586700612, -183.7533135795160320 ) ) ;
#4188=ORIENTED_EDGE ( 'NONE', *, *, #13109, .T. ) ;
#4190=ORIENTED_EDGE ( 'NONE', *, *, #7354, .T. ) ;
#4193=AXIS2_PLACEMENT_3D ( 'NONE', #2689, #5020, #11140 ) ;
#4195=LINE ( 'NONE', #1710, #2114 ) ;
#4200=DIRECTION ( 'NONE',  ( 0.000000000000000000, 0.000000000000000000, -1.000000000000000000 ) ) ;
#4209=ORIENTED_EDGE ( 'NONE', *, *, #10858, .F. ) ;
#4210=VERTEX_POINT ( 'NONE', #4662 ) ;
#4211=DIRECTION ( 'NONE',  ( 1.000000000000000000, 0.000000000000000000, 0.000000000000000000 ) ) ;
#4213=LINE ( 'NONE', #6557, #8551 ) ;
#4214=CARTESIAN_POINT ( 'NONE',  ( -73.80978675135780520, 64.78624853950366003, -81.84847958357697451 ) ) ;
#4216=DIRECTION ( 'NONE',  ( -0.000000000000000000, -0.000000000000000000, -1.000000000000000000 ) ) ;
#4217=CARTESIAN_POINT ( 'NONE',  ( -52.77438362644100067, 99.17411849586700612, -150.4984795835770228 ) ) ;
#4219=ADVANCED_FACE ( 'NONE', ( #10621, #8302, #3716, #13121, #11870, #14269 ), #3411, .F. ) ;
#4225=DIRECTION ( 'NONE',  ( 0.000000000000000000, 0.000000000000000000, 1.000000000000000000 ) ) ;
#4227=EDGE_CURVE ( 'NONE', #9170, #1220, #8301, .T. ) ;
#4230=LINE ( 'NONE', #5484, #7478 ) ;
#4231=ADVANCED_FACE ( 'NONE', ( #6987 ), #7072, .F. ) ;
#4236=EDGE_CURVE ( 'NONE', #10374, #8857, #15188, .T. ) ;
#4239=FACE_BOUND ( 'NONE', #5153, .T. ) ;
#4241=AXIS2_PLACEMENT_3D ( 'NONE', #1891, #11356, #1965 ) ;
#4242=EDGE_LOOP ( 'NONE', ( #15234, #13528, #3120, #1949 ) ) ;
#4245=ORIENTED_EDGE ( 'NONE', *, *, #9961, .F. ) ;
#4246=CARTESIAN_POINT ( 'NONE',  ( -52.77438362644000591, 99.17411849586700612, -86.49847958357699440 ) ) ;
#4247=AXIS2_PLACEMENT_3D ( 'NONE', #420, #5312, #4064 ) ;
#4248=DIRECTION ( 'NONE',  ( 0.000000000000000000, 1.000000000000000000, 0.000000000000000000 ) ) ;
#4249=AXIS2_PLACEMENT_3D ( 'NONE', #10575, #11898, #6104 ) ;
#4252=CARTESIAN_POINT ( 'NONE',  ( -62.02799568714584666, 59.67411849586701322, -79.59847958357700293 ) ) ;
#4255=EDGE_LOOP ( 'NONE', ( #3674, #6935, #13180, #8209 ) ) ;
#4256=AXIS2_PLACEMENT_3D ( 'NONE', #12801, #12961, #4732 ) ;
#4257=ORIENTED_EDGE ( 'NONE', *, *, #4490, .T. ) ;
#4260=VERTEX_POINT ( 'NONE', #3566 ) ;
#4262=AXIS2_PLACEMENT_3D ( 'NONE', #2299, #7050, #10600 ) ;
#4267=FACE_OUTER_BOUND ( 'NONE', #4508, .T. ) ;
#4268=VECTOR ( 'NONE', #14760, 1000.000000000000000 ) ;
#4270=CARTESIAN_POINT ( 'NONE',  ( -69.77438362644001302, 90.17411849586700612, -58.99847958357700151 ) ) ;
#4272=DIRECTION ( 'NONE',  ( -0.000000000000000000, -0.000000000000000000, 1.000000000000000000 ) ) ;
#4276=DIRECTION ( 'NONE',  ( 0.000000000000000000, 0.000000000000000000, 1.000000000000000000 ) ) ;
#4277=VECTOR ( 'NONE', #6118, 1000.000000000000000 ) ;
#4279=ORIENTED_EDGE ( 'NONE', *, *, #886, .F. ) ;
#4280=ORIENTED_EDGE ( 'NONE', *, *, #7929, .F. ) ;
#4286=DIRECTION ( 'NONE',  ( 0.000000000000000000, 1.000000000000000000, 0.000000000000000000 ) ) ;
#4288=AXIS2_PLACEMENT_3D ( 'NONE', #14192, #13126, #6078 ) ;
#4289=DIRECTION ( 'NONE',  ( 0.000000000000000000, 0.000000000000000000, 1.000000000000000000 ) ) ;
#4291=CARTESIAN_POINT ( 'NONE',  ( -71.44964421664379017, 75.17411849586702033, -44.18949531478482839 ) ) ;
#4295=EDGE_LOOP ( 'NONE', ( #2176, #611, #11593, #6994 ) ) ;
#4296=CARTESIAN_POINT ( 'NONE',  ( -86.77438362643999881, 67.53201699523744139, -147.9984795835769944 ) ) ;
#4297=VERTEX_POINT ( 'NONE', #11943 ) ;
#4299=ORIENTED_EDGE ( 'NONE', *, *, #14000, .F. ) ;
#4304=VECTOR ( 'NONE', #11262, 1000.000000000000114 ) ;
#4305=FACE_OUTER_BOUND ( 'NONE', #14298, .T. ) ;
#4308=AXIS2_PLACEMENT_3D ( 'NONE', #6783, #10330, #12442 ) ;
#4309=VECTOR ( 'NONE', #11685, 1000.000000000000000 ) ;
#4310=ADVANCED_FACE ( 'NONE', ( #15267 ), #9674, .T. ) ;
#4311=FACE_OUTER_BOUND ( 'NONE', #2463, .T. ) ;
#4312=FACE_OUTER_BOUND ( 'NONE', #6532, .T. ) ;
#4317=EDGE_CURVE ( 'NONE', #14576, #6162, #14492, .T. ) ;
#4319=CARTESIAN_POINT ( 'NONE',  ( -86.77438362644100778, 99.17411849586700612, -150.4984795835770228 ) ) ;
#4326=EDGE_CURVE ( 'NONE', #16, #9472, #12039, .T. ) ;
#4327=DIRECTION ( 'NONE',  ( 0.000000000000000000, 0.000000000000000000, 1.000000000000000000 ) ) ;
#4328=CARTESIAN_POINT ( 'NONE',  ( -50.73238362643999722, 65.17411849586700612, -147.9984795835769944 ) ) ;
#4331=DIRECTION ( 'NONE',  ( 0.000000000000000000, 1.000000000000000000, 0.000000000000000000 ) ) ;
#4332=DIRECTION ( 'NONE',  ( -1.000000000000000000, 0.000000000000000000, 0.000000000000000000 ) ) ;
#4335=ORIENTED_EDGE ( 'NONE', *, *, #9906, .F. ) ;
#4337=DIRECTION ( 'NONE',  ( 0.000000000000000000, 0.000000000000000000, 1.000000000000000000 ) ) ;
#4339=EDGE_LOOP ( 'NONE', ( #3476, #7874 ) ) ;
#4342=ORIENTED_EDGE ( 'NONE', *, *, #14827, .F. ) ;
#4343=EDGE_LOOP ( 'NONE', ( #12689, #15249, #4361, #12221, #1534 ) ) ;
#4344=ORIENTED_EDGE ( 'NONE', *, *, #6304, .F. ) ;
#4347=VECTOR ( 'NONE', #8650, 1000.000000000000000 ) ;
#4350=DIRECTION ( 'NONE',  ( 1.000000000000000000, 0.000000000000000000, 0.000000000000000000 ) ) ;
#4351=FACE_OUTER_BOUND ( 'NONE', #3672, .T. ) ;
#4352=CARTESIAN_POINT ( 'NONE',  ( -53.70938362644000819, 81.46011849586699327, -81.84847958357697451 ) ) ;
#4353=CARTESIAN_POINT ( 'NONE',  ( -47.27438362644100778, 57.67411849586700612, -79.49847958357700861 ) ) ;
#4356=VERTEX_POINT ( 'NONE', #9911 ) ;
#4357=CARTESIAN_POINT ( 'NONE',  ( -69.77438362644001302, 82.17411849586700612, -3.496191900462991775 ) ) ;
#4360=ORIENTED_EDGE ( 'NONE', *, *, #3098, .F. ) ;
#4361=ORIENTED_EDGE ( 'NONE', *, *, #2104, .T. ) ;
#4363=CARTESIAN_POINT ( 'NONE',  ( -65.73898050152220662, 64.78624853950366003, -83.44847958357698303 ) ) ;
#4365=DIRECTION ( 'NONE',  ( 1.000000000000000000, 0.000000000000000000, 0.000000000000000000 ) ) ;
#4367=CARTESIAN_POINT ( 'NONE',  ( -69.77438362644002723, 75.17411849587348627, -43.99847958364158984 ) ) ;
#4368=CYLINDRICAL_SURFACE ( 'NONE', #892, 16.00000000000000000 ) ;
#4372=AXIS2_PLACEMENT_3D ( 'NONE', #6134, #11370, #1909 ) ;
#4375=CARTESIAN_POINT ( 'NONE',  ( -82.27438362643999881, 99.17411849586700612, -145.4984795835769660 ) ) ;
#4376=EDGE_CURVE ( 'NONE', #2744, #4095, #1397, .T. ) ;
#4378=CARTESIAN_POINT ( 'NONE',  ( -89.52438362644001302, 99.17411849586700612, -152.4984795835769944 ) ) ;
#4379=VECTOR ( 'NONE', #8492, 1000.000000000000000 ) ;
#4380=EDGE_LOOP ( 'NONE', ( #2157, #11248, #2155, #13077 ) ) ;
#4383=VERTEX_POINT ( 'NONE', #2551 ) ;
#4386=PLANE ( 'NONE',  #8816 ) ;
#4390=AXIS2_PLACEMENT_3D ( 'NONE', #13757, #3051, #5467 ) ;
#4391=FACE_OUTER_BOUND ( 'NONE', #8269, .T. ) ;
#4394=ORIENTED_EDGE ( 'NONE', *, *, #14226, .F. ) ;
#4397=ORIENTED_EDGE ( 'NONE', *, *, #3009, .F. ) ;
#4398=VECTOR ( 'NONE', #9466, 1000.000000000000000 ) ;
#4402=DIRECTION ( 'NONE',  ( 0.000000000000000000, 1.000000000000000000, 0.000000000000000000 ) ) ;
#4404=LINE ( 'NONE', #5270, #4562 ) ;
#4405=CARTESIAN_POINT ( 'NONE',  ( -69.77438362644001302, 82.17411849586700612, -43.99847958357699440 ) ) ;
#4406=CARTESIAN_POINT ( 'NONE',  ( -69.77438362644001302, 82.17411849586700612, -29.37106258560738681 ) ) ;
#4407=ADVANCED_FACE ( 'NONE', ( #14639 ), #9838, .F. ) ;
#4412=CARTESIAN_POINT ( 'NONE',  ( -59.27438362644000591, 82.17411849586700612, -152.4984795835769944 ) ) ;
#4413=VERTEX_POINT ( 'NONE', #8676 ) ;
#4414=ORIENTED_EDGE ( 'NONE', *, *, #14450, .T. ) ;
#4415=ORIENTED_EDGE ( 'NONE', *, *, #4127, .F. ) ;
#4417=VERTEX_POINT ( 'NONE', #221 ) ;
#4418=CARTESIAN_POINT ( 'NONE',  ( -89.27438362644100778, 110.1741184958670061, -79.59847958357700293 ) ) ;
#4419=EDGE_CURVE ( 'NONE', #8823, #8783, #463, .T. ) ;
#4424=DIRECTION ( 'NONE',  ( 1.000000000000000000, 0.000000000000000000, 0.000000000000000000 ) ) ;
#4426=CARTESIAN_POINT ( 'NONE',  ( -69.77438362644001302, 81.46011849586699327, -83.44847958357698303 ) ) ;
#4428=LINE ( 'NONE', #12721, #8719 ) ;
#4429=CARTESIAN_POINT ( 'NONE',  ( -52.77438362643999881, 67.53201699523744139, -147.9984795835769944 ) ) ;
#4430=LINE ( 'NONE', #7987, #14522 ) ;
#4431=CARTESIAN_POINT ( 'NONE',  ( -80.27438362643999881, 82.17411849586700612, -150.4984795835769944 ) ) ;
#4438=FACE_OUTER_BOUND ( 'NONE', #4380, .T. ) ;
#4441=CARTESIAN_POINT ( 'NONE',  ( -77.89938362643999881, 82.17411849586700612, -79.49847958357700861 ) ) ;
#4444=CARTESIAN_POINT ( 'NONE',  ( -69.77438362644001302, 82.17411849586700612, -93.49847958357699440 ) ) ;
#4449=ORIENTED_EDGE ( 'NONE', *, *, #11979, .T. ) ;
#4451=ORIENTED_EDGE ( 'NONE', *, *, #13613, .T. ) ;
#4452=EDGE_LOOP ( 'NONE', ( #5783, #1480, #11630, #6291 ) ) ;
#4453=LINE ( 'NONE', #14909, #12167 ) ;
#4454=VERTEX_POINT ( 'NONE', #10363 ) ;
#4456=ORIENTED_EDGE ( 'NONE', *, *, #7343, .T. ) ;
#4459=ADVANCED_FACE ( 'NONE', ( #2071 ), #15017, .T. ) ;
#4460=CARTESIAN_POINT ( 'NONE',  ( -69.77438362644001302, 81.46011849586699327, -83.44847958357698303 ) ) ;
#4461=DIRECTION ( 'NONE',  ( -0.7071067811865474617, 8.659560562354921765E-17, 0.7071067811865474617 ) ) ;
#4462=FACE_OUTER_BOUND ( 'NONE', #556, .T. ) ;
#4475=LINE ( 'NONE', #979, #8074 ) ;
#4476=CARTESIAN_POINT ( 'NONE',  ( -69.77438362644001302, 82.17411849586700612, -81.84847958357698872 ) ) ;
#4479=DIRECTION ( 'NONE',  ( 0.000000000000000000, 0.000000000000000000, -1.000000000000000000 ) ) ;
#4480=VERTEX_POINT ( 'NONE', #14793 ) ;
#4490=EDGE_CURVE ( 'NONE', #8420, #2616, #8565, .T. ) ;
#4492=DIRECTION ( 'NONE',  ( 0.000000000000000000, 0.000000000000000000, -1.000000000000000000 ) ) ;
#4494=DIRECTION ( 'NONE',  ( 0.000000000000000000, 0.000000000000000000, -1.000000000000000000 ) ) ;
#4495=CARTESIAN_POINT ( 'NONE',  ( -52.77438362643999881, 67.53201699523744139, -150.4984795835770228 ) ) ;
#4498=LINE ( 'NONE', #2012, #8798 ) ;
#4499=DIRECTION ( 'NONE',  ( 0.000000000000000000, 0.000000000000000000, -1.000000000000000000 ) ) ;
#4500=CARTESIAN_POINT ( 'NONE',  ( -53.77438362644000591, 82.17411849586700612, -93.49847958357699440 ) ) ;
#4501=VECTOR ( 'NONE', #23, 1000.000000000000000 ) ;
#4508=EDGE_LOOP ( 'NONE', ( #4644, #13507, #1677, #13032 ) ) ;
#4509=VECTOR ( 'NONE', #5813, 1000.000000000000000 ) ;
#4511=CARTESIAN_POINT ( 'NONE',  ( -83.02438362644100778, 99.17411849586700612, -150.4984795835770228 ) ) ;
#4516=DIRECTION ( 'NONE',  ( 0.8660254037844383745, -0.5000000000000003331, 0.000000000000000000 ) ) ;
#4517=CARTESIAN_POINT ( 'NONE',  ( -68.42626121176353138, 75.17411849586696349, -44.11946707556869995 ) ) ;
#4519=CARTESIAN_POINT ( 'NONE',  ( -52.77438362643999881, 65.17411849586700612, -79.59847958357700293 ) ) ;
#4520=DIRECTION ( 'NONE',  ( 0.000000000000000000, 0.000000000000000000, -1.000000000000000000 ) ) ;
#4523=AXIS2_PLACEMENT_3D ( 'NONE', #3452, #4542, #7032 ) ;
#4524=ORIENTED_EDGE ( 'NONE', *, *, #8948, .F. ) ;
#4525=DIRECTION ( 'NONE',  ( 1.000000000000000000, 0.000000000000000000, 0.000000000000000000 ) ) ;
#4532=AXIS2_PLACEMENT_3D ( 'NONE', #11707, #9296, #5829 ) ;
#4536=AXIS2_PLACEMENT_3D ( 'NONE', #8812, #11076, #13401 ) ;
#4538=FACE_OUTER_BOUND ( 'NONE', #4824, .T. ) ;
#4539=EDGE_LOOP ( 'NONE', ( #7887, #5360 ) ) ;
#4542=DIRECTION ( 'NONE',  ( 0.000000000000000000, -0.000000000000000000, 1.000000000000000000 ) ) ;
#4545=LINE ( 'NONE', #13786, #9781 ) ;
#4547=ORIENTED_EDGE ( 'NONE', *, *, #14630, .F. ) ;
#4550=DIRECTION ( 'NONE',  ( 1.000000000000000000, 0.000000000000000000, 0.000000000000000000 ) ) ;
#4554=CARTESIAN_POINT ( 'NONE',  ( -86.77438362643999881, 65.17411849586700612, -147.9984795835769944 ) ) ;
#4560=VECTOR ( 'NONE', #8544, 1000.000000000000114 ) ;
#4561=ADVANCED_FACE ( 'NONE', ( #12699 ), #11237, .F. ) ;
#4562=VECTOR ( 'NONE', #4179, 1000.000000000000114 ) ;
#4564=VERTEX_POINT ( 'NONE', #5665 ) ;
#4565=ORIENTED_EDGE ( 'NONE', *, *, #2693, .F. ) ;
#4571=AXIS2_PLACEMENT_3D ( 'NONE', #12255, #1624, #9677 ) ;
#4577=ADVANCED_FACE ( 'NONE', ( #10062 ), #13646, .F. ) ;
#4578=PLANE ( 'NONE',  #10816 ) ;
#4580=CARTESIAN_POINT ( 'NONE',  ( -52.77438362644100067, 96.81621999649657084, -147.9984795835769944 ) ) ;
#4583=VERTEX_POINT ( 'NONE', #1216 ) ;
#4584=ORIENTED_EDGE ( 'NONE', *, *, #1144, .T. ) ;
#4585=VERTEX_POINT ( 'NONE', #5975 ) ;
#4588=VECTOR ( 'NONE', #7556, 1000.000000000000000 ) ;
#4590=ADVANCED_FACE ( 'NONE', ( #8129 ), #13104, .F. ) ;
#4591=DIRECTION ( 'NONE',  ( -1.000000000000000000, 0.000000000000000000, 0.000000000000000000 ) ) ;
#4593=FACE_OUTER_BOUND ( 'NONE', #6974, .T. ) ;
#4594=FACE_OUTER_BOUND ( 'NONE', #13523, .T. ) ;
#4596=DIRECTION ( 'NONE',  ( -0.8660254037844387076, -0.4999999999999998890, 0.000000000000000000 ) ) ;
#4598=CARTESIAN_POINT ( 'NONE',  ( -79.02077156573416516, 103.6741184958669777, -152.4984795835769944 ) ) ;
#4603=VERTEX_POINT ( 'NONE', #3392 ) ;
#4604=CARTESIAN_POINT ( 'NONE',  ( -86.77438362644001302, 99.17411849586700612, -145.4984795835769660 ) ) ;
#4605=EDGE_CURVE ( 'NONE', #4417, #15299, #8314, .T. ) ;
#4611=EDGE_LOOP ( 'NONE', ( #2368, #9308 ) ) ;
#4612=AXIS2_PLACEMENT_3D ( 'NONE', #7195, #11914, #2518 ) ;
#4618=CARTESIAN_POINT ( 'NONE',  ( -69.77438362644001302, 82.17411849586700612, -83.44847958357698303 ) ) ;
#4620=EDGE_CURVE ( 'NONE', #6732, #1190, #10516, .T. ) ;
#4636=DIRECTION ( 'NONE',  ( 0.000000000000000000, 0.000000000000000000, -1.000000000000000000 ) ) ;
#4638=DIRECTION ( 'NONE',  ( 1.000000000000000000, 0.000000000000000000, 0.000000000000000000 ) ) ;
#4640=DIRECTION ( 'NONE',  ( 0.000000000000000000, 1.000000000000000000, 0.000000000000000000 ) ) ;
#4643=CYLINDRICAL_SURFACE ( 'NONE', #7244, 5.499999999999998224 ) ;
#4644=ORIENTED_EDGE ( 'NONE', *, *, #4708, .T. ) ;
#4645=DIRECTION ( 'NONE',  ( 0.000000000000000000, 0.000000000000000000, -1.000000000000000000 ) ) ;
#4646=CIRCLE ( 'NONE', #13079, 16.00000000000000000 ) ;
#4648=AXIS2_PLACEMENT_3D ( 'NONE', #1468, #9751, #5037 ) ;
#4651=ORIENTED_EDGE ( 'NONE', *, *, #10171, .T. ) ;
#4653=ORIENTED_EDGE ( 'NONE', *, *, #7651, .T. ) ;
#4655=CARTESIAN_POINT ( 'NONE',  ( -69.77438362644001302, 82.17411849586700612, -80.14847958357698587 ) ) ;
#4656=FACE_OUTER_BOUND ( 'NONE', #2731, .T. ) ;
#4659=CYLINDRICAL_SURFACE ( 'NONE', #7118, 2.750000000000002665 ) ;
#4660=AXIS2_PLACEMENT_3D ( 'NONE', #8924, #9927, #1867 ) ;
#4662=CARTESIAN_POINT ( 'NONE',  ( -50.27438362643999881, 65.17411849586700612, -145.2984795835770058 ) ) ;
#4663=CYLINDRICAL_SURFACE ( 'NONE', #11798, 5.500000000000005329 ) ;
#4666=VERTEX_POINT ( 'NONE', #6964 ) ;
#4669=EDGE_LOOP ( 'NONE', ( #14315, #1608, #6832 ) ) ;
#4670=ORIENTED_EDGE ( 'NONE', *, *, #11417, .F. ) ;
#4672=DIRECTION ( 'NONE',  ( -1.000000000000000000, 0.000000000000000000, 0.000000000000000000 ) ) ;
#4676=PLANE ( 'NONE',  #12795 ) ;
#4677=DIRECTION ( 'NONE',  ( -1.000000000000000000, 0.000000000000000000, 0.000000000000000000 ) ) ;
#4679=EDGE_CURVE ( 'NONE', #13729, #10133, #1377, .T. ) ;
#4680=DIRECTION ( 'NONE',  ( 0.000000000000000000, 1.000000000000000000, 0.000000000000000000 ) ) ;
#4681=FACE_OUTER_BOUND ( 'NONE', #11552, .T. ) ;
#4683=CARTESIAN_POINT ( 'NONE',  ( -86.77438362643999881, 67.53201699523744139, -147.9984795835769944 ) ) ;
#4686=ORIENTED_EDGE ( 'NONE', *, *, #12644, .T. ) ;
#4691=VERTEX_POINT ( 'NONE', #11769 ) ;
#4694=AXIS2_PLACEMENT_3D ( 'NONE', #8890, #3152, #735 ) ;
#4695=CARTESIAN_POINT ( 'NONE',  ( -84.73238362643999722, 65.17411849586700612, -147.9984795835769944 ) ) ;
#4696=ADVANCED_FACE ( 'NONE', ( #14165, #2379 ), #11926, .T. ) ;
#4697=LINE ( 'NONE', #3682, #5111 ) ;
#4699=FACE_OUTER_BOUND ( 'NONE', #14555, .T. ) ;
#4700=ORIENTED_EDGE ( 'NONE', *, *, #7275, .F. ) ;
#4701=FACE_OUTER_BOUND ( 'NONE', #4242, .T. ) ;
#4702=DIRECTION ( 'NONE',  ( -1.000000000000000000, 0.000000000000000000, 0.000000000000000000 ) ) ;
#4704=EDGE_LOOP ( 'NONE', ( #6404, #6548, #12515, #4245 ) ) ;
#4705=SURFACE_STYLE_USAGE ( .BOTH. , #6122 ) ;
#4707=EDGE_LOOP ( 'NONE', ( #11180, #4209, #5558, #13731, #1441 ) ) ;
#4708=EDGE_CURVE ( 'NONE', #13728, #13838, #4475, .T. ) ;
#4710=EDGE_CURVE ( 'NONE', #7835, #2560, #3777, .T. ) ;
#4711=EDGE_CURVE ( 'NONE', #13765, #1574, #1139, .T. ) ;
#4712=CARTESIAN_POINT ( 'NONE',  ( -86.77438362644100778, 99.17411849586700612, -145.2984795835770058 ) ) ;
#4718=ORIENTED_EDGE ( 'NONE', *, *, #11521, .F. ) ;
#4719=DIRECTION ( 'NONE',  ( 0.000000000000000000, 0.000000000000000000, -1.000000000000000000 ) ) ;
#4721=FACE_OUTER_BOUND ( 'NONE', #1970, .T. ) ;
#4725=ORIENTED_EDGE ( 'NONE', *, *, #11048, .T. ) ;
#4730=DIRECTION ( 'NONE',  ( 0.000000000000000000, 1.000000000000000000, 0.000000000000000000 ) ) ;
#4732=DIRECTION ( 'NONE',  ( 1.000000000000000000, 0.000000000000000000, 0.000000000000000000 ) ) ;
#4733=DIRECTION ( 'NONE',  ( 0.000000000000000000, 0.000000000000000000, 1.000000000000000000 ) ) ;
#4735=DIRECTION ( 'NONE',  ( -1.000000000000000000, 0.000000000000000000, -0.000000000000000000 ) ) ;
#4736=ORIENTED_EDGE ( 'NONE', *, *, #10578, .T. ) ;
#4739=AXIS2_PLACEMENT_3D ( 'NONE', #14692, #14916, #2836 ) ;
#4740=ORIENTED_EDGE ( 'NONE', *, *, #6592, .T. ) ;
#4742=AXIS2_PLACEMENT_3D ( 'NONE', #11681, #6959, #10512 ) ;
#4743=CARTESIAN_POINT ( 'NONE',  ( -69.77438362644001302, 82.17411849586700612, -93.49847958357699440 ) ) ;
#4744=CARTESIAN_POINT ( 'NONE',  ( -63.90163006221920483, 66.22072495173567575, -81.84847958357697451 ) ) ;
#4746=FACE_OUTER_BOUND ( 'NONE', #6342, .T. ) ;
#4747=DIRECTION ( 'NONE',  ( -1.000000000000000000, 0.000000000000000000, 0.000000000000000000 ) ) ;
#4751=DIRECTION ( 'NONE',  ( 0.000000000000000000, 0.000000000000000000, -1.000000000000000000 ) ) ;
#4755=VERTEX_POINT ( 'NONE', #202 ) ;
#4756=CARTESIAN_POINT ( 'NONE',  ( -57.27438362644000591, 99.17411849586700612, -152.4984795835769944 ) ) ;
#4759=VERTEX_POINT ( 'NONE', #1524 ) ;
#4760=ORIENTED_EDGE ( 'NONE', *, *, #1668, .F. ) ;
#4762=EDGE_CURVE ( 'NONE', #11586, #10105, #14765, .T. ) ;
#4763=VECTOR ( 'NONE', #6088, 1000.000000000000000 ) ;
#4769=CARTESIAN_POINT ( 'NONE',  ( -69.77438362644001302, 84.67411849586700612, -51.99847958357699440 ) ) ;
#4770=CARTESIAN_POINT ( 'NONE',  ( -52.77438362644100067, 96.81621999649657084, -150.4984795835770228 ) ) ;
#4772=ORIENTED_EDGE ( 'NONE', *, *, #5193, .T. ) ;
#4777=ORIENTED_EDGE ( 'NONE', *, *, #15300, .F. ) ;
#4781=TOROIDAL_SURFACE ( 'NONE', #6774, 2.700000000000000178, 0.2000000000000000111 ) ;
#4783=DIRECTION ( 'NONE',  ( 0.000000000000000000, 0.000000000000000000, -1.000000000000000000 ) ) ;
#4785=EDGE_CURVE ( 'NONE', #9369, #5220, #8341, .T. ) ;
#4787=DIRECTION ( 'NONE',  ( -1.224646799147353947E-16, 1.000000000000000000, 0.000000000000000000 ) ) ;
#4790=CARTESIAN_POINT ( 'NONE',  ( -54.81638362644100226, 100.3530677455522238, -147.9984795835769944 ) ) ;
#4793=EDGE_CURVE ( 'NONE', #2784, #14784, #2631, .T. ) ;
#4795=ORIENTED_EDGE ( 'NONE', *, *, #13781, .T. ) ;
#4796=CARTESIAN_POINT ( 'NONE',  ( -52.77438362643999881, 65.17411849586700612, -150.4984795835770228 ) ) ;
#4797=ORIENTED_EDGE ( 'NONE', *, *, #14443, .T. ) ;
#4799=DIRECTION ( 'NONE',  ( 0.000000000000000000, 0.000000000000000000, -1.000000000000000000 ) ) ;
#4803=EDGE_LOOP ( 'NONE', ( #6043, #4092, #2080 ) ) ;
#4804=AXIS2_PLACEMENT_3D ( 'NONE', #1250, #10481, #13979 ) ;
#4805=AXIS2_PLACEMENT_3D ( 'NONE', #3395, #4337, #9059 ) ;
#4807=DIRECTION ( 'NONE',  ( 0.000000000000000000, 0.000000000000000000, -1.000000000000000000 ) ) ;
#4809=EDGE_CURVE ( 'NONE', #6326, #6998, #6371, .T. ) ;
#4810=CARTESIAN_POINT ( 'NONE',  ( -69.77438362644001302, 99.17411849586700612, -81.84847958357698872 ) ) ;
#4811=CARTESIAN_POINT ( 'NONE',  ( -59.27438362644000591, 82.17411849586700612, -80.44847958357698303 ) ) ;
#4815=AXIS2_PLACEMENT_3D ( 'NONE', #7717, #1804, #11422 ) ;
#4819=CARTESIAN_POINT ( 'NONE',  ( -57.27438362644000591, 99.17411849586700612, -86.49847958357699440 ) ) ;
#4820=EDGE_LOOP ( 'NONE', ( #7994, #516 ) ) ;
#4821=DIRECTION ( 'NONE',  ( 0.000000000000000000, 0.000000000000000000, -1.000000000000000000 ) ) ;
#4822=VERTEX_POINT ( 'NONE', #1606 ) ;
#4823=EDGE_LOOP ( 'NONE', ( #5910, #12037 ) ) ;
#4824=EDGE_LOOP ( 'NONE', ( #3255, #1509, #14171, #6632 ) ) ;
#4826=CIRCLE ( 'NONE', #9022, 16.50000000000000000 ) ;
#4827=AXIS2_PLACEMENT_3D ( 'NONE', #8766, #303, #6533 ) ;
#4830=CARTESIAN_POINT ( 'NONE',  ( -88.81638362644100937, 97.99516924618178848, -147.9984795835769944 ) ) ;
#4834=FACE_OUTER_BOUND ( 'NONE', #14723, .T. ) ;
#4835=CARTESIAN_POINT ( 'NONE',  ( 0.000000000000000000, 0.000000000000000000, -79.49847958357700861 ) ) ;
#4836=DIRECTION ( 'NONE',  ( 0.000000000000000000, 0.000000000000000000, 1.000000000000000000 ) ) ;
#4838=DIRECTION ( 'NONE',  ( 0.4999999999999998890, -0.8660254037844387076, 0.000000000000000000 ) ) ;
#4839=ORIENTED_EDGE ( 'NONE', *, *, #6098, .T. ) ;
#4840=LINE ( 'NONE', #409, #12814 ) ;
#4841=VERTEX_POINT ( 'NONE', #14322 ) ;
#4847=EDGE_LOOP ( 'NONE', ( #1223, #2115 ) ) ;
#4850=PLANE ( 'NONE',  #5499 ) ;
#4851=DIRECTION ( 'NONE',  ( 0.000000000000000000, 0.000000000000000000, -1.000000000000000000 ) ) ;
#4854=EDGE_CURVE ( 'NONE', #10808, #10427, #10912, .T. ) ;
#4856=EDGE_LOOP ( 'NONE', ( #2281, #2645, #4524, #6163 ) ) ;
#4858=LINE ( 'NONE', #9493, #9211 ) ;
#4859=VECTOR ( 'NONE', #11203, 1000.000000000000114 ) ;
#4862=AXIS2_PLACEMENT_3D ( 'NONE', #12840, #1903, #3215 ) ;
#4865=ORIENTED_EDGE ( 'NONE', *, *, #15269, .T. ) ;
#4873=ADVANCED_FACE ( 'NONE', ( #6359 ), #9822, .T. ) ;
#4874=CIRCLE ( 'NONE', #10560, 10.49999999999999467 ) ;
#4877=AXIS2_PLACEMENT_3D ( 'NONE', #6777, #3268, #11274 ) ;
#4878=DIRECTION ( 'NONE',  ( 0.000000000000000000, 0.000000000000000000, -1.000000000000000000 ) ) ;
#4879=EDGE_LOOP ( 'NONE', ( #113, #72 ) ) ;
#4880=CARTESIAN_POINT ( 'NONE',  ( -75.01311196519617397, 67.29799558322736175, -83.44847958357698303 ) ) ;
#4882=ORIENTED_EDGE ( 'NONE', *, *, #10381, .F. ) ;
#4887=VECTOR ( 'NONE', #12767, 1000.000000000000000 ) ;
#4888=VERTEX_POINT ( 'NONE', #13563 ) ;
#4890=AXIS2_PLACEMENT_3D ( 'NONE', #619, #14738, #10225 ) ;
#4896=DIRECTION ( 'NONE',  ( 0.000000000000000000, 0.000000000000000000, -1.000000000000000000 ) ) ;
#4898=VECTOR ( 'NONE', #4155, 1000.000000000000114 ) ;
#4903=CARTESIAN_POINT ( 'NONE',  ( -52.77438362644100067, 99.17411849586700612, -147.9984795835769944 ) ) ;
#4904=ORIENTED_EDGE ( 'NONE', *, *, #14622, .T. ) ;
#4907=EDGE_LOOP ( 'NONE', ( #7804, #14067, #2809, #14348 ) ) ;
#4908=EDGE_LOOP ( 'NONE', ( #12949, #2662, #7876, #3287 ) ) ;
#4910=AXIS2_PLACEMENT_3D ( 'NONE', #8396, #8321, #8239 ) ;
#4911=CARTESIAN_POINT ( 'NONE',  ( -86.77438362643999881, 62.81621999649657084, -147.9984795835769944 ) ) ;
#4915=ADVANCED_FACE ( 'NONE', ( #11215 ), #5490, .F. ) ;
#4916=CARTESIAN_POINT ( 'NONE',  ( -50.73238362643999722, 66.35306774555222376, -147.9984795835769944 ) ) ;
#4917=CARTESIAN_POINT ( 'NONE',  ( -56.52438362644099357, 99.17411849586700612, -150.4984795835770228 ) ) ;
#4920=CARTESIAN_POINT ( 'NONE',  ( -69.43626855224066219, 89.17411849586700612, -43.99847958365484146 ) ) ;
#4921=EDGE_LOOP ( 'NONE', ( #9133, #10212, #7141, #2286 ) ) ;
#4926=FACE_BOUND ( 'NONE', #3785, .T. ) ;
#4930=CARTESIAN_POINT ( 'NONE',  ( -69.77438362644001302, 82.17411849586700612, -150.4984795835769944 ) ) ;
#4933=CARTESIAN_POINT ( 'NONE',  ( -69.77438362644001302, 99.17411849586700612, -81.84847958357698872 ) ) ;
#4938=CARTESIAN_POINT ( 'NONE',  ( -69.77438362644001302, 92.67411849586700612, -80.44847958357698303 ) ) ;
#4940=EDGE_LOOP ( 'NONE', ( #7288, #9586, #1776, #4397 ) ) ;
#4941=EDGE_CURVE ( 'NONE', #12703, #6907, #14699, .T. ) ;
#4943=DIRECTION ( 'NONE',  ( -1.000000000000000000, 0.000000000000000000, 0.000000000000000000 ) ) ;
#4944=CARTESIAN_POINT ( 'NONE',  ( -86.77438362644001302, 59.67411849586700612, -152.4984795835769944 ) ) ;
#4948=FACE_OUTER_BOUND ( 'NONE', #3018, .T. ) ;
#4949=ORIENTED_EDGE ( 'NONE', *, *, #2887, .T. ) ;
#4950=DIRECTION ( 'NONE',  ( 0.000000000000000000, 0.000000000000000000, 1.000000000000000000 ) ) ;
#4954=DIRECTION ( 'NONE',  ( 1.000000000000000000, 0.000000000000000000, -0.000000000000000000 ) ) ;
#4956=EDGE_LOOP ( 'NONE', ( #10505, #1613, #7114, #14229, #6180 ) ) ;
#4961=CARTESIAN_POINT ( 'NONE',  ( -80.52077156573417938, 164.3482369917340122, -79.59847958357700293 ) ) ;
#4962=DIRECTION ( 'NONE',  ( 0.000000000000000000, 0.000000000000000000, -1.000000000000000000 ) ) ;
#4964=CARTESIAN_POINT ( 'NONE',  ( -84.27438362643998460, 65.17411849586700612, -145.2984795835770058 ) ) ;
#4965=DIRECTION ( 'NONE',  ( 0.000000000000000000, 0.000000000000000000, -1.000000000000000000 ) ) ;
#4968=DIRECTION ( 'NONE',  ( 0.000000000000000000, 1.000000000000000000, 0.000000000000000000 ) ) ;
#4969=VERTEX_POINT ( 'NONE', #5332 ) ;
#4971=EDGE_CURVE ( 'NONE', #1421, #7439, #13297, .T. ) ;
#4972=ORIENTED_EDGE ( 'NONE', *, *, #12470, .T. ) ;
#4973=EDGE_LOOP ( 'NONE', ( #9554, #1629, #539, #2172 ) ) ;
#4975=ORIENTED_EDGE ( 'NONE', *, *, #11135, .F. ) ;
#4978=SURFACE_STYLE_FILL_AREA ( #234 ) ;
#4981=DIRECTION ( 'NONE',  ( -1.287488025362404182E-15, -1.000000000000000000, 0.000000000000000000 ) ) ;
#4985=CARTESIAN_POINT ( 'NONE',  ( -53.77438362644000591, 82.17411849586700612, -138.4984795835769944 ) ) ;
#4987=ORIENTED_EDGE ( 'NONE', *, *, #11812, .F. ) ;
#4989=ADVANCED_FACE ( 'NONE', ( #6335, #6257 ), #6186, .T. ) ;
#4990=ORIENTED_EDGE ( 'NONE', *, *, #5738, .T. ) ;
#4991=CIRCLE ( 'NONE', #2005, 4.500000000000003553 ) ;
#5002=VECTOR ( 'NONE', #8094, 1000.000000000000000 ) ;
#5005=ORIENTED_EDGE ( 'NONE', *, *, #1762, .T. ) ;
#5006=CARTESIAN_POINT ( 'NONE',  ( -89.27438362643999881, 65.17411849586700612, -79.59847958357700293 ) ) ;
#5007=ADVANCED_FACE ( 'NONE', ( #3979 ), #13308, .F. ) ;
#5010=SHAPE_REPRESENTATION ( 'Pneumatic Cylinder Piston', ( #285 ), #15141 ) ;
#5011=SURFACE_SIDE_STYLE ('',( #7036 ) ) ;
#5014=CIRCLE ( 'NONE', #13187, 4.500000000000003553 ) ;
#5020=DIRECTION ( 'NONE',  ( 0.000000000000000000, 0.000000000000000000, -1.000000000000000000 ) ) ;
#5021=LINE ( 'NONE', #10761, #5790 ) ;
#5023=DIRECTION ( 'NONE',  ( -1.000000000000000000, 0.000000000000000000, 0.000000000000000000 ) ) ;
#5025=ORIENTED_EDGE ( 'NONE', *, *, #7265, .T. ) ;
#5028=AXIS2_PLACEMENT_3D ( 'NONE', #201, #8506, #11925 ) ;
#5031=ORIENTED_EDGE ( 'NONE', *, *, #12900, .F. ) ;
#5034=CIRCLE ( 'NONE', #11720, 0.2000000000000057288 ) ;
#5035=DIRECTION ( 'NONE',  ( -1.000000000000000000, 0.000000000000000000, 0.000000000000000000 ) ) ;
#5036=AXIS2_PLACEMENT_3D ( 'NONE', #7078, #11490, #9153 ) ;
#5037=DIRECTION ( 'NONE',  ( -1.000000000000000000, 0.000000000000000000, 0.000000000000000000 ) ) ;
#5038=EDGE_CURVE ( 'NONE', #11568, #7541, #2668, .T. ) ;
#5039=CARTESIAN_POINT ( 'NONE',  ( -56.85838362644099675, 99.17411849586700612, -147.9984795835769944 ) ) ;
#5045=CARTESIAN_POINT ( 'NONE',  ( -69.77438362644001302, 82.17411849586700612, -79.49847958357700861 ) ) ;
#5049=EDGE_LOOP ( 'NONE', ( #7563, #7223, #10548, #4033 ) ) ;
#5050=ORIENTED_EDGE ( 'NONE', *, *, #14827, .T. ) ;
#5052=AXIS2_PLACEMENT_3D ( 'NONE', #8698, #1567, #316 ) ;
#5059=AXIS2_PLACEMENT_3D ( 'NONE', #9760, #13276, #7224 ) ;
#5060=DIRECTION ( 'NONE',  ( -1.000000000000000000, 0.000000000000000000, 0.000000000000000000 ) ) ;
#5061=LINE ( 'NONE', #309, #13828 ) ;
#5062=CARTESIAN_POINT ( 'NONE',  ( -59.02799568714584666, 60.67411849586701322, -73.34256232478206528 ) ) ;
#5063=CYLINDRICAL_SURFACE ( 'NONE', #2359, 4.500000000000003553 ) ;
#5064=LINE ( 'NONE', #7320, #1134 ) ;
#5065=EDGE_CURVE ( 'NONE', #13986, #2062, #7596, .T. ) ;
#5066=DIRECTION ( 'NONE',  ( -0.000000000000000000, -0.000000000000000000, -1.000000000000000000 ) ) ;
#5068=DIRECTION ( 'NONE',  ( 0.000000000000000000, 0.000000000000000000, -1.000000000000000000 ) ) ;
#5070=ORIENTED_EDGE ( 'NONE', *, *, #12932, .T. ) ;
#5079=CARTESIAN_POINT ( 'NONE',  ( -57.02438362643999170, 65.17411849586700612, -182.2484795835770228 ) ) ;
#5081=CARTESIAN_POINT ( 'NONE',  ( -61.42438362644001160, 82.17411849586700612, -80.14847958357698587 ) ) ;
#5082=CARTESIAN_POINT ( 'NONE',  ( -52.77438362644100067, 99.17411849586700612, -150.4984795835770228 ) ) ;
#5084=AXIS2_PLACEMENT_3D ( 'NONE', #8584, #6356, #5179 ) ;
#5087=EDGE_CURVE ( 'NONE', #12014, #13910, #3342, .T. ) ;
#5088=ORIENTED_EDGE ( 'NONE', *, *, #6429, .F. ) ;
#5089=LINE ( 'NONE', #14533, #4379 ) ;
#5094=ORIENTED_EDGE ( 'NONE', *, *, #9993, .F. ) ;
#5095=AXIS2_PLACEMENT_3D ( 'NONE', #4011, #1913, #11300 ) ;
#5096=VECTOR ( 'NONE', #14360, 1000.000000000000000 ) ;
#5101=ADVANCED_FACE ( 'NONE', ( #419, #12063 ), #14599, .T. ) ;
#5106=DIRECTION ( 'NONE',  ( -1.000000000000000000, 0.000000000000000000, -0.000000000000000000 ) ) ;
#5108=VECTOR ( 'NONE', #13007, 1000.000000000000114 ) ;
#5110=CARTESIAN_POINT ( 'NONE',  ( -52.77438362643999881, 62.81621999649657084, -147.9984795835769944 ) ) ;
#5111=VECTOR ( 'NONE', #14145, 1000.000000000000114 ) ;
#5112=ORIENTED_EDGE ( 'NONE', *, *, #7230, .F. ) ;
#5113=AXIS2_PLACEMENT_3D ( 'NONE', #12029, #5273, #7299 ) ;
#5115=EDGE_LOOP ( 'NONE', ( #3863, #11469, #10125, #15117, #14121 ) ) ;
#5116=CARTESIAN_POINT ( 'NONE',  ( -69.77438362644001302, 82.17411849586700612, -150.4984795835769944 ) ) ;
#5118=EDGE_LOOP ( 'NONE', ( #2701, #1897 ) ) ;
#5119=ORIENTED_EDGE ( 'NONE', *, *, #7660, .F. ) ;
#5120=CIRCLE ( 'NONE', #10299, 17.00000000000000000 ) ;
#5121=DIRECTION ( 'NONE',  ( -0.8660254037844387076, -0.4999999999999998890, 0.000000000000000000 ) ) ;
#5122=CIRCLE ( 'NONE', #11554, 0.1999999999999987899 ) ;
#5125=PLANE ( 'NONE',  #15201 ) ;
#5128=DIRECTION ( 'NONE',  ( 0.000000000000000000, 0.000000000000000000, 1.000000000000000000 ) ) ;
#5129=ORIENTED_EDGE ( 'NONE', *, *, #13140, .F. ) ;
#5131=AXIS2_PLACEMENT_3D ( 'NONE', #1828, #14925, #812 ) ;
#5133=AXIS2_PLACEMENT_3D ( 'NONE', #8377, #10694, #2318 ) ;
#5134=ORIENTED_EDGE ( 'NONE', *, *, #3952, .T. ) ;
#5137=EDGE_LOOP ( 'NONE', ( #8534, #8204, #6115, #15095, #1060 ) ) ;
#5138=CARTESIAN_POINT ( 'NONE',  ( -53.70938362644000819, 81.46011849586699327, -83.44847958357698303 ) ) ;
#5140=EDGE_CURVE ( 'NONE', #11281, #4564, #7489, .T. ) ;
#5145=AXIS2_PLACEMENT_3D ( 'NONE', #4178, #3307, #596 ) ;
#5148=CARTESIAN_POINT ( 'NONE',  ( -50.73238362644099197, 100.3530677455522238, -147.9984795835769944 ) ) ;
#5151=CARTESIAN_POINT ( 'NONE',  ( -73.76311196519618818, 67.29799558322736175, -83.44847958357698303 ) ) ;
#5153=EDGE_LOOP ( 'NONE', ( #14177, #6120 ) ) ;
#5154=ORIENTED_EDGE ( 'NONE', *, *, #3349, .F. ) ;
#5155=UNCERTAINTY_MEASURE_WITH_UNIT (LENGTH_MEASURE( 1.000000000000000082E-05 ), #11839, 'distance_accuracy_value', 'NONE');
#5157=ADVANCED_FACE ( 'NONE', ( #11416, #14759 ), #1882, .T. ) ;
#5162=DIRECTION ( 'NONE',  ( 0.000000000000000000, -1.000000000000000000, 0.000000000000000000 ) ) ;
#5166=DIRECTION ( 'NONE',  ( 0.000000000000000000, 0.000000000000000000, -1.000000000000000000 ) ) ;
#5168=VERTEX_POINT ( 'NONE', #13679 ) ;
#5170=EDGE_CURVE ( 'NONE', #7524, #13652, #8087, .T. ) ;
#5175=AXIS2_PLACEMENT_3D ( 'NONE', #5525, #9218, #13882 ) ;
#5177=CARTESIAN_POINT ( 'NONE',  ( -80.52077156573417938, 164.3482369917340122, -73.34256232478206528 ) ) ;
#5179=DIRECTION ( 'NONE',  ( -1.000000000000000000, 0.000000000000000000, 0.000000000000000000 ) ) ;
#5180=EDGE_CURVE ( 'NONE', #4176, #2932, #10325, .T. ) ;
#5181=DIRECTION ( 'NONE',  ( 0.000000000000000000, -1.000000000000000000, 0.000000000000000000 ) ) ;
#5183=CARTESIAN_POINT ( 'NONE',  ( -42.77438362644000591, 65.17411849586700612, -79.59847958357700293 ) ) ;
#5186=AXIS2_PLACEMENT_3D ( 'NONE', #4554, #9277, #678 ) ;
#5187=ORIENTED_EDGE ( 'NONE', *, *, #6346, .T. ) ;
#5188=ADVANCED_FACE ( 'NONE', ( #12660 ), #6854, .T. ) ;
#5193=EDGE_CURVE ( 'NONE', #6231, #3959, #863, .T. ) ;
#5195=DIRECTION ( 'NONE',  ( 0.3469356515732570645, 0.9378889346118971515, 0.000000000000000000 ) ) ;
#5197=DIRECTION ( 'NONE',  ( 0.000000000000000000, -0.000000000000000000, 1.000000000000000000 ) ) ;
#5198=CARTESIAN_POINT ( 'NONE',  ( -48.27438362644000591, 99.17411849586700612, -152.4984795835769944 ) ) ;
#5201=CARTESIAN_POINT ( 'NONE',  ( -62.27438362644000591, 89.17411849586700612, -57.99847958357699440 ) ) ;
#5204=ORIENTED_EDGE ( 'NONE', *, *, #2584, .F. ) ;
#5206=ORIENTED_EDGE ( 'NONE', *, *, #7265, .F. ) ;
#5207=ORIENTED_EDGE ( 'NONE', *, *, #10009, .F. ) ;
#5209=DIRECTION ( 'NONE',  ( 0.000000000000000000, -1.000000000000000000, 0.000000000000000000 ) ) ;
#5213=CARTESIAN_POINT ( 'NONE',  ( -52.77438362643999881, 62.81621999649657084, -150.4984795835770228 ) ) ;
#5214=CARTESIAN_POINT ( 'NONE',  ( -52.77438362644000591, 82.17411849586700612, -3.496191900462991775 ) ) ;
#5215=LINE ( 'NONE', #1329, #8015 ) ;
#5216=CARTESIAN_POINT ( 'NONE',  ( -62.02799568714584666, 103.6741184958669919, -152.4984795835769944 ) ) ;
#5217=DIRECTION ( 'NONE',  ( 1.000000000000000000, -1.287488025362404182E-15, 0.000000000000000000 ) ) ;
#5219=DIRECTION ( 'NONE',  ( -1.000000000000000000, 0.000000000000000000, 0.000000000000000000 ) ) ;
#5220=VERTEX_POINT ( 'NONE', #10096 ) ;
#5222=ORIENTED_EDGE ( 'NONE', *, *, #12631, .F. ) ;
#5227=CARTESIAN_POINT ( 'NONE',  ( -82.52438362644100778, 99.17411849586700612, -149.9984795835770228 ) ) ;
#5229=CARTESIAN_POINT ( 'NONE',  ( -86.77438362643999881, 62.81621999649657084, -147.9984795835769944 ) ) ;
#5230=FACE_BOUND ( 'NONE', #12214, .T. ) ;
#5231=ADVANCED_FACE ( 'NONE', ( #783 ), #6639, .F. ) ;
#5233=DIRECTION ( 'NONE',  ( -1.000000000000000000, 0.000000000000000000, -0.000000000000000000 ) ) ;
#5235=LINE ( 'NONE', #4375, #7122 ) ;
#5237=VERTEX_POINT ( 'NONE', #5311 ) ;
#5241=ORIENTED_EDGE ( 'NONE', *, *, #14757, .T. ) ;
#5242=CIRCLE ( 'NONE', #12924, 17.00000000000000000 ) ;
#5243=CARTESIAN_POINT ( 'NONE',  ( -69.77438362644001302, 82.17411849586700612, -81.84847958357698872 ) ) ;
#5246=EDGE_CURVE ( 'NONE', #11629, #13653, #4213, .T. ) ;
#5247=AXIS2_PLACEMENT_3D ( 'NONE', #6874, #1973, #12759 ) ;
#5251=DIRECTION ( 'NONE',  ( 0.000000000000000000, 1.000000000000000000, 0.000000000000000000 ) ) ;
#5254=VERTEX_POINT ( 'NONE', #2976 ) ;
#5255=AXIS2_PLACEMENT_3D ( 'NONE', #7738, #4006, #9040 ) ;
#5257=EDGE_LOOP ( 'NONE', ( #1971, #1499, #2742, #4008, #8494, #14377, #8135, #8761, #9932, #8099, #13872, #7640, #14885, #5475, #2595, #432, #7673, #11492, #4342, #10764, #14554, #14191, #8156, #193 ) ) ;
#5258=CARTESIAN_POINT ( 'NONE',  ( -73.64736697264743270, 75.17411849586699191, -57.99847958357699440 ) ) ;
#5260=VERTEX_POINT ( 'NONE', #7713 ) ;
#5261=VECTOR ( 'NONE', #6778, 1000.000000000000000 ) ;
#5264=ADVANCED_FACE ( 'NONE', ( #715, #7788 ), #1958, .T. ) ;
#5265=DIRECTION ( 'NONE',  ( -1.000000000000000000, 0.000000000000000000, 0.000000000000000000 ) ) ;
#5267=CARTESIAN_POINT ( 'NONE',  ( -52.77438362643999881, 65.17411849586700612, -145.4984795835769944 ) ) ;
#5268=AXIS2_PLACEMENT_3D ( 'NONE', #14152, #2283, #11448 ) ;
#5270=CARTESIAN_POINT ( 'NONE',  ( -86.77438362643999881, 67.53201699523744139, -150.4984795835770228 ) ) ;
#5273=DIRECTION ( 'NONE',  ( 0.000000000000000000, -0.000000000000000000, 1.000000000000000000 ) ) ;
#5277=EDGE_CURVE ( 'NONE', #13838, #13566, #6707, .T. ) ;
#5278=VERTEX_POINT ( 'NONE', #5769 ) ;
#5282=EDGE_LOOP ( 'NONE', ( #12280, #13003, #5305, #1772 ) ) ;
#5289=VECTOR ( 'NONE', #12825, 1000.000000000000000 ) ;
#5293=EDGE_CURVE ( 'NONE', #2023, #10086, #14056, .T. ) ;
#5300=DIRECTION ( 'NONE',  ( 0.000000000000000000, 0.000000000000000000, -1.000000000000000000 ) ) ;
#5301=ORIENTED_EDGE ( 'NONE', *, *, #9833, .T. ) ;
#5303=ORIENTED_EDGE ( 'NONE', *, *, #2147, .F. ) ;
#5304=AXIS2_PLACEMENT_3D ( 'NONE', #3336, #1400, #4968 ) ;
#5305=ORIENTED_EDGE ( 'NONE', *, *, #12556, .F. ) ;
#5306=VERTEX_POINT ( 'NONE', #940 ) ;
#5308=CARTESIAN_POINT ( 'NONE',  ( -76.26311196519618818, 67.29799558322736175, -83.44847958357698303 ) ) ;
#5309=AXIS2_PLACEMENT_3D ( 'NONE', #5856, #15128, #6011 ) ;
#5310=AXIS2_PLACEMENT_3D ( 'NONE', #10065, #14798, #6677 ) ;
#5311=CARTESIAN_POINT ( 'NONE',  ( -102.2743836264399988, 65.17411849586700612, -152.4984795835769944 ) ) ;
#5312=DIRECTION ( 'NONE',  ( -0.000000000000000000, -0.000000000000000000, 1.000000000000000000 ) ) ;
#5313=DIRECTION ( 'NONE',  ( 1.000000000000000000, 0.000000000000000000, 0.000000000000000000 ) ) ;
#5314=CARTESIAN_POINT ( 'NONE',  ( -88.81638362644100937, 97.99516924618178848, -147.9984795835769944 ) ) ;
#5318=CARTESIAN_POINT ( 'NONE',  ( -86.77438362644100778, 96.81621999649657084, -150.4984795835770228 ) ) ;
#5319=CIRCLE ( 'NONE', #14708, 16.06499999999999773 ) ;
#5320=ORIENTED_EDGE ( 'NONE', *, *, #13699, .F. ) ;
#5324=CARTESIAN_POINT ( 'NONE',  ( -52.77438362643999881, 65.17411849586700612, -149.9984795835770228 ) ) ;
#5325=AXIS2_PLACEMENT_3D ( 'NONE', #7898, #13647, #15019 ) ;
#5326=EDGE_CURVE ( 'NONE', #10086, #4564, #7326, .T. ) ;
#5327=AXIS2_PLACEMENT_3D ( 'NONE', #903, #10433, #9356 ) ;
#5328=PLANE ( 'NONE',  #13542 ) ;
#5329=CARTESIAN_POINT ( 'NONE',  ( -52.77438362643999881, 65.17411849586700612, -147.9984795835769944 ) ) ;
#5330=FACE_OUTER_BOUND ( 'NONE', #5118, .T. ) ;
#5331=LINE ( 'NONE', #7590, #10208 ) ;
#5332=CARTESIAN_POINT ( 'NONE',  ( -84.73238362644100619, 100.3530677455522238, -147.9984795835769944 ) ) ;
#5333=CARTESIAN_POINT ( 'NONE',  ( -72.71333998487527595, 97.90337055318686055, -93.68950548826974511 ) ) ;
#5334=CARTESIAN_POINT ( 'NONE',  ( -52.77438362644100067, 101.5320169952374414, -147.9984795835769944 ) ) ;
#5337=ORIENTED_EDGE ( 'NONE', *, *, #14260, .F. ) ;
#5338=COLOUR_RGB ( '', 0.66274510, 0.83137255, 0.94901961) ;
#5339=LINE ( 'NONE', #1758, #4079 ) ;
#5341=VERTEX_POINT ( 'NONE', #8159 ) ;
#5342=VECTOR ( 'NONE', #13369, 1000.000000000000114 ) ;
#5343=ADVANCED_FACE ( 'NONE', ( #12890 ), #8045, .F. ) ;
#5351=AXIS2_PLACEMENT_3D ( 'NONE', #14808, #3181, #694 ) ;
#5352=CARTESIAN_POINT ( 'NONE',  ( -96.77438362643999881, 110.1741184958670061, -79.59847958357700293 ) ) ;
#5356=DIRECTION ( 'NONE',  ( 1.000000000000000000, 0.000000000000000000, 0.000000000000000000 ) ) ;
#5357=EDGE_LOOP ( 'NONE', ( #10352, #11096 ) ) ;
#5358=CYLINDRICAL_SURFACE ( 'NONE', #5310, 3.000000000000002665 ) ;
#5359=ORIENTED_EDGE ( 'NONE', *, *, #7103, .T. ) ;
#5360=ORIENTED_EDGE ( 'NONE', *, *, #11805, .T. ) ;
#5361=VERTEX_POINT ( 'NONE', #4744 ) ;
#5362=AXIS2_PLACEMENT_3D ( 'NONE', #8927, #4272, #2805 ) ;
#5364=ADVANCED_FACE ( 'NONE', ( #11576 ), #4676, .F. ) ;
#5368=VECTOR ( 'NONE', #8813, 1000.000000000000114 ) ;
#5370=EDGE_CURVE ( 'NONE', #11654, #6682, #11807, .T. ) ;
#5374=CARTESIAN_POINT ( 'NONE',  ( -77.82438362644001018, 82.17411849586700612, -80.44847958357698303 ) ) ;
#5375=DIRECTION ( 'NONE',  ( -1.000000000000000000, 0.000000000000000000, 0.000000000000000000 ) ) ;
#5378=CIRCLE ( 'NONE', #10556, 11.49999999999999645 ) ;
#5379=DIRECTION ( 'NONE',  ( 0.8660254037844383745, -0.5000000000000003331, 0.000000000000000000 ) ) ;
#5381=DIRECTION ( 'NONE',  ( 0.000000000000000000, -1.000000000000000000, 0.000000000000000000 ) ) ;
#5382=CIRCLE ( 'NONE', #14771, 3.749999999999996447 ) ;
#5385=AXIS2_PLACEMENT_3D ( 'NONE', #7862, #12596, #4146 ) ;
#5386=CARTESIAN_POINT ( 'NONE',  ( -50.02438362644000591, 65.17411849586700612, -86.49847958357699440 ) ) ;
#5388=ORIENTED_EDGE ( 'NONE', *, *, #894, .F. ) ;
#5390=ADVANCED_FACE ( 'NONE', ( #5697 ), #10631, .T. ) ;
#5392=VECTOR ( 'NONE', #11756, 1000.000000000000000 ) ;
#5394=EDGE_CURVE ( 'NONE', #9704, #682, #8317, .T. ) ;
#5397=DIRECTION ( 'NONE',  ( 0.000000000000000000, -1.000000000000000000, 0.000000000000000000 ) ) ;
#5399=DIRECTION ( 'NONE',  ( 0.000000000000000000, 0.000000000000000000, 1.000000000000000000 ) ) ;
#5400=CARTESIAN_POINT ( 'NONE',  ( -59.02799568714584666, 0.000000000000000000, -73.34256232478206528 ) ) ;
#5401=CARTESIAN_POINT ( 'NONE',  ( -64.53565528768383786, 67.29799558322736175, -81.84847958357697451 ) ) ;
#5404=AXIS2_PLACEMENT_3D ( 'NONE', #8470, #11034, #245 ) ;
#5405=DIRECTION ( 'NONE',  ( 0.000000000000000000, -1.000000000000000000, 0.000000000000000000 ) ) ;
#5407=VECTOR ( 'NONE', #3875, 1000.000000000000000 ) ;
#5413=VECTOR ( 'NONE', #788, 1000.000000000000114 ) ;
#5415=FACE_OUTER_BOUND ( 'NONE', #6696, .T. ) ;
#5418=CARTESIAN_POINT ( 'NONE',  ( -69.48563225166269319, 98.17410195967158870, -94.70794860920351255 ) ) ;
#5420=ORIENTED_EDGE ( 'NONE', *, *, #8308, .T. ) ;
#5421=CIRCLE ( 'NONE', #7888, 2.042000000000002036 ) ;
#5422=DIRECTION ( 'NONE',  ( 0.000000000000000000, 0.000000000000000000, -1.000000000000000000 ) ) ;
#5427=CYLINDRICAL_SURFACE ( 'NONE', #14300, 2.000000000000001776 ) ;
#5428=DIRECTION ( 'NONE',  ( 0.000000000000000000, 0.000000000000000000, 1.000000000000000000 ) ) ;
#5429=AXIS2_PLACEMENT_3D ( 'NONE', #11461, #10434, #8041 ) ;
#5432=EDGE_CURVE ( 'NONE', #3491, #13082, #10519, .T. ) ;
#5433=CARTESIAN_POINT ( 'NONE',  ( -50.73238362644099197, 97.99516924618178848, -147.9984795835769944 ) ) ;
#5435=ORIENTED_EDGE ( 'NONE', *, *, #1656, .T. ) ;
#5438=ORIENTED_EDGE ( 'NONE', *, *, #6779, .T. ) ;
#5439=ORIENTED_EDGE ( 'NONE', *, *, #2031, .F. ) ;
#5440=ORIENTED_EDGE ( 'NONE', *, *, #13775, .F. ) ;
#5441=EDGE_LOOP ( 'NONE', ( #4565, #13424, #10751, #918 ) ) ;
#5445=PLANE ( 'NONE',  #13022 ) ;
#5451=DIRECTION ( 'NONE',  ( -0.000000000000000000, -0.000000000000000000, 1.000000000000000000 ) ) ;
#5452=EDGE_CURVE ( 'NONE', #704, #11895, #3729, .T. ) ;
#5453=DIRECTION ( 'NONE',  ( 0.000000000000000000, -1.000000000000000000, 0.000000000000000000 ) ) ;
#5455=CARTESIAN_POINT ( 'NONE',  ( -86.27438362644001302, 82.17411849586700612, -152.4984795835769944 ) ) ;
#5456=EDGE_CURVE ( 'NONE', #5220, #9369, #11307, .T. ) ;
#5457=ORIENTED_EDGE ( 'NONE', *, *, #14630, .T. ) ;
#5460=DIRECTION ( 'NONE',  ( 1.000000000000000000, 0.000000000000000000, 0.000000000000000000 ) ) ;
#5467=DIRECTION ( 'NONE',  ( -1.000000000000000000, 0.000000000000000000, 0.000000000000000000 ) ) ;
#5469=DIRECTION ( 'NONE',  ( 0.000000000000000000, 0.000000000000000000, 1.000000000000000000 ) ) ;
#5470=EDGE_CURVE ( 'NONE', #10234, #12733, #6170, .T. ) ;
#5473=DIRECTION ( 'NONE',  ( 1.000000000000000000, 0.000000000000000000, 0.000000000000000000 ) ) ;
#5475=ORIENTED_EDGE ( 'NONE', *, *, #11979, .F. ) ;
#5480=MANIFOLD_SOLID_BREP ( 'NONE', #9271 ) ;
#5484=CARTESIAN_POINT ( 'NONE',  ( -89.27438362643999881, 65.17411849586700612, -182.2484795835770228 ) ) ;
#5486=CYLINDRICAL_SURFACE ( 'NONE', #4050, 1.250000000000001110 ) ;
#5490=PLANE ( 'NONE',  #3370 ) ;
#5498=CARTESIAN_POINT ( 'NONE',  ( -69.77438362644001302, 82.17411849586700612, -83.44847958357698303 ) ) ;
#5499=AXIS2_PLACEMENT_3D ( 'NONE', #9406, #14144, #3519 ) ;
#5500=CARTESIAN_POINT ( 'NONE',  ( -86.77438362643999881, 65.17411849586700612, -149.9984795835770228 ) ) ;
#5506=AXIS2_PLACEMENT_3D ( 'NONE', #9508, #10844, #7363 ) ;
#5507=FACE_OUTER_BOUND ( 'NONE', #4973, .T. ) ;
#5510=ORIENTED_EDGE ( 'NONE', *, *, #3085, .F. ) ;
#5512=ORIENTED_EDGE ( 'NONE', *, *, #7430, .T. ) ;
#5515=VERTEX_POINT ( 'NONE', #11327 ) ;
#5522=ADVANCED_FACE ( 'NONE', ( #13812 ), #6619, .T. ) ;
#5525=CARTESIAN_POINT ( 'NONE',  ( -52.77438362644100067, 99.17411849586700612, -147.9984795835769944 ) ) ;
#5529=CARTESIAN_POINT ( 'NONE',  ( -54.81638362644000040, 65.17411849586700612, -147.9984795835769944 ) ) ;
#5530=EDGE_LOOP ( 'NONE', ( #13181, #11933, #12901, #8512 ) ) ;
#5533=ORIENTED_EDGE ( 'NONE', *, *, #13334, .T. ) ;
#5536=CONICAL_SURFACE ( 'NONE', #7273, 8.349999999999996092, 0.7853981633974476129 ) ;
#5537=DIRECTION ( 'NONE',  ( -0.9378889346118977066, 0.3469356515732558988, 0.000000000000000000 ) ) ;
#5540=DIRECTION ( 'NONE',  ( 0.000000000000000000, 0.000000000000000000, -1.000000000000000000 ) ) ;
#5541=DIRECTION ( 'NONE',  ( -0.000000000000000000, -0.000000000000000000, 1.000000000000000000 ) ) ;
#5543=ADVANCED_FACE ( 'NONE', ( #12501 ), #5445, .F. ) ;
#5544=CIRCLE ( 'NONE', #3540, 2.500000000000002220 ) ;
#5545=CARTESIAN_POINT ( 'NONE',  ( -85.77438362644001302, 82.17411849586700612, -112.9984795835769944 ) ) ;
#5546=LINE ( 'NONE', #6860, #5413 ) ;
#5549=CIRCLE ( 'NONE', #4057, 1.250000000000001110 ) ;
#5550=ORIENTED_EDGE ( 'NONE', *, *, #1356, .T. ) ;
#5551=DIRECTION ( 'NONE',  ( 0.000000000000000000, 0.000000000000000000, 1.000000000000000000 ) ) ;
#5554=DIRECTION ( 'NONE',  ( 0.000000000000000000, 0.000000000000000000, -1.000000000000000000 ) ) ;
#5555=ORIENTED_EDGE ( 'NONE', *, *, #11521, .T. ) ;
#5556=AXIS2_PLACEMENT_3D ( 'NONE', #11467, #14102, #832 ) ;
#5558=ORIENTED_EDGE ( 'NONE', *, *, #7964, .T. ) ;
#5559=EDGE_CURVE ( 'NONE', #1481, #2078, #6352, .T. ) ;
#5567=AXIS2_PLACEMENT_3D ( 'NONE', #10857, #5197, #14635 ) ;
#5570=CARTESIAN_POINT ( 'NONE',  ( -86.77438362644001302, 65.17411849586700612, -79.59847958357700293 ) ) ;
#5572=ORIENTED_EDGE ( 'NONE', *, *, #1247, .T. ) ;
#5573=CARTESIAN_POINT ( 'NONE',  ( -66.41143315690761995, 66.60412428008086749, -83.44847958357698303 ) ) ;
#5575=ORIENTED_EDGE ( 'NONE', *, *, #5087, .F. ) ;
#5578=EDGE_CURVE ( 'NONE', #4297, #14050, #4195, .T. ) ;
#5580=CARTESIAN_POINT ( 'NONE',  ( -86.77438362643999881, 65.17411849586700612, -145.4984795835769944 ) ) ;
#5581=DIRECTION ( 'NONE',  ( 0.000000000000000000, 0.000000000000000000, -1.000000000000000000 ) ) ;
#5587=ORIENTED_EDGE ( 'NONE', *, *, #6232, .T. ) ;
#5588=CIRCLE ( 'NONE', #13999, 0.2000000000000057288 ) ;
#5589=DIRECTION ( 'NONE',  ( 0.000000000000000000, 0.000000000000000000, 1.000000000000000000 ) ) ;
#5591=ORIENTED_EDGE ( 'NONE', *, *, #11212, .T. ) ;
#5594=VERTEX_POINT ( 'NONE', #12577 ) ;
#5595=ORIENTED_EDGE ( 'NONE', *, *, #10381, .T. ) ;
#5600=CARTESIAN_POINT ( 'NONE',  ( -56.85838362643999488, 65.17411849586700612, -147.9984795835769944 ) ) ;
#5604=DIRECTION ( 'NONE',  ( -0.000000000000000000, 1.000000000000000000, 0.000000000000000000 ) ) ;
#5605=CARTESIAN_POINT ( 'NONE',  ( -69.77438362644001302, 71.67411849586700612, -80.44847958357698303 ) ) ;
#5607=DIRECTION ( 'NONE',  ( 0.8660254037844387076, 0.4999999999999998890, 0.000000000000000000 ) ) ;
#5608=CARTESIAN_POINT ( 'NONE',  ( -96.77438362643999881, 104.6741184958670061, -15.85886927678779834 ) ) ;
#5609=DIRECTION ( 'NONE',  ( -1.000000000000000000, 0.000000000000000000, 0.000000000000000000 ) ) ;
#5612=DIRECTION ( 'NONE',  ( 0.000000000000000000, 0.000000000000000000, -1.000000000000000000 ) ) ;
#5614=ORIENTED_EDGE ( 'NONE', *, *, #2432, .F. ) ;
#5615=CIRCLE ( 'NONE', #13037, 0.2000000000000057288 ) ;
#5616=ORIENTED_EDGE ( 'NONE', *, *, #436, .T. ) ;
#5618=AXIS2_PLACEMENT_3D ( 'NONE', #5183, #2691, #7437 ) ;
#5620=CARTESIAN_POINT ( 'NONE',  ( -86.77438362644100778, 101.5320169952374414, -150.4984795835770228 ) ) ;
#5622=AXIS2_PLACEMENT_3D ( 'NONE', #6434, #11143, #5251 ) ;
#5623=CARTESIAN_POINT ( 'NONE',  ( -69.77438362644001302, 82.17411849586700612, -112.9984795835769944 ) ) ;
#5626=AXIS2_PLACEMENT_3D ( 'NONE', #6008, #8320, #11960 ) ;
#5627=DIRECTION ( 'NONE',  ( -1.000000000000000000, 0.000000000000000000, 0.000000000000000000 ) ) ;
#5631=ORIENTED_EDGE ( 'NONE', *, *, #620, .T. ) ;
#5637=AXIS2_PLACEMENT_3D ( 'NONE', #14685, #11129, #5473 ) ;
#5639=EDGE_CURVE ( 'NONE', #8947, #5361, #4102, .T. ) ;
#5640=AXIS2_PLACEMENT_3D ( 'NONE', #4810, #12955, #217 ) ;
#5642=ORIENTED_EDGE ( 'NONE', *, *, #5394, .F. ) ;
#5645=FACE_OUTER_BOUND ( 'NONE', #5530, .T. ) ;
#5647=AXIS2_PLACEMENT_3D ( 'NONE', #5267, #9050, #7751 ) ;
#5649=CARTESIAN_POINT ( 'NONE',  ( -70.34862606286944242, 98.16638921377227689, -94.68195642959773295 ) ) ;
#5651=CARTESIAN_POINT ( 'NONE',  ( -60.52799568714584666, 103.6741184958669919, -73.34256232478206528 ) ) ;
#5653=ORIENTED_EDGE ( 'NONE', *, *, #13122, .F. ) ;
#5654=EDGE_CURVE ( 'NONE', #7059, #2214, #9502, .T. ) ;
#5660=EDGE_CURVE ( 'NONE', #12429, #13931, #11037, .T. ) ;
#5662=CARTESIAN_POINT ( 'NONE',  ( -61.64938362644000591, 82.17411849586700612, -93.49847958357699440 ) ) ;
#5663=FACE_BOUND ( 'NONE', #10648, .T. ) ;
#5665=CARTESIAN_POINT ( 'NONE',  ( -91.02438362644100778, 99.17411849586700612, -149.9984795835770228 ) ) ;
#5666=EDGE_CURVE ( 'NONE', #13685, #5306, #13878, .T. ) ;
#5668=FACE_OUTER_BOUND ( 'NONE', #6510, .T. ) ;
#5669=CONICAL_SURFACE ( 'NONE', #13588, 7.999999999992790656, 0.7853981634258691003 ) ;
#5671=DIRECTION ( 'NONE',  ( 1.000000000000000000, 0.000000000000000000, 0.000000000000000000 ) ) ;
#5675=EDGE_CURVE ( 'NONE', #12970, #12826, #14980, .T. ) ;
#5679=EDGE_LOOP ( 'NONE', ( #6192, #5025 ) ) ;
#5680=LINE ( 'NONE', #4418, #3579 ) ;
#5682=AXIS2_PLACEMENT_3D ( 'NONE', #5973, #8127, #4640 ) ;
#5685=CARTESIAN_POINT ( 'NONE',  ( -82.52438362643998460, 65.17411849586700612, -145.4984795835769944 ) ) ;
#5686=PLANE ( 'NONE',  #4145 ) ;
#5688=CARTESIAN_POINT ( 'NONE',  ( -69.77438362644001302, 82.17411849586700612, -150.4984795835769944 ) ) ;
#5689=CARTESIAN_POINT ( 'NONE',  ( -69.77438362644001302, 82.17411849586700612, -79.59847958357700293 ) ) ;
#5694=ORIENTED_EDGE ( 'NONE', *, *, #3761, .F. ) ;
#5695=DIRECTION ( 'NONE',  ( 0.000000000000000000, 0.000000000000000000, -1.000000000000000000 ) ) ;
#5697=FACE_OUTER_BOUND ( 'NONE', #5872, .T. ) ;
#5698=LINE ( 'NONE', #6708, #11444 ) ;
#5705=DIRECTION ( 'NONE',  ( 0.000000000000000000, 0.000000000000000000, 1.000000000000000000 ) ) ;
#5706=ORIENTED_EDGE ( 'NONE', *, *, #10178, .T. ) ;
#5708=CARTESIAN_POINT ( 'NONE',  ( -79.02077156573416516, 103.6741184958669777, -73.34256232478206528 ) ) ;
#5711=ORIENTED_EDGE ( 'NONE', *, *, #11382, .T. ) ;
#5715=CARTESIAN_POINT ( 'NONE',  ( -68.41221392010733382, 90.17411849586700612, -58.99847958357691624 ) ) ;
#5716=DIRECTION ( 'NONE',  ( 0.000000000000000000, 0.000000000000000000, 1.000000000000000000 ) ) ;
#5717=EDGE_CURVE ( 'NONE', #1201, #13826, #3624, .T. ) ;
#5719=ORIENTED_EDGE ( 'NONE', *, *, #11321, .T. ) ;
#5720=CYLINDRICAL_SURFACE ( 'NONE', #6143, 2.500000000000002220 ) ;
#5721=CARTESIAN_POINT ( 'NONE',  ( -86.77438362644100778, 99.17411849586700612, -145.4984795835769944 ) ) ;
#5726=EDGE_CURVE ( 'NONE', #6907, #6162, #14246, .T. ) ;
#5728=EDGE_CURVE ( 'NONE', #5594, #13232, #8312, .T. ) ;
#5729=DIRECTION ( 'NONE',  ( 0.000000000000000000, 0.000000000000000000, 1.000000000000000000 ) ) ;
#5732=DIRECTION ( 'NONE',  ( 0.000000000000000000, 0.000000000000000000, 1.000000000000000000 ) ) ;
#5733=CARTESIAN_POINT ( 'NONE',  ( -69.77438362644001302, 82.17411849586700612, -3.496191900462991775 ) ) ;
#5734=CIRCLE ( 'NONE', #3994, 1.500000000000001332 ) ;
#5738=EDGE_CURVE ( 'NONE', #12429, #858, #8057, .T. ) ;
#5739=VERTEX_POINT ( 'NONE', #10987 ) ;
#5741=ORIENTED_EDGE ( 'NONE', *, *, #197, .T. ) ;
#5742=EDGE_CURVE ( 'NONE', #449, #9860, #14544, .T. ) ;
#5745=CIRCLE ( 'NONE', #14871, 4.249999999999996447 ) ;
#5752=CARTESIAN_POINT ( 'NONE',  ( -96.77438362643999881, 65.17411849586700612, -15.85886927678779834 ) ) ;
#5754=EDGE_CURVE ( 'NONE', #897, #1574, #439, .T. ) ;
#5761=ORIENTED_EDGE ( 'NONE', *, *, #6419, .F. ) ;
#5762=ADVANCED_FACE ( 'NONE', ( #9814 ), #9962, .F. ) ;
#5765=CARTESIAN_POINT ( 'NONE',  ( -89.52438362644001302, 65.17411849586700612, -145.4984795835769660 ) ) ;
#5767=EDGE_CURVE ( 'NONE', #14049, #8186, #2754, .T. ) ;
#5769=CARTESIAN_POINT ( 'NONE',  ( -88.81638362644100937, 100.3530677455522238, -147.9984795835769944 ) ) ;
#5770=CARTESIAN_POINT ( 'NONE',  ( -67.13357088347154900, 75.17411849586700612, -44.45439862457403990 ) ) ;
#5774=CARTESIAN_POINT ( 'NONE',  ( -90.85838362644101096, 99.17411849586700612, -147.9984795835769944 ) ) ;
#5775=DIRECTION ( 'NONE',  ( 1.000000000000000000, 0.000000000000000000, 0.000000000000000000 ) ) ;
#5778=CARTESIAN_POINT ( 'NONE',  ( -50.73238362644099197, 99.17411849586700612, -147.9984795835769944 ) ) ;
#5780=CARTESIAN_POINT ( 'NONE',  ( -69.77438362644001302, 82.17411849586700612, -67.69567958357700377 ) ) ;
#5781=ORIENTED_EDGE ( 'NONE', *, *, #7230, .T. ) ;
#5783=ORIENTED_EDGE ( 'NONE', *, *, #4227, .F. ) ;
#5786=VECTOR ( 'NONE', #6462, 1000.000000000000000 ) ;
#5788=DIRECTION ( 'NONE',  ( 0.000000000000000000, 0.000000000000000000, 1.000000000000000000 ) ) ;
#5789=DIRECTION ( 'NONE',  ( 0.000000000000000000, 0.000000000000000000, -1.000000000000000000 ) ) ;
#5790=VECTOR ( 'NONE', #14475, 1000.000000000000000 ) ;
#5791=CARTESIAN_POINT ( 'NONE',  ( -60.52799568714584666, 60.67411849586701322, -73.34256232478206528 ) ) ;
#5792=FACE_OUTER_BOUND ( 'NONE', #795, .T. ) ;
#5793=ORIENTED_EDGE ( 'NONE', *, *, #10067, .T. ) ;
#5794=DIRECTION ( 'NONE',  ( -0.8660254037844387076, -0.4999999999999998890, 0.000000000000000000 ) ) ;
#5795=CIRCLE ( 'NONE', #6303, 2.042000000000002036 ) ;
#5800=CIRCLE ( 'NONE', #9006, 4.500000000000003553 ) ;
#5803=ORIENTED_EDGE ( 'NONE', *, *, #4605, .F. ) ;
#5806=AXIS2_PLACEMENT_3D ( 'NONE', #8164, #9467, #1019 ) ;
#5808=CIRCLE ( 'NONE', #5059, 4.499999999999997335 ) ;
#5810=DIRECTION ( 'NONE',  ( 0.000000000000000000, 0.000000000000000000, 1.000000000000000000 ) ) ;
#5813=DIRECTION ( 'NONE',  ( 0.000000000000000000, -1.000000000000000000, 0.000000000000000000 ) ) ;
#5814=VERTEX_POINT ( 'NONE', #10041 ) ;
#5815=CARTESIAN_POINT ( 'NONE',  ( -86.77438362643999881, 65.17411849586700612, -182.2484795835770228 ) ) ;
#5817=CIRCLE ( 'NONE', #592, 4.499999999999997335 ) ;
#5818=ADVANCED_FACE ( 'NONE', ( #7586 ), #14776, .T. ) ;
#5819=VECTOR ( 'NONE', #9982, 1000.000000000000000 ) ;
#5822=VERTEX_POINT ( 'NONE', #12224 ) ;
#5827=DIRECTION ( 'NONE',  ( -1.000000000000000000, 0.000000000000000000, 0.000000000000000000 ) ) ;
#5828=DIRECTION ( 'NONE',  ( 0.000000000000000000, 0.000000000000000000, -1.000000000000000000 ) ) ;
#5829=DIRECTION ( 'NONE',  ( 1.000000000000000000, 0.000000000000000000, 0.000000000000000000 ) ) ;
#5831=DIRECTION ( 'NONE',  ( 0.000000000000000000, 1.000000000000000000, 0.000000000000000000 ) ) ;
#5833=CARTESIAN_POINT ( 'NONE',  ( -55.47438362644099641, 99.17411849586700612, -145.2984795835770058 ) ) ;
#5842=ORIENTED_EDGE ( 'NONE', *, *, #8100, .T. ) ;
#5845=VECTOR ( 'NONE', #2685, 1000.000000000000114 ) ;
#5846=FACE_OUTER_BOUND ( 'NONE', #7922, .T. ) ;
#5847=ADVANCED_FACE ( 'NONE', ( #6428 ), #5328, .F. ) ;
#5848=CIRCLE ( 'NONE', #3598, 8.124999999999992895 ) ;
#5850=DIRECTION ( 'NONE',  ( -1.000000000000000000, 0.000000000000000000, 0.000000000000000000 ) ) ;
#5852=CARTESIAN_POINT ( 'NONE',  ( -52.77438362644100067, 101.5320169952374414, -147.9984795835769944 ) ) ;
#5854=EDGE_CURVE ( 'NONE', #7225, #11930, #12548, .T. ) ;
#5856=CARTESIAN_POINT ( 'NONE',  ( -52.77438362643999881, 65.17411849586700612, -150.4984795835770228 ) ) ;
#5857=AXIS2_PLACEMENT_3D ( 'NONE', #4319, #15005, #11530 ) ;
#5859=CARTESIAN_POINT ( 'NONE',  ( -66.41143315690761995, 66.60412428008086749, -83.44847958357698303 ) ) ;
#5860=CIRCLE ( 'NONE', #2127, 4.499999999999997335 ) ;
#5865=ORIENTED_EDGE ( 'NONE', *, *, #13775, .T. ) ;
#5870=DIRECTION ( 'NONE',  ( 0.000000000000000000, 0.000000000000000000, -1.000000000000000000 ) ) ;
#5872=EDGE_LOOP ( 'NONE', ( #10853, #14363, #12097, #1126, #13301 ) ) ;
#5877=AXIS2_PLACEMENT_3D ( 'NONE', #10895, #11190, #2737 ) ;
#5880=DIRECTION ( 'NONE',  ( 0.000000000000000000, 0.000000000000000000, -1.000000000000000000 ) ) ;
#5887=VECTOR ( 'NONE', #2033, 1000.000000000000000 ) ;
#5888=EDGE_LOOP ( 'NONE', ( #2681, #15065, #6016, #12637, #5337, #12217, #13357, #12112, #4972, #952, #11410 ) ) ;
#5889=CARTESIAN_POINT ( 'NONE',  ( -82.27438362643999881, 99.17411849586700612, -86.49847958357699440 ) ) ;
#5895=DIRECTION ( 'NONE',  ( 0.000000000000000000, 0.000000000000000000, -1.000000000000000000 ) ) ;
#5896=CIRCLE ( 'NONE', #2652, 8.050000000000000711 ) ;
#5901=DIRECTION ( 'NONE',  ( -1.000000000000000000, 0.000000000000000000, 0.000000000000000000 ) ) ;
#5903=ORIENTED_EDGE ( 'NONE', *, *, #4124, .F. ) ;
#5904=CARTESIAN_POINT ( 'NONE',  ( -77.89938362643999881, 82.17411849586700612, -150.4984795835769944 ) ) ;
#5906=VECTOR ( 'NONE', #7716, 1000.000000000000000 ) ;
#5908=ORIENTED_EDGE ( 'NONE', *, *, #2407, .T. ) ;
#5909=ORIENTED_EDGE ( 'NONE', *, *, #8292, .F. ) ;
#5910=ORIENTED_EDGE ( 'NONE', *, *, #11407, .T. ) ;
#5912=DIRECTION ( 'NONE',  ( 1.000000000000000000, 0.000000000000000000, 0.000000000000000000 ) ) ;
#5916=CYLINDRICAL_SURFACE ( 'NONE', #3141, 5.500000000000005329 ) ;
#5918=DIRECTION ( 'NONE',  ( 0.000000000000000000, 0.000000000000000000, -1.000000000000000000 ) ) ;
#5920=EDGE_CURVE ( 'NONE', #10374, #9201, #10247, .T. ) ;
#5922=DIRECTION ( 'NONE',  ( 1.000000000000000000, 0.000000000000000000, 0.000000000000000000 ) ) ;
#5923=ORIENTED_EDGE ( 'NONE', *, *, #8207, .T. ) ;
#5924=CARTESIAN_POINT ( 'NONE',  ( -69.77438362644001302, 94.57411849586699759, -93.49847958357699440 ) ) ;
#5927=ORIENTED_EDGE ( 'NONE', *, *, #6624, .T. ) ;
#5931=DIRECTION ( 'NONE',  ( 0.000000000000000000, 0.000000000000000000, -1.000000000000000000 ) ) ;
#5933=CYLINDRICAL_SURFACE ( 'NONE', #15151, 3.000000000000002665 ) ;
#5934=ADVANCED_FACE ( 'NONE', ( #6801 ), #4386, .F. ) ;
#5938=CYLINDRICAL_SURFACE ( 'NONE', #9785, 8.124999999999992895 ) ;
#5942=VECTOR ( 'NONE', #3628, 1000.000000000000114 ) ;
#5944=CARTESIAN_POINT ( 'NONE',  ( -69.77438362644001302, 81.46011849586699327, -83.44847958357698303 ) ) ;
#5945=ORIENTED_EDGE ( 'NONE', *, *, #8476, .T. ) ;
#5946=ORIENTED_EDGE ( 'NONE', *, *, #5958, .F. ) ;
#5947=CARTESIAN_POINT ( 'NONE',  ( -69.77438362644100778, 92.17411849586700612, -67.49847958357700861 ) ) ;
#5950=VERTEX_POINT ( 'NONE', #883 ) ;
#5951=EDGE_CURVE ( 'NONE', #2123, #3176, #14261, .T. ) ;
#5953=AXIS2_PLACEMENT_3D ( 'NONE', #2758, #14549, #4002 ) ;
#5955=EDGE_CURVE ( 'NONE', #9472, #16, #14016, .T. ) ;
#5956=CARTESIAN_POINT ( 'NONE',  ( -64.53565528768383786, 67.29799558322736175, -81.84847958357697451 ) ) ;
#5957=DIRECTION ( 'NONE',  ( -0.000000000000000000, 0.000000000000000000, -1.000000000000000000 ) ) ;
#5958=EDGE_CURVE ( 'NONE', #9229, #9845, #13920, .T. ) ;
#5959=CARTESIAN_POINT ( 'NONE',  ( -50.73238362644099197, 100.3530677455522238, -150.4984795835770228 ) ) ;
#5968=DIRECTION ( 'NONE',  ( -0.4999999999999998890, 0.8660254037844387076, 0.000000000000000000 ) ) ;
#5969=ADVANCED_FACE ( 'NONE', ( #5645 ), #10185, .F. ) ;
#5971=CARTESIAN_POINT ( 'NONE',  ( -84.73238362643999722, 66.35306774555222376, -147.9984795835769944 ) ) ;
#5972=DIRECTION ( 'NONE',  ( -1.000000000000000000, 0.000000000000000000, 0.000000000000000000 ) ) ;
#5973=CARTESIAN_POINT ( 'NONE',  ( -90.85838362644101096, 99.17411849586700612, -147.9984795835769944 ) ) ;
#5974=LINE ( 'NONE', #3629, #4040 ) ;
#5975=CARTESIAN_POINT ( 'NONE',  ( -73.80978675135780520, 64.78624853950366003, -81.84847958357697451 ) ) ;
#5976=CYLINDRICAL_SURFACE ( 'NONE', #2522, 17.00000000000000000 ) ;
#5978=DIRECTION ( 'NONE',  ( -1.000000000000000000, 0.000000000000000000, 0.000000000000000000 ) ) ;
#5983=EDGE_LOOP ( 'NONE', ( #2232, #13467, #5204 ) ) ;
#5984=VERTEX_POINT ( 'NONE', #3291 ) ;
#5986=CARTESIAN_POINT ( 'NONE',  ( -69.77438362644001302, 81.46011849586699327, -83.44847958357698303 ) ) ;
#5988=LINE ( 'NONE', #7667, #6770 ) ;
#5989=DIRECTION ( 'NONE',  ( -0.8660254037844387076, -0.4999999999999998890, 0.000000000000000000 ) ) ;
#5991=PLANE ( 'NONE',  #6181 ) ;
#5992=CYLINDRICAL_SURFACE ( 'NONE', #4256, 2.750000000000002665 ) ;
#5995=DIRECTION ( 'NONE',  ( 0.000000000000000000, 0.000000000000000000, -1.000000000000000000 ) ) ;
#5998=ORIENTED_EDGE ( 'NONE', *, *, #2198, .T. ) ;
#5999=CIRCLE ( 'NONE', #11179, 17.00000000000000000 ) ;
#6000=ORIENTED_EDGE ( 'NONE', *, *, #249, .T. ) ;
#6004=ADVANCED_FACE ( 'NONE', ( #13697, #7807 ), #9033, .T. ) ;
#6006=LINE ( 'NONE', #14286, #4763 ) ;
#6008=CARTESIAN_POINT ( 'NONE',  ( -62.27438362644000591, 74.17411849586699191, -58.99847958357700151 ) ) ;
#6010=CARTESIAN_POINT ( 'NONE',  ( -96.77438362643999881, 104.6741184958670061, -79.59847958357700293 ) ) ;
#6011=DIRECTION ( 'NONE',  ( -1.000000000000000000, 0.000000000000000000, 0.000000000000000000 ) ) ;
#6013=CARTESIAN_POINT ( 'NONE',  ( -59.02799568714584666, 103.6741184958669919, -79.59847958357700293 ) ) ;
#6016=ORIENTED_EDGE ( 'NONE', *, *, #8119, .F. ) ;
#6020=ORIENTED_EDGE ( 'NONE', *, *, #10917, .T. ) ;
#6021=CARTESIAN_POINT ( 'NONE',  ( -57.27438362644000591, 99.17411849586700612, -145.4984795835769660 ) ) ;
#6023=EDGE_CURVE ( 'NONE', #14332, #14841, #5860, .T. ) ;
#6024=AXIS2_PLACEMENT_3D ( 'NONE', #7490, #1883, #5162 ) ;
#6028=CARTESIAN_POINT ( 'NONE',  ( -52.77438362643999881, 65.17411849586700612, -145.2984795835770058 ) ) ;
#6029=CIRCLE ( 'NONE', #5268, 1.250000000000001110 ) ;
#6030=LINE ( 'NONE', #1348, #390 ) ;
#6034=CARTESIAN_POINT ( 'NONE',  ( -48.27438362644000591, 99.17411849586700612, -79.59847958357700293 ) ) ;
#6035=ORIENTED_EDGE ( 'NONE', *, *, #3814, .F. ) ;
#6036=FACE_OUTER_BOUND ( 'NONE', #282, .T. ) ;
#6038=AXIS2_PLACEMENT_3D ( 'NONE', #7397, #9771, #8393 ) ;
#6040=EDGE_CURVE ( 'NONE', #9472, #2388, #8413, .T. ) ;
#6041=ORIENTED_EDGE ( 'NONE', *, *, #14470, .T. ) ;
#6043=ORIENTED_EDGE ( 'NONE', *, *, #10348, .T. ) ;
#6044=EDGE_CURVE ( 'NONE', #13867, #1293, #9796, .T. ) ;
#6046=EDGE_CURVE ( 'NONE', #8280, #14101, #5615, .T. ) ;
#6049=CIRCLE ( 'NONE', #3063, 2.000000000000001776 ) ;
#6050=ADVANCED_FACE ( 'NONE', ( #6109 ), #14374, .F. ) ;
#6053=AXIS2_PLACEMENT_3D ( 'NONE', #9150, #13665, #5381 ) ;
#6055=DIRECTION ( 'NONE',  ( -1.000000000000000000, 0.000000000000000000, 0.000000000000000000 ) ) ;
#6056=EDGE_CURVE ( 'NONE', #957, #10550, #6030, .T. ) ;
#6058=DIRECTION ( 'NONE',  ( 0.000000000000000000, 0.000000000000000000, -1.000000000000000000 ) ) ;
#6060=ORIENTED_EDGE ( 'NONE', *, *, #5675, .T. ) ;
#6062=AXIS2_PLACEMENT_3D ( 'NONE', #401, #3734, #14509 ) ;
#6063=CIRCLE ( 'NONE', #7539, 2.699999999999993960 ) ;
#6064=ORIENTED_EDGE ( 'NONE', *, *, #3814, .T. ) ;
#6067=DIRECTION ( 'NONE',  ( 0.000000000000000000, -1.000000000000000000, 0.000000000000000000 ) ) ;
#6068=FACE_OUTER_BOUND ( 'NONE', #6905, .T. ) ;
#6069=CARTESIAN_POINT ( 'NONE',  ( -54.81638362644100226, 97.99516924618178848, -147.9984795835769944 ) ) ;
#6073=AXIS2_PLACEMENT_3D ( 'NONE', #1389, #11862, #12954 ) ;
#6076=DIRECTION ( 'NONE',  ( -1.000000000000000000, 0.000000000000000000, 0.000000000000000000 ) ) ;
#6078=DIRECTION ( 'NONE',  ( -1.000000000000000000, 0.000000000000000000, 0.000000000000000000 ) ) ;
#6079=ORIENTED_EDGE ( 'NONE', *, *, #2994, .F. ) ;
#6084=VECTOR ( 'NONE', #3879, 1000.000000000000000 ) ;
#6086=CIRCLE ( 'NONE', #14227, 4.500000000000003553 ) ;
#6088=DIRECTION ( 'NONE',  ( 1.287488025362404182E-15, 1.000000000000000000, 0.000000000000000000 ) ) ;
#6092=CARTESIAN_POINT ( 'NONE',  ( -71.44964421664191434, 89.17411849586702033, -44.18949531478440917 ) ) ;
#6098=EDGE_CURVE ( 'NONE', #632, #11758, #10820, .T. ) ;
#6099=ORIENTED_EDGE ( 'NONE', *, *, #6968, .F. ) ;
#6101=ORIENTED_EDGE ( 'NONE', *, *, #11303, .T. ) ;
#6102=CIRCLE ( 'NONE', #3107, 1.500000000000001332 ) ;
#6104=DIRECTION ( 'NONE',  ( 1.000000000000000000, 0.000000000000000000, 0.000000000000000000 ) ) ;
#6107=CIRCLE ( 'NONE', #5095, 0.1999999999999987899 ) ;
#6108=LINE ( 'NONE', #9639, #15137 ) ;
#6109=FACE_OUTER_BOUND ( 'NONE', #4921, .T. ) ;
#6115=ORIENTED_EDGE ( 'NONE', *, *, #224, .F. ) ;
#6118=DIRECTION ( 'NONE',  ( 0.000000000000000000, 0.000000000000000000, 1.000000000000000000 ) ) ;
#6120=ORIENTED_EDGE ( 'NONE', *, *, #10634, .T. ) ;
#6122=SURFACE_SIDE_STYLE ('',( #7269 ) ) ;
#6128=EDGE_CURVE ( 'NONE', #6732, #14103, #1117, .T. ) ;
#6129=LINE ( 'NONE', #7510, #6815 ) ;
#6130=AXIS2_PLACEMENT_3D ( 'NONE', #547, #11105, #8775 ) ;
#6131=CARTESIAN_POINT ( 'NONE',  ( -65.90140028023257912, 89.17411849586700612, -44.99847958359791988 ) ) ;
#6132=DIRECTION ( 'NONE',  ( 0.000000000000000000, 0.000000000000000000, -1.000000000000000000 ) ) ;
#6134=CARTESIAN_POINT ( 'NONE',  ( -86.77438362644100778, 101.5320169952374414, -147.9984795835769944 ) ) ;
#6135=CARTESIAN_POINT ( 'NONE',  ( -69.77438362644001302, 82.17411849586700612, -83.44847958357698303 ) ) ;
#6136=EDGE_CURVE ( 'NONE', #14050, #4013, #14992, .T. ) ;
#6138=DIRECTION ( 'NONE',  ( 0.000000000000000000, 0.000000000000000000, -1.000000000000000000 ) ) ;
#6139=VERTEX_POINT ( 'NONE', #13085 ) ;
#6140=FACE_OUTER_BOUND ( 'NONE', #8054, .T. ) ;
#6143=AXIS2_PLACEMENT_3D ( 'NONE', #7191, #8111, #9412 ) ;
#6144=EDGE_LOOP ( 'NONE', ( #5555, #6680, #6602, #15295 ) ) ;
#6146=CIRCLE ( 'NONE', #6638, 16.06499999999999773 ) ;
#6148=ADVANCED_FACE ( 'NONE', ( #8179, #8343 ), #99, .T. ) ;
#6149=LINE ( 'NONE', #4961, #8025 ) ;
#6151=EDGE_CURVE ( 'NONE', #449, #1588, #4697, .T. ) ;
#6152=PLANE ( 'NONE',  #5567 ) ;
#6154=FACE_BOUND ( 'NONE', #5357, .T. ) ;
#6155=AXIS2_PLACEMENT_3D ( 'NONE', #5780, #3508, #11740 ) ;
#6156=DIRECTION ( 'NONE',  ( 0.5000000000000003331, 0.8660254037844384856, 0.000000000000000000 ) ) ;
#6160=VECTOR ( 'NONE', #14789, 1000.000000000000000 ) ;
#6161=EDGE_CURVE ( 'NONE', #12055, #11016, #10049, .T. ) ;
#6162=VERTEX_POINT ( 'NONE', #5081 ) ;
#6163=ORIENTED_EDGE ( 'NONE', *, *, #4111, .F. ) ;
#6164=ORIENTED_EDGE ( 'NONE', *, *, #7082, .F. ) ;
#6165=VERTEX_POINT ( 'NONE', #13383 ) ;
#6169=AXIS2_PLACEMENT_3D ( 'NONE', #12211, #14899, #12294 ) ;
#6170=LINE ( 'NONE', #4911, #14732 ) ;
#6173=DIRECTION ( 'NONE',  ( 0.000000000000000000, 0.000000000000000000, -1.000000000000000000 ) ) ;
#6174=CYLINDRICAL_SURFACE ( 'NONE', #2166, 4.500000000000003553 ) ;
#6175=DIRECTION ( 'NONE',  ( 0.000000000000000000, 0.000000000000000000, -1.000000000000000000 ) ) ;
#6176=DIRECTION ( 'NONE',  ( 0.000000000000000000, 0.000000000000000000, -1.000000000000000000 ) ) ;
#6177=FACE_OUTER_BOUND ( 'NONE', #6922, .T. ) ;
#6180=ORIENTED_EDGE ( 'NONE', *, *, #9766, .F. ) ;
#6181=AXIS2_PLACEMENT_3D ( 'NONE', #8523, #13268, #10538 ) ;
#6182=ORIENTED_EDGE ( 'NONE', *, *, #4046, .F. ) ;
#6186=PLANE ( 'NONE',  #13055 ) ;
#6189=CIRCLE ( 'NONE', #5186, 2.042000000000002036 ) ;
#6191=CARTESIAN_POINT ( 'NONE',  ( -50.27438362643999881, 65.17411849586700612, -79.59847958357700293 ) ) ;
#6192=ORIENTED_EDGE ( 'NONE', *, *, #12068, .T. ) ;
#6195=EDGE_LOOP ( 'NONE', ( #12592, #9745 ) ) ;
#6196=AXIS2_PLACEMENT_3D ( 'NONE', #964, #12461, #1977 ) ;
#6197=FILL_AREA_STYLE_COLOUR ( '', #12278 ) ;
#6199=EDGE_LOOP ( 'NONE', ( #14419, #5510, #6824, #13769 ) ) ;
#6200=ADVANCED_FACE ( 'NONE', ( #9716 ), #6259, .F. ) ;
#6201=DIRECTION ( 'NONE',  ( 0.000000000000000000, 0.000000000000000000, -1.000000000000000000 ) ) ;
#6202=EDGE_CURVE ( 'NONE', #8186, #12412, #7347, .T. ) ;
#6210=FACE_OUTER_BOUND ( 'NONE', #2024, .T. ) ;
#6212=DIRECTION ( 'NONE',  ( 0.000000000000000000, 0.000000000000000000, 1.000000000000000000 ) ) ;
#6215=ORIENTED_EDGE ( 'NONE', *, *, #8859, .T. ) ;
#6218=CARTESIAN_POINT ( 'NONE',  ( -60.52799568714584666, 103.6741184958669919, -79.59847958357700293 ) ) ;
#6221=DIRECTION ( 'NONE',  ( 0.000000000000000000, 0.000000000000000000, 1.000000000000000000 ) ) ;
#6224=CARTESIAN_POINT ( 'NONE',  ( -87.79538362643998539, 63.40569462133918677, -147.9984795835769944 ) ) ;
#6231=VERTEX_POINT ( 'NONE', #8792 ) ;
#6232=EDGE_CURVE ( 'NONE', #5168, #557, #6412, .T. ) ;
#6237=( LENGTH_UNIT ( ) NAMED_UNIT ( * ) SI_UNIT ( .MILLI., .METRE. ) );
#6241=DIRECTION ( 'NONE',  ( -0.7071067811865474617, 8.659560562354921765E-17, 0.7071067811865474617 ) ) ;
#6244=CARTESIAN_POINT ( 'NONE',  ( -48.27438362644000591, 65.17411849586700612, -86.49847958357699440 ) ) ;
#6248=DIRECTION ( 'NONE',  ( 0.8660254037844387076, 0.4999999999999998890, 0.000000000000000000 ) ) ;
#6250=CIRCLE ( 'NONE', #14636, 1.500000000000001332 ) ;
#6251=ORIENTED_EDGE ( 'NONE', *, *, #3947, .F. ) ;
#6254=DIRECTION ( 'NONE',  ( -1.460279444460352888E-17, 0.7071067811865485719, -0.7071067811865465735 ) ) ;
#6257=FACE_OUTER_BOUND ( 'NONE', #8167, .T. ) ;
#6259=CYLINDRICAL_SURFACE ( 'NONE', #6614, 9.999999999999994671 ) ;
#6261=CARTESIAN_POINT ( 'NONE',  ( -54.81638362644100226, 99.17411849586700612, -147.9984795835769944 ) ) ;
#6262=DIRECTION ( 'NONE',  ( 0.8660254037844383745, -0.5000000000000003331, 0.000000000000000000 ) ) ;
#6263=DIRECTION ( 'NONE',  ( 0.000000000000000000, 0.000000000000000000, 1.000000000000000000 ) ) ;
#6265=AXIS2_PLACEMENT_3D ( 'NONE', #11792, #5918, #3565 ) ;
#6266=ORIENTED_EDGE ( 'NONE', *, *, #14733, .F. ) ;
#6267=CIRCLE ( 'NONE', #2034, 3.000000000000002665 ) ;
#6268=DIRECTION ( 'NONE',  ( 0.000000000000000000, 0.000000000000000000, 1.000000000000000000 ) ) ;
#6275=FACE_OUTER_BOUND ( 'NONE', #9977, .T. ) ;
#6276=CARTESIAN_POINT ( 'NONE',  ( -77.52077156573416516, 164.3482369917340122, -73.34256232478206528 ) ) ;
#6285=EDGE_CURVE ( 'NONE', #1774, #8449, #3616, .T. ) ;
#6291=ORIENTED_EDGE ( 'NONE', *, *, #232, .F. ) ;
#6293=VECTOR ( 'NONE', #1720, 1000.000000000000000 ) ;
#6296=AXIS2_PLACEMENT_3D ( 'NONE', #13777, #1021, #3356 ) ;
#6303=AXIS2_PLACEMENT_3D ( 'NONE', #5329, #10042, #3561 ) ;
#6304=EDGE_CURVE ( 'NONE', #7017, #384, #4874, .T. ) ;
#6305=ORIENTED_EDGE ( 'NONE', *, *, #2486, .F. ) ;
#6309=VECTOR ( 'NONE', #7703, 1000.000000000000000 ) ;
#6310=CARTESIAN_POINT ( 'NONE',  ( -48.27438362644000591, 65.17411849586700612, -86.49847958357699440 ) ) ;
#6313=CIRCLE ( 'NONE', #5806, 2.750000000000002665 ) ;
#6315=AXIS2_PLACEMENT_3D ( 'NONE', #11233, #5428, #826 ) ;
#6317=DIRECTION ( 'NONE',  ( 1.000000000000000000, 0.000000000000000000, 0.000000000000000000 ) ) ;
#6319=PLANE ( 'NONE',  #10266 ) ;
#6322=CARTESIAN_POINT ( 'NONE',  ( -75.01311196519617397, 67.29799558322736175, -81.84847958357698872 ) ) ;
#6323=VERTEX_POINT ( 'NONE', #865 ) ;
#6324=DIRECTION ( 'NONE',  ( 0.000000000000000000, 1.000000000000000000, 0.000000000000000000 ) ) ;
#6326=VERTEX_POINT ( 'NONE', #11276 ) ;
#6327=ORIENTED_EDGE ( 'NONE', *, *, #10839, .T. ) ;
#6334=EDGE_CURVE ( 'NONE', #14279, #2123, #786, .T. ) ;
#6335=FACE_BOUND ( 'NONE', #5679, .T. ) ;
#6336=DIRECTION ( 'NONE',  ( 1.000000000000000000, 0.000000000000000000, 0.000000000000000000 ) ) ;
#6339=DIRECTION ( 'NONE',  ( 1.000000000000000000, 0.000000000000000000, 0.000000000000000000 ) ) ;
#6340=ADVANCED_FACE ( 'NONE', ( #12440 ), #3271, .F. ) ;
#6341=DIRECTION ( 'NONE',  ( -1.000000000000000000, 0.000000000000000000, 0.000000000000000000 ) ) ;
#6342=EDGE_LOOP ( 'NONE', ( #9385, #12705, #11641, #13947 ) ) ;
#6346=EDGE_CURVE ( 'NONE', #12791, #11451, #9560, .T. ) ;
#6349=LINE ( 'NONE', #6421, #4859 ) ;
#6352=CIRCLE ( 'NONE', #11529, 2.750000000000002665 ) ;
#6353=AXIS2_PLACEMENT_3D ( 'NONE', #8361, #9195, #11619 ) ;
#6354=DIRECTION ( 'NONE',  ( 0.000000000000000000, 0.000000000000000000, 1.000000000000000000 ) ) ;
#6356=DIRECTION ( 'NONE',  ( 0.000000000000000000, 0.000000000000000000, -1.000000000000000000 ) ) ;
#6357=LINE ( 'NONE', #9820, #14591 ) ;
#6358=CARTESIAN_POINT ( 'NONE',  ( -88.81638362644000040, 66.35306774555222376, -147.9984795835769944 ) ) ;
#6359=FACE_OUTER_BOUND ( 'NONE', #3886, .T. ) ;
#6360=AXIS2_PLACEMENT_3D ( 'NONE', #12049, #14434, #7402 ) ;
#6362=VECTOR ( 'NONE', #8254, 1000.000000000000000 ) ;
#6367=ORIENTED_EDGE ( 'NONE', *, *, #14970, .F. ) ;
#6368=CONICAL_SURFACE ( 'NONE', #13305, 3.749999999999996447, 0.7853981633974476129 ) ;
#6369=DIRECTION ( 'NONE',  ( -1.000000000000000000, 0.000000000000000000, 0.000000000000000000 ) ) ;
#6371=CIRCLE ( 'NONE', #7351, 2.042000000000002036 ) ;
#6373=CARTESIAN_POINT ( 'NONE',  ( -90.85838362644101096, 99.17411849586700612, -147.9984795835769944 ) ) ;
#6377=ORIENTED_EDGE ( 'NONE', *, *, #2848, .F. ) ;
#6380=AXIS2_PLACEMENT_3D ( 'NONE', #3644, #3406, #13117 ) ;
#6381=ORIENTED_EDGE ( 'NONE', *, *, #2887, .F. ) ;
#6382=ORIENTED_EDGE ( 'NONE', *, *, #6592, .F. ) ;
#6383=ORIENTED_EDGE ( 'NONE', *, *, #14970, .T. ) ;
#6385=DIRECTION ( 'NONE',  ( -1.000000000000000000, 0.000000000000000000, 0.000000000000000000 ) ) ;
#6386=ADVANCED_FACE ( 'NONE', ( #10398 ), #10098, .F. ) ;
#6391=CARTESIAN_POINT ( 'NONE',  ( -61.72438362644000165, 82.17411849586700612, -85.04847958357699156 ) ) ;
#6392=ADVANCED_FACE ( 'NONE', ( #13901 ), #4368, .F. ) ;
#6394=VECTOR ( 'NONE', #13792, 1000.000000000000114 ) ;
#6395=DIRECTION ( 'NONE',  ( 0.000000000000000000, 0.000000000000000000, 1.000000000000000000 ) ) ;
#6398=LINE ( 'NONE', #14816, #1403 ) ;
#6400=ORIENTED_EDGE ( 'NONE', *, *, #136, .F. ) ;
#6402=ORIENTED_EDGE ( 'NONE', *, *, #8077, .T. ) ;
#6403=VERTEX_POINT ( 'NONE', #5545 ) ;
#6404=ORIENTED_EDGE ( 'NONE', *, *, #13896, .F. ) ;
#6406=CIRCLE ( 'NONE', #15037, 4.250000000000003553 ) ;
#6408=EDGE_CURVE ( 'NONE', #12872, #7767, #13554, .T. ) ;
#6411=CARTESIAN_POINT ( 'NONE',  ( -69.77438362644001302, 82.17411849586700612, -80.44847958357698303 ) ) ;
#6412=LINE ( 'NONE', #12137, #10549 ) ;
#6413=DIRECTION ( 'NONE',  ( 0.000000000000000000, 0.000000000000000000, -1.000000000000000000 ) ) ;
#6418=EDGE_CURVE ( 'NONE', #9995, #3958, #12062, .T. ) ;
#6419=EDGE_CURVE ( 'NONE', #13943, #5822, #5382, .T. ) ;
#6420=ORIENTED_EDGE ( 'NONE', *, *, #14794, .T. ) ;
#6421=CARTESIAN_POINT ( 'NONE',  ( -56.52438362644099357, 99.17411849586700612, -150.4984795835770228 ) ) ;
#6423=EDGE_LOOP ( 'NONE', ( #3709, #13982, #10551, #1256 ) ) ;
#6424=EDGE_CURVE ( 'NONE', #486, #14010, #12522, .T. ) ;
#6426=CYLINDRICAL_SURFACE ( 'NONE', #2002, 2.750000000000002665 ) ;
#6427=EDGE_CURVE ( 'NONE', #558, #14943, #1884, .T. ) ;
#6428=FACE_OUTER_BOUND ( 'NONE', #14027, .T. ) ;
#6429=EDGE_CURVE ( 'NONE', #9368, #9847, #14276, .T. ) ;
#6430=DIRECTION ( 'NONE',  ( 0.000000000000000000, 0.000000000000000000, 1.000000000000000000 ) ) ;
#6432=CARTESIAN_POINT ( 'NONE',  ( -86.77438362643999881, 65.17411849586700612, -147.9984795835769944 ) ) ;
#6434=CARTESIAN_POINT ( 'NONE',  ( -69.77438362644001302, 82.17411849586700612, -43.99847958362880007 ) ) ;
#6435=DIRECTION ( 'NONE',  ( -1.000000000000000000, 0.000000000000000000, 0.000000000000000000 ) ) ;
#6437=EDGE_CURVE ( 'NONE', #13375, #15273, #156, .T. ) ;
#6440=ORIENTED_EDGE ( 'NONE', *, *, #3757, .T. ) ;
#6443=ORIENTED_EDGE ( 'NONE', *, *, #9530, .T. ) ;
#6445=DIRECTION ( 'NONE',  ( 0.000000000000000000, 0.000000000000000000, 1.000000000000000000 ) ) ;
#6447=DIRECTION ( 'NONE',  ( 0.000000000000000000, 0.000000000000000000, 1.000000000000000000 ) ) ;
#6451=CARTESIAN_POINT ( 'NONE',  ( -86.77438362644100778, 99.17411849586700612, -147.9984795835769944 ) ) ;
#6452=ORIENTED_EDGE ( 'NONE', *, *, #13628, .F. ) ;
#6455=ORIENTED_EDGE ( 'NONE', *, *, #615, .T. ) ;
#6457=ORIENTED_EDGE ( 'NONE', *, *, #7891, .T. ) ;
#6462=DIRECTION ( 'NONE',  ( 0.000000000000000000, 0.000000000000000000, -1.000000000000000000 ) ) ;
#6463=CARTESIAN_POINT ( 'NONE',  ( -52.77438362643999881, 65.17411849586700612, -182.2484795835770228 ) ) ;
#6468=DIRECTION ( 'NONE',  ( 1.000000000000000000, 0.000000000000000000, 0.000000000000000000 ) ) ;
#6474=PLANE ( 'NONE',  #2022 ) ;
#6475=EDGE_CURVE ( 'NONE', #13765, #1201, #9015, .T. ) ;
#6476=DIRECTION ( 'NONE',  ( 0.000000000000000000, 0.000000000000000000, -1.000000000000000000 ) ) ;
#6478=DIRECTION ( 'NONE',  ( 0.000000000000000000, -0.000000000000000000, 1.000000000000000000 ) ) ;
#6479=DIRECTION ( 'NONE',  ( 0.000000000000000000, 1.000000000000000000, 0.000000000000000000 ) ) ;
#6480=CARTESIAN_POINT ( 'NONE',  ( -75.01311196519617397, 67.29799558322736175, -83.44847958357698303 ) ) ;
#6482=VECTOR ( 'NONE', #2704, 1000.000000000000000 ) ;
#6485=DIRECTION ( 'NONE',  ( 1.000000000000000000, 0.000000000000000000, 0.000000000000000000 ) ) ;
#6488=ADVANCED_FACE ( 'NONE', ( #4594 ), #7165, .F. ) ;
#6489=AXIS2_PLACEMENT_3D ( 'NONE', #11136, #2920, #1743 ) ;
#6491=EDGE_LOOP ( 'NONE', ( #5088, #8115, #11405, #13410 ) ) ;
#6492=AXIS2_PLACEMENT_3D ( 'NONE', #11043, #3907, #4211 ) ;
#6493=CARTESIAN_POINT ( 'NONE',  ( -84.27438362643998460, 65.17411849586700612, -79.59847958357700293 ) ) ;
#6495=CARTESIAN_POINT ( 'NONE',  ( -86.77438362644001302, 59.67411849586700612, -152.4984795835769944 ) ) ;
#6496=AXIS2_PLACEMENT_3D ( 'NONE', #4930, #10819, #10968 ) ;
#6498=DIRECTION ( 'NONE',  ( -1.000000000000000000, 0.000000000000000000, 0.000000000000000000 ) ) ;
#6500=DIRECTION ( 'NONE',  ( 0.000000000000000000, 0.000000000000000000, 1.000000000000000000 ) ) ;
#6502=CARTESIAN_POINT ( 'NONE',  ( -50.02438362644000591, 65.17411849586700612, -145.4984795835769944 ) ) ;
#6504=VECTOR ( 'NONE', #11239, 1000.000000000000114 ) ;
#6507=DIRECTION ( 'NONE',  ( 1.287488025362404182E-15, 1.000000000000000000, 0.000000000000000000 ) ) ;
#6510=EDGE_LOOP ( 'NONE', ( #7462, #3224, #3193, #9184 ) ) ;
#6512=LINE ( 'NONE', #13572, #10675 ) ;
#6515=VECTOR ( 'NONE', #10558, 1000.000000000000000 ) ;
#6517=CYLINDRICAL_SURFACE ( 'NONE', #4180, 4.500000000000003553 ) ;
#6518=LINE ( 'NONE', #10205, #3282 ) ;
#6521=CARTESIAN_POINT ( 'NONE',  ( -54.81638362644100226, 97.99516924618178848, -147.9984795835769944 ) ) ;
#6525=ORIENTED_EDGE ( 'NONE', *, *, #9766, .T. ) ;
#6526=EDGE_CURVE ( 'NONE', #7439, #1421, #14525, .T. ) ;
#6530=EDGE_LOOP ( 'NONE', ( #386, #9749, #7691, #750 ) ) ;
#6531=CIRCLE ( 'NONE', #4532, 3.000000000000002665 ) ;
#6532=EDGE_LOOP ( 'NONE', ( #13749, #3169 ) ) ;
#6533=DIRECTION ( 'NONE',  ( 1.000000000000000000, 0.000000000000000000, 0.000000000000000000 ) ) ;
#6535=AXIS2_PLACEMENT_3D ( 'NONE', #3072, #10044, #12318 ) ;
#6539=DIRECTION ( 'NONE',  ( 0.000000000000000000, 0.000000000000000000, -1.000000000000000000 ) ) ;
#6540=CARTESIAN_POINT ( 'NONE',  ( -86.77438362644100778, 99.17411849586700612, -145.4984795835769944 ) ) ;
#6542=DIRECTION ( 'NONE',  ( 0.4999999999999998890, -0.8660254037844387076, 0.000000000000000000 ) ) ;
#6543=CARTESIAN_POINT ( 'NONE',  ( -69.77438362644001302, 82.17411849586700612, -43.99847958357699440 ) ) ;
#6548=ORIENTED_EDGE ( 'NONE', *, *, #689, .T. ) ;
#6549=VECTOR ( 'NONE', #2781, 1000.000000000000000 ) ;
#6550=VERTEX_POINT ( 'NONE', #11883 ) ;
#6552=UNCERTAINTY_MEASURE_WITH_UNIT (LENGTH_MEASURE( 1.000000000000000082E-05 ), #10749, 'distance_accuracy_value', 'NONE');
#6553=CARTESIAN_POINT ( 'NONE',  ( -96.77438362643999881, 104.6741184958670061, -152.4984795835769944 ) ) ;
#6557=CARTESIAN_POINT ( 'NONE',  ( -52.77438362644100067, 96.81621999649657084, -147.9984795835769944 ) ) ;
#6559=DIRECTION ( 'NONE',  ( -1.000000000000000000, 0.000000000000000000, 0.000000000000000000 ) ) ;
#6560=DIRECTION ( 'NONE',  ( 0.000000000000000000, -0.000000000000000000, 1.000000000000000000 ) ) ;
#6561=DIRECTION ( 'NONE',  ( 0.000000000000000000, 0.000000000000000000, -1.000000000000000000 ) ) ;
#6563=VERTEX_POINT ( 'NONE', #11733 ) ;
#6564=DIRECTION ( 'NONE',  ( 0.5000000000000003331, 0.8660254037844384856, 0.000000000000000000 ) ) ;
#6565=VECTOR ( 'NONE', #8845, 1000.000000000000000 ) ;
#6566=AXIS2_PLACEMENT_3D ( 'NONE', #4020, #12025, #9670 ) ;
#6576=DIRECTION ( 'NONE',  ( 0.000000000000000000, 0.000000000000000000, -1.000000000000000000 ) ) ;
#6577=CARTESIAN_POINT ( 'NONE',  ( -52.77438362643999881, 67.53201699523744139, -147.9984795835769944 ) ) ;
#6578=EDGE_CURVE ( 'NONE', #1067, #3159, #8826, .T. ) ;
#6580=CARTESIAN_POINT ( 'NONE',  ( -52.77438362644000591, 65.17411849586700612, -145.4984795835769660 ) ) ;
#6582=CARTESIAN_POINT ( 'NONE',  ( -66.83542154218349651, 97.90336940298355728, -93.68950033318012061 ) ) ;
#6583=CARTESIAN_POINT ( 'NONE',  ( -75.01311196519617397, 67.29799558322736175, -83.44847958357698303 ) ) ;
#6585=ORIENTED_EDGE ( 'NONE', *, *, #14629, .T. ) ;
#6587=DIRECTION ( 'NONE',  ( 1.000000000000000000, 0.000000000000000000, 0.000000000000000000 ) ) ;
#6590=AXIS2_PLACEMENT_3D ( 'NONE', #14814, #6542, #5607 ) ;
#6591=DIRECTION ( 'NONE',  ( 0.000000000000000000, 0.000000000000000000, 1.000000000000000000 ) ) ;
#6592=EDGE_CURVE ( 'NONE', #1912, #10774, #5122, .T. ) ;
#6594=LINE ( 'NONE', #13862, #5819 ) ;
#6596=MECHANICAL_DESIGN_GEOMETRIC_PRESENTATION_REPRESENTATION('',(#11288),#3862);
#6599=VECTOR ( 'NONE', #7382, 1000.000000000000114 ) ;
#6602=ORIENTED_EDGE ( 'NONE', *, *, #14758, .T. ) ;
#6604=VERTEX_POINT ( 'NONE', #12821 ) ;
#6605=ADVANCED_FACE ( 'NONE', ( #8 ), #9465, .F. ) ;
#6606=ORIENTED_EDGE ( 'NONE', *, *, #6151, .T. ) ;
#6607=ORIENTED_EDGE ( 'NONE', *, *, #9833, .F. ) ;
#6614=AXIS2_PLACEMENT_3D ( 'NONE', #13460, #255, #6479 ) ;
#6615=CARTESIAN_POINT ( 'NONE',  ( -80.52077156573417938, 110.1741184958670061, -79.59847958357700293 ) ) ;
#6619=CYLINDRICAL_SURFACE ( 'NONE', #5351, 2.500000000000002220 ) ;
#6621=DIRECTION ( 'NONE',  ( -1.287488025362404182E-15, -1.000000000000000000, 0.000000000000000000 ) ) ;
#6623=EDGE_CURVE ( 'NONE', #12145, #6920, #1898, .T. ) ;
#6624=EDGE_CURVE ( 'NONE', #12412, #8931, #9805, .T. ) ;
#6625=DIRECTION ( 'NONE',  ( -1.000000000000000000, 0.000000000000000000, 0.000000000000000000 ) ) ;
#6627=CARTESIAN_POINT ( 'NONE',  ( -52.77438362644100067, 99.17411849586700612, -79.59847958357700293 ) ) ;
#6632=ORIENTED_EDGE ( 'NONE', *, *, #7341, .F. ) ;
#6633=ORIENTED_EDGE ( 'NONE', *, *, #9615, .F. ) ;
#6634=PLANE ( 'NONE',  #1778 ) ;
#6638=AXIS2_PLACEMENT_3D ( 'NONE', #4426, #11330, #13816 ) ;
#6639=PLANE ( 'NONE',  #8827 ) ;
#6640=DIRECTION ( 'NONE',  ( 0.000000000000000000, 1.000000000000000000, 0.000000000000000000 ) ) ;
#6641=DIRECTION ( 'NONE',  ( 0.000000000000000000, 0.000000000000000000, -1.000000000000000000 ) ) ;
#6642=DIRECTION ( 'NONE',  ( -1.000000000000000000, 0.000000000000000000, 0.000000000000000000 ) ) ;
#6644=FACE_OUTER_BOUND ( 'NONE', #7837, .T. ) ;
#6646=ORIENTED_EDGE ( 'NONE', *, *, #14344, .F. ) ;
#6648=DIRECTION ( 'NONE',  ( 1.000000000000000000, 0.000000000000000000, 0.000000000000000000 ) ) ;
#6651=CARTESIAN_POINT ( 'NONE',  ( -52.77438362644100067, 103.4241184958670061, -145.4984795835769944 ) ) ;
#6655=CYLINDRICAL_SURFACE ( 'NONE', #6489, 1.500000000000001332 ) ;
#6656=VECTOR ( 'NONE', #14812, 1000.000000000000000 ) ;
#6659=CARTESIAN_POINT ( 'NONE',  ( -88.81638362644100937, 97.99516924618178848, -147.9984795835769944 ) ) ;
#6660=DIRECTION ( 'NONE',  ( 0.000000000000000000, -0.000000000000000000, 1.000000000000000000 ) ) ;
#6661=CARTESIAN_POINT ( 'NONE',  ( -55.47438362644099641, 99.17411849586700612, -145.4984795835769944 ) ) ;
#6663=VERTEX_POINT ( 'NONE', #13366 ) ;
#6664=AXIS2_PLACEMENT_3D ( 'NONE', #13818, #12584, #3187 ) ;
#6668=ADVANCED_FACE ( 'NONE', ( #14429 ), #478, .T. ) ;
#6670=CARTESIAN_POINT ( 'NONE',  ( -54.81638362644100226, 97.99516924618178848, -147.9984795835769944 ) ) ;
#6672=CIRCLE ( 'NONE', #15313, 2.000000000000001776 ) ;
#6675=CARTESIAN_POINT ( 'NONE',  ( -89.27438362644100778, 99.17411849586700612, -145.2984795835770058 ) ) ;
#6677=DIRECTION ( 'NONE',  ( -1.000000000000000000, 0.000000000000000000, 0.000000000000000000 ) ) ;
#6679=ORIENTED_EDGE ( 'NONE', *, *, #2693, .T. ) ;
#6680=ORIENTED_EDGE ( 'NONE', *, *, #7709, .T. ) ;
#6682=VERTEX_POINT ( 'NONE', #5213 ) ;
#6683=ORIENTED_EDGE ( 'NONE', *, *, #5578, .F. ) ;
#6684=VECTOR ( 'NONE', #6879, 1000.000000000000000 ) ;
#6693=PLANE ( 'NONE',  #6590 ) ;
#6696=EDGE_LOOP ( 'NONE', ( #2246, #2871, #3196, #6943, #9726 ) ) ;
#6697=CARTESIAN_POINT ( 'NONE',  ( -69.77438362644001302, 94.57411849586699759, -89.99847958357699440 ) ) ;
#6702=UNCERTAINTY_MEASURE_WITH_UNIT (LENGTH_MEASURE( 1.000000000000000082E-05 ), #6237, 'distance_accuracy_value', 'NONE');
#6704=DIRECTION ( 'NONE',  ( 1.000000000000000000, 0.000000000000000000, 0.000000000000000000 ) ) ;
#6707=LINE ( 'NONE', #15202, #14774 ) ;
#6708=CARTESIAN_POINT ( 'NONE',  ( -59.02799568714584666, 110.1741184958670061, -15.85886927678779834 ) ) ;
#6711=DIRECTION ( 'NONE',  ( 0.000000000000000000, -0.000000000000000000, 1.000000000000000000 ) ) ;
#6712=CARTESIAN_POINT ( 'NONE',  ( -72.41519636941028182, 75.17411849586697770, -44.45439862457464386 ) ) ;
#6718=VERTEX_POINT ( 'NONE', #11027 ) ;
#6721=EDGE_LOOP ( 'NONE', ( #4171, #10728, #4865, #13197 ) ) ;
#6724=DIRECTION ( 'NONE',  ( 0.000000000000000000, 0.000000000000000000, 1.000000000000000000 ) ) ;
#6725=CARTESIAN_POINT ( 'NONE',  ( -69.77438362644001302, 82.17411849586700612, -43.99847958362880007 ) ) ;
#6728=CARTESIAN_POINT ( 'NONE',  ( -68.34858040079876673, 98.11273180361364155, -94.49612629051017620 ) ) ;
#6732=VERTEX_POINT ( 'NONE', #1641 ) ;
#6733=VECTOR ( 'NONE', #5121, 1000.000000000000000 ) ;
#6738=VECTOR ( 'NONE', #8791, 1000.000000000000000 ) ;
#6739=DIRECTION ( 'NONE',  ( 0.000000000000000000, -0.000000000000000000, 1.000000000000000000 ) ) ;
#6744=ORIENTED_EDGE ( 'NONE', *, *, #5639, .F. ) ;
#6746=ORIENTED_EDGE ( 'NONE', *, *, #2672, .T. ) ;
#6747=CIRCLE ( 'NONE', #13688, 8.000000000000007105 ) ;
#6750=EDGE_LOOP ( 'NONE', ( #8884, #14380, #9347, #11967 ) ) ;
#6751=ORIENTED_EDGE ( 'NONE', *, *, #7519, .T. ) ;
#6752=CIRCLE ( 'NONE', #12934, 8.124999999999992895 ) ;
#6754=VECTOR ( 'NONE', #3348, 1000.000000000000114 ) ;
#6759=ADVANCED_FACE ( 'NONE', ( #7316 ), #308, .T. ) ;
#6760=LINE ( 'NONE', #3030, #3151 ) ;
#6766=ADVANCED_FACE ( 'NONE', ( #399 ), #13881, .T. ) ;
#6769=PLANE ( 'NONE',  #13706 ) ;
#6770=VECTOR ( 'NONE', #440, 1000.000000000000000 ) ;
#6772=ORIENTED_EDGE ( 'NONE', *, *, #6884, .F. ) ;
#6774=AXIS2_PLACEMENT_3D ( 'NONE', #13294, #12193, #11032 ) ;
#6775=DIRECTION ( 'NONE',  ( 0.000000000000000000, 0.000000000000000000, 1.000000000000000000 ) ) ;
#6777=CARTESIAN_POINT ( 'NONE',  ( -69.77438362644001302, 82.17411849586700612, -182.1969643934119745 ) ) ;
#6778=DIRECTION ( 'NONE',  ( 0.000000000000000000, 1.000000000000000000, 0.000000000000000000 ) ) ;
#6779=EDGE_CURVE ( 'NONE', #14576, #12703, #5896, .T. ) ;
#6780=AXIS2_PLACEMENT_3D ( 'NONE', #14819, #3038, #705 ) ;
#6781=CARTESIAN_POINT ( 'NONE',  ( -86.77438362644001302, 65.17411849586700612, -145.4984795835769660 ) ) ;
#6783=CARTESIAN_POINT ( 'NONE',  ( -54.81638362644000040, 63.99516924618178848, -147.9984795835769944 ) ) ;
#6788=CARTESIAN_POINT ( 'NONE',  ( -60.43728955831366534, 68.38713492810558137, -83.44847958357698303 ) ) ;
#6789=ORIENTED_EDGE ( 'NONE', *, *, #3741, .T. ) ;
#6791=CARTESIAN_POINT ( 'NONE',  ( -66.41143315690761995, 66.60412428008086749, -81.84847958357697451 ) ) ;
#6792=AXIS2_PLACEMENT_3D ( 'NONE', #4835, #15287, #2187 ) ;
#6793=ORIENTED_EDGE ( 'NONE', *, *, #2848, .T. ) ;
#6794=VECTOR ( 'NONE', #8681, 1000.000000000000000 ) ;
#6795=ADVANCED_FACE ( 'NONE', ( #4267 ), #2009, .F. ) ;
#6800=EDGE_CURVE ( 'NONE', #11016, #12055, #3894, .T. ) ;
#6801=FACE_OUTER_BOUND ( 'NONE', #6195, .T. ) ;
#6804=CONICAL_SURFACE ( 'NONE', #2830, 3.749999999999996447, 0.7853981633974476129 ) ;
#6806=DIRECTION ( 'NONE',  ( 0.000000000000000000, 0.000000000000000000, 1.000000000000000000 ) ) ;
#6808=CARTESIAN_POINT ( 'NONE',  ( -68.62457557633291572, 98.13530264660337821, -94.57468145058379605 ) ) ;
#6811=DIRECTION ( 'NONE',  ( 0.000000000000000000, 0.000000000000000000, -1.000000000000000000 ) ) ;
#6814=AXIS2_PLACEMENT_3D ( 'NONE', #14359, #7318, #8621 ) ;
#6815=VECTOR ( 'NONE', #7202, 1000.000000000000114 ) ;
#6817=LINE ( 'NONE', #2068, #14874 ) ;
#6818=FACE_OUTER_BOUND ( 'NONE', #7227, .T. ) ;
#6819=LINE ( 'NONE', #11539, #4309 ) ;
#6822=DIRECTION ( 'NONE',  ( 0.000000000000000000, -0.000000000000000000, 1.000000000000000000 ) ) ;
#6824=ORIENTED_EDGE ( 'NONE', *, *, #6578, .T. ) ;
#6832=ORIENTED_EDGE ( 'NONE', *, *, #2864, .F. ) ;
#6840=CARTESIAN_POINT ( 'NONE',  ( -48.52438362643999881, 65.17411849586700612, -149.9984795835770228 ) ) ;
#6842=DIRECTION ( 'NONE',  ( 0.000000000000000000, 0.000000000000000000, 1.000000000000000000 ) ) ;
#6843=CARTESIAN_POINT ( 'NONE',  ( -64.53565528768383786, 67.29799558322736175, -81.84847958357697451 ) ) ;
#6844=ORIENTED_EDGE ( 'NONE', *, *, #14265, .F. ) ;
#6847=AXIS2_PLACEMENT_3D ( 'NONE', #4460, #6724, #8958 ) ;
#6851=EDGE_CURVE ( 'NONE', #2365, #14049, #6146, .T. ) ;
#6852=CARTESIAN_POINT ( 'NONE',  ( -84.02438362643999881, 65.17411849586700612, -152.4984795835769944 ) ) ;
#6854=CYLINDRICAL_SURFACE ( 'NONE', #4877, 10.50000000000000178 ) ;
#6856=CARTESIAN_POINT ( 'NONE',  ( -86.77438362643999881, 65.17411849586700612, -79.59847958357700293 ) ) ;
#6859=VECTOR ( 'NONE', #4216, 1000.000000000000000 ) ;
#6860=CARTESIAN_POINT ( 'NONE',  ( -84.73238362644100619, 99.17411849586700612, -147.9984795835769944 ) ) ;
#6862=CARTESIAN_POINT ( 'NONE',  ( -54.81638362644100226, 100.3530677455522238, -150.4984795835770228 ) ) ;
#6866=VERTEX_POINT ( 'NONE', #14878 ) ;
#6867=FACE_OUTER_BOUND ( 'NONE', #5049, .T. ) ;
#6872=ORIENTED_EDGE ( 'NONE', *, *, #11139, .T. ) ;
#6874=CARTESIAN_POINT ( 'NONE',  ( -69.77438362644001302, 82.17411849586700612, -93.49847958357699440 ) ) ;
#6876=AXIS2_PLACEMENT_3D ( 'NONE', #5944, #5705, #4525 ) ;
#6878=EDGE_CURVE ( 'NONE', #3986, #14025, #8601, .T. ) ;
#6879=DIRECTION ( 'NONE',  ( -1.000000000000000000, 0.000000000000000000, 0.000000000000000000 ) ) ;
#6880=ORIENTED_EDGE ( 'NONE', *, *, #12556, .T. ) ;
#6881=EDGE_CURVE ( 'NONE', #6165, #7621, #7698, .T. ) ;
#6884=EDGE_CURVE ( 'NONE', #11036, #4583, #6760, .T. ) ;
#6885=EDGE_LOOP ( 'NONE', ( #10387, #12155, #15196, #11430 ) ) ;
#6888=ORIENTED_EDGE ( 'NONE', *, *, #975, .T. ) ;
#6889=ADVANCED_FACE ( 'NONE', ( #4351 ), #3389, .F. ) ;
#6890=AXIS2_PLACEMENT_3D ( 'NONE', #6931, #3204, #5627 ) ;
#6891=ADVANCED_FACE ( 'NONE', ( #7773 ), #661, .T. ) ;
#6893=FACE_OUTER_BOUND ( 'NONE', #13388, .T. ) ;
#6900=VECTOR ( 'NONE', #8064, 1000.000000000000000 ) ;
#6901=ORIENTED_EDGE ( 'NONE', *, *, #3741, .F. ) ;
#6905=EDGE_LOOP ( 'NONE', ( #11268, #13127, #10891, #9167 ) ) ;
#6907=VERTEX_POINT ( 'NONE', #8296 ) ;
#6912=AXIS2_PLACEMENT_3D ( 'NONE', #13400, #7589, #9890 ) ;
#6915=CARTESIAN_POINT ( 'NONE',  ( -91.27438362643999881, 65.17411849586700612, -79.59847958357700293 ) ) ;
#6918=DIRECTION ( 'NONE',  ( -0.000000000000000000, 0.000000000000000000, -1.000000000000000000 ) ) ;
#6920=VERTEX_POINT ( 'NONE', #6915 ) ;
#6921=LINE ( 'NONE', #3490, #4052 ) ;
#6922=EDGE_LOOP ( 'NONE', ( #9759, #6939, #2896 ) ) ;
#6924=EDGE_LOOP ( 'NONE', ( #14647, #6751, #13219, #1482, #4112 ) ) ;
#6925=ORIENTED_EDGE ( 'NONE', *, *, #769, .F. ) ;
#6926=FACE_OUTER_BOUND ( 'NONE', #10135, .T. ) ;
#6928=CARTESIAN_POINT ( 'NONE',  ( -66.51083064278975598, 75.17411849586699191, -44.70344037800771275 ) ) ;
#6930=CARTESIAN_POINT ( 'NONE',  ( -55.47438362644000165, 65.17411849586700612, -145.2984795835770058 ) ) ;
#6931=CARTESIAN_POINT ( 'NONE',  ( -86.77438362644100778, 99.17411849586700612, -147.9984795835769944 ) ) ;
#6932=PLANE ( 'NONE',  #10240 ) ;
#6935=ORIENTED_EDGE ( 'NONE', *, *, #4127, .T. ) ;
#6939=ORIENTED_EDGE ( 'NONE', *, *, #9503, .T. ) ;
#6940=CARTESIAN_POINT ( 'NONE',  ( -64.53565528768383786, 67.29799558322736175, -83.44847958357698303 ) ) ;
#6941=ORIENTED_EDGE ( 'NONE', *, *, #4110, .F. ) ;
#6943=ORIENTED_EDGE ( 'NONE', *, *, #13413, .F. ) ;
#6945=CARTESIAN_POINT ( 'NONE',  ( -77.94906324475290660, 70.01464610989972925, -83.44847958357698303 ) ) ;
#6948=ADVANCED_FACE ( 'NONE', ( #14264 ), #5686, .F. ) ;
#6949=DIRECTION ( 'NONE',  ( 0.000000000000000000, 0.000000000000000000, -1.000000000000000000 ) ) ;
#6950=ORIENTED_EDGE ( 'NONE', *, *, #14443, .F. ) ;
#6952=ADVANCED_FACE ( 'NONE', ( #998 ), #11708, .F. ) ;
#6953=DIRECTION ( 'NONE',  ( 0.9378889346118977066, 0.3469356515732558988, 0.000000000000000000 ) ) ;
#6955=FACE_OUTER_BOUND ( 'NONE', #12034, .T. ) ;
#6957=ORIENTED_EDGE ( 'NONE', *, *, #8207, .F. ) ;
#6959=DIRECTION ( 'NONE',  ( 0.000000000000000000, 0.000000000000000000, 1.000000000000000000 ) ) ;
#6964=CARTESIAN_POINT ( 'NONE',  ( -65.90140028023573393, 75.17411849586525818, -44.99847958359791278 ) ) ;
#6965=EDGE_CURVE ( 'NONE', #11097, #557, #13041, .T. ) ;
#6966=DIRECTION ( 'NONE',  ( 0.000000000000000000, 0.000000000000000000, -1.000000000000000000 ) ) ;
#6967=CIRCLE ( 'NONE', #9430, 4.499999999999997335 ) ;
#6968=EDGE_CURVE ( 'NONE', #897, #682, #14534, .T. ) ;
#6971=EDGE_LOOP ( 'NONE', ( #10389, #755, #11820 ) ) ;
#6974=EDGE_LOOP ( 'NONE', ( #12746, #5946, #13392, #6305 ) ) ;
#6981=CIRCLE ( 'NONE', #1277, 4.249999999999996447 ) ;
#6982=DIRECTION ( 'NONE',  ( -0.000000000000000000, 0.000000000000000000, -1.000000000000000000 ) ) ;
#6983=CYLINDRICAL_SURFACE ( 'NONE', #3049, 10.50000000000000178 ) ;
#6984=ADVANCED_FACE ( 'NONE', ( #10537 ), #5916, .T. ) ;
#6985=PLANE ( 'NONE',  #5133 ) ;
#6986=DIRECTION ( 'NONE',  ( 0.000000000000000000, 0.000000000000000000, -1.000000000000000000 ) ) ;
#6987=FACE_OUTER_BOUND ( 'NONE', #3841, .T. ) ;
#6990=ADVANCED_FACE ( 'NONE', ( #12958 ), #6985, .F. ) ;
#6992=VECTOR ( 'NONE', #15142, 1000.000000000000000 ) ;
#6993=EDGE_CURVE ( 'NONE', #5515, #9845, #15185, .T. ) ;
#6994=ORIENTED_EDGE ( 'NONE', *, *, #2672, .F. ) ;
#6995=CARTESIAN_POINT ( 'NONE',  ( -85.83938362643999653, 81.46011849586699327, -81.84847958357697451 ) ) ;
#6996=ORIENTED_EDGE ( 'NONE', *, *, #7964, .F. ) ;
#6998=VERTEX_POINT ( 'NONE', #13118 ) ;
#7005=CARTESIAN_POINT ( 'NONE',  ( -91.27438362643999881, 99.17411849586700612, -86.49847958357699440 ) ) ;
#7008=LINE ( 'NONE', #12742, #2414 ) ;
#7009=CARTESIAN_POINT ( 'NONE',  ( -52.77438362643999881, 62.81621999649657084, -147.9984795835769944 ) ) ;
#7010=LINE ( 'NONE', #171, #3839 ) ;
#7011=CARTESIAN_POINT ( 'NONE',  ( -80.52077156573417938, 0.000000000000000000, -79.59847958357700293 ) ) ;
#7013=DIRECTION ( 'NONE',  ( 0.000000000000000000, -1.000000000000000000, 0.000000000000000000 ) ) ;
#7017=VERTEX_POINT ( 'NONE', #4811 ) ;
#7019=ORIENTED_EDGE ( 'NONE', *, *, #11344, .F. ) ;
#7022=VECTOR ( 'NONE', #12110, 1000.000000000000000 ) ;
#7023=CARTESIAN_POINT ( 'NONE',  ( -86.77438362644001302, 99.17411849586700612, -145.4984795835769660 ) ) ;
#7024=DIRECTION ( 'NONE',  ( 0.000000000000000000, 0.000000000000000000, -1.000000000000000000 ) ) ;
#7032=DIRECTION ( 'NONE',  ( 0.000000000000000000, 1.000000000000000000, 0.000000000000000000 ) ) ;
#7036=SURFACE_STYLE_FILL_AREA ( #10903 ) ;
#7038=ORIENTED_EDGE ( 'NONE', *, *, #12766, .T. ) ;
#7039=ADVANCED_FACE ( 'NONE', ( #7217 ), #4659, .F. ) ;
#7041=CIRCLE ( 'NONE', #343, 17.00000000000000000 ) ;
#7042=CARTESIAN_POINT ( 'NONE',  ( -52.77438362643999881, 67.53201699523744139, -147.9984795835769944 ) ) ;
#7044=VECTOR ( 'NONE', #683, 1000.000000000000000 ) ;
#7045=CARTESIAN_POINT ( 'NONE',  ( -58.27438362644001302, 82.17411849586700612, -82.44847958357698303 ) ) ;
#7046=DIRECTION ( 'NONE',  ( 0.000000000000000000, 0.000000000000000000, 1.000000000000000000 ) ) ;
#7047=DIRECTION ( 'NONE',  ( 1.000000000000000000, 0.000000000000000000, 0.000000000000000000 ) ) ;
#7050=DIRECTION ( 'NONE',  ( 0.000000000000000000, 0.000000000000000000, -1.000000000000000000 ) ) ;
#7053=VECTOR ( 'NONE', #7599, 1000.000000000000000 ) ;
#7054=CIRCLE ( 'NONE', #353, 2.750000000000002665 ) ;
#7056=ORIENTED_EDGE ( 'NONE', *, *, #11805, .F. ) ;
#7059=VERTEX_POINT ( 'NONE', #2546 ) ;
#7060=ORIENTED_EDGE ( 'NONE', *, *, #12764, .F. ) ;
#7061=ADVANCED_FACE ( 'NONE', ( #9373 ), #3560, .F. ) ;
#7062=EDGE_LOOP ( 'NONE', ( #11934, #1892, #5908, #12811 ) ) ;
#7064=DIRECTION ( 'NONE',  ( 0.000000000000000000, 0.000000000000000000, -1.000000000000000000 ) ) ;
#7067=DIRECTION ( 'NONE',  ( -1.287488025362404182E-15, -1.000000000000000000, 0.000000000000000000 ) ) ;
#7070=DIRECTION ( 'NONE',  ( 0.000000000000000000, 1.000000000000000000, 0.000000000000000000 ) ) ;
#7072=PLANE ( 'NONE',  #128 ) ;
#7076=ORIENTED_EDGE ( 'NONE', *, *, #1274, .T. ) ;
#7077=ADVANCED_FACE ( 'NONE', ( #14336 ), #12024, .F. ) ;
#7078=CARTESIAN_POINT ( 'NONE',  ( -86.77438362643999881, 65.17411849586700612, -150.4984795835770228 ) ) ;
#7082=EDGE_CURVE ( 'NONE', #14576, #12826, #9521, .T. ) ;
#7083=VECTOR ( 'NONE', #10836, 1000.000000000000000 ) ;
#7084=AXIS2_PLACEMENT_3D ( 'NONE', #15110, #10384, #624 ) ;
#7096=FACE_OUTER_BOUND ( 'NONE', #14220, .T. ) ;
#7098=EDGE_LOOP ( 'NONE', ( #11604, #7483, #1719, #8259 ) ) ;
#7099=AXIS2_PLACEMENT_3D ( 'NONE', #8906, #6822, #11543 ) ;
#7103=EDGE_CURVE ( 'NONE', #10418, #7517, #1305, .T. ) ;
#7105=CIRCLE ( 'NONE', #7850, 4.499999999999997335 ) ;
#7108=VECTOR ( 'NONE', #271, 1000.000000000000000 ) ;
#7109=FACE_OUTER_BOUND ( 'NONE', #14105, .T. ) ;
#7112=PRODUCT ( 'Pneumatic Cylinder Piston', 'Pneumatic Cylinder Piston', '', ( #2516 ) ) ;
#7114=ORIENTED_EDGE ( 'NONE', *, *, #14369, .F. ) ;
#7115=VECTOR ( 'NONE', #2514, 1000.000000000000000 ) ;
#7116=CARTESIAN_POINT ( 'NONE',  ( -54.81638362644000040, 63.99516924618178848, -147.9984795835769944 ) ) ;
#7118=AXIS2_PLACEMENT_3D ( 'NONE', #14184, #11941, #13956 ) ;
#7119=EDGE_LOOP ( 'NONE', ( #955, #4700, #9864, #14947, #11065 ) ) ;
#7122=VECTOR ( 'NONE', #9951, 1000.000000000000000 ) ;
#7125=AXIS2_PLACEMENT_3D ( 'NONE', #5082, #5729, #8125 ) ;
#7130=CARTESIAN_POINT ( 'NONE',  ( -86.77438362644100778, 103.4241184958670061, -145.4984795835769944 ) ) ;
#7131=CARTESIAN_POINT ( 'NONE',  ( -82.27438362643999881, 99.17411849586700612, -152.4984795835769944 ) ) ;
#7139=ORIENTED_EDGE ( 'NONE', *, *, #1646, .F. ) ;
#7141=ORIENTED_EDGE ( 'NONE', *, *, #13987, .T. ) ;
#7144=CARTESIAN_POINT ( 'NONE',  ( -52.77438362644100067, 99.17411849586700612, -147.9984795835769944 ) ) ;
#7146=CIRCLE ( 'NONE', #4910, 16.00000000000000000 ) ;
#7149=DIRECTION ( 'NONE',  ( 0.000000000000000000, 0.000000000000000000, -1.000000000000000000 ) ) ;
#7150=ADVANCED_FACE ( 'NONE', ( #9444 ), #14182, .F. ) ;
#7153=ORIENTED_EDGE ( 'NONE', *, *, #5038, .F. ) ;
#7155=ORIENTED_EDGE ( 'NONE', *, *, #11519, .F. ) ;
#7157=EDGE_LOOP ( 'NONE', ( #6683, #2598, #9401, #3457 ) ) ;
#7158=AXIS2_PLACEMENT_3D ( 'NONE', #2724, #1787, #6625 ) ;
#7163=CARTESIAN_POINT ( 'NONE',  ( 0.000000000000000000, 0.000000000000000000, -79.59847958357700293 ) ) ;
#7165=PLANE ( 'NONE',  #5626 ) ;
#7166=CARTESIAN_POINT ( 'NONE',  ( -86.77438362644100778, 99.17411849586700612, -150.4984795835770228 ) ) ;
#7167=CARTESIAN_POINT ( 'NONE',  ( -35.27438362644000591, 60.67411849586700612, -79.49847958357700861 ) ) ;
#7168=FACE_OUTER_BOUND ( 'NONE', #13296, .T. ) ;
#7169=EDGE_CURVE ( 'NONE', #3095, #8331, #15260, .T. ) ;
#7170=PLANE ( 'NONE',  #6360 ) ;
#7171=CARTESIAN_POINT ( 'NONE',  ( -73.64736697264743270, 75.17411849586699191, -44.99847958359794120 ) ) ;
#7173=ORIENTED_EDGE ( 'NONE', *, *, #14349, .T. ) ;
#7175=EDGE_CURVE ( 'NONE', #13238, #5950, #12877, .T. ) ;
#7176=EDGE_LOOP ( 'NONE', ( #1336, #9282, #10157, #7687 ) ) ;
#7177=ADVANCED_FACE ( 'NONE', ( #4656 ), #14110, .F. ) ;
#7182=ORIENTED_EDGE ( 'NONE', *, *, #7362, .F. ) ;
#7186=DIRECTION ( 'NONE',  ( -1.000000000000000000, 0.000000000000000000, 0.000000000000000000 ) ) ;
#7187=CYLINDRICAL_SURFACE ( 'NONE', #10732, 1.500000000000001332 ) ;
#7188=EDGE_CURVE ( 'NONE', #13728, #6550, #14712, .T. ) ;
#7190=EDGE_LOOP ( 'NONE', ( #5803, #11039, #9664, #11976 ) ) ;
#7191=CARTESIAN_POINT ( 'NONE',  ( -52.77438362644100067, 99.17411849586700612, -182.2484795835770228 ) ) ;
#7193=PRODUCT_DEFINITION_FORMATION_WITH_SPECIFIED_SOURCE ( 'ANY', '', #7112, .NOT_KNOWN. ) ;
#7195=CARTESIAN_POINT ( 'NONE',  ( -79.02077156573416516, 103.6741184958669777, -79.59847958357700293 ) ) ;
#7202=DIRECTION ( 'NONE',  ( 0.7071067811865474617, 0.000000000000000000, 0.7071067811865474617 ) ) ;
#7206=EDGE_LOOP ( 'NONE', ( #8953, #4987, #9830, #8550, #106 ) ) ;
#7209=DIRECTION ( 'NONE',  ( -1.000000000000000000, 0.000000000000000000, 0.000000000000000000 ) ) ;
#7211=ORIENTED_EDGE ( 'NONE', *, *, #7472, .T. ) ;
#7217=FACE_OUTER_BOUND ( 'NONE', #6721, .T. ) ;
#7218=AXIS2_PLACEMENT_3D ( 'NONE', #5498, #14858, #14935 ) ;
#7222=CARTESIAN_POINT ( 'NONE',  ( -69.77438362644001302, 82.17411849586700612, -80.14847958357698587 ) ) ;
#7223=ORIENTED_EDGE ( 'NONE', *, *, #8917, .T. ) ;
#7224=DIRECTION ( 'NONE',  ( -1.000000000000000000, 0.000000000000000000, 0.000000000000000000 ) ) ;
#7225=VERTEX_POINT ( 'NONE', #2938 ) ;
#7227=EDGE_LOOP ( 'NONE', ( #3759, #3576, #5575, #8614 ) ) ;
#7230=EDGE_CURVE ( 'NONE', #8280, #2251, #15280, .T. ) ;
#7235=ADVANCED_FACE ( 'NONE', ( #8671 ), #7872, .F. ) ;
#7237=DIRECTION ( 'NONE',  ( 1.000000000000000000, 0.000000000000000000, 0.000000000000000000 ) ) ;
#7238=CARTESIAN_POINT ( 'NONE',  ( -86.77438362644001302, 82.17411849586700612, -81.84847958357697451 ) ) ;
#7241=DIRECTION ( 'NONE',  ( 0.8660254037844387076, 0.4999999999999998890, 0.000000000000000000 ) ) ;
#7244=AXIS2_PLACEMENT_3D ( 'NONE', #9128, #9360, #8200 ) ;
#7245=EDGE_LOOP ( 'NONE', ( #14334, #3020 ) ) ;
#7253=VECTOR ( 'NONE', #1092, 1000.000000000000000 ) ;
#7260=CARTESIAN_POINT ( 'NONE',  ( -61.59970400812709102, 70.01464610989972925, -83.44847958357698303 ) ) ;
#7262=CARTESIAN_POINT ( 'NONE',  ( -84.73238362644100619, 100.3530677455522238, -150.4984795835770228 ) ) ;
#7263=CARTESIAN_POINT ( 'NONE',  ( -60.43728955831366534, 68.38713492810558137, -81.84847958357697451 ) ) ;
#7265=EDGE_CURVE ( 'NONE', #10774, #1225, #12328, .T. ) ;
#7269=SURFACE_STYLE_FILL_AREA ( #7348 ) ;
#7272=EDGE_CURVE ( 'NONE', #8742, #1753, #1987, .T. ) ;
#7273=AXIS2_PLACEMENT_3D ( 'NONE', #2189, #11816, #9471 ) ;
#7274=CARTESIAN_POINT ( 'NONE',  ( -69.77438362644001302, 84.67411849586700612, -67.69567958357700377 ) ) ;
#7275=EDGE_CURVE ( 'NONE', #15133, #3902, #7959, .T. ) ;
#7276=CARTESIAN_POINT ( 'NONE',  ( -75.01311196519617397, 67.29799558322736175, -83.44847958357698303 ) ) ;
#7277=ADVANCED_FACE ( 'NONE', ( #6818 ), #11458, .T. ) ;
#7278=CIRCLE ( 'NONE', #9978, 2.042000000000002036 ) ;
#7280=CIRCLE ( 'NONE', #11473, 8.349999999999996092 ) ;
#7281=DIRECTION ( 'NONE',  ( -1.000000000000000000, 0.000000000000000000, 0.000000000000000000 ) ) ;
#7285=AXIS2_PLACEMENT_3D ( 'NONE', #2094, #7917, #5609 ) ;
#7286=VERTEX_POINT ( 'NONE', #8975 ) ;
#7287=CARTESIAN_POINT ( 'NONE',  ( -69.77438362644001302, 82.17411849586700612, -80.44847958357698303 ) ) ;
#7288=ORIENTED_EDGE ( 'NONE', *, *, #10171, .F. ) ;
#7291=EDGE_LOOP ( 'NONE', ( #5842, #13501, #740, #9367 ) ) ;
#7293=VECTOR ( 'NONE', #8465, 1000.000000000000000 ) ;
#7297=DIRECTION ( 'NONE',  ( 0.000000000000000000, -0.000000000000000000, 1.000000000000000000 ) ) ;
#7299=DIRECTION ( 'NONE',  ( 0.000000000000000000, 1.000000000000000000, 0.000000000000000000 ) ) ;
#7303=CARTESIAN_POINT ( 'NONE',  ( -52.77438362644000591, 65.17411849586700612, -86.49847958357699440 ) ) ;
#7305=DIRECTION ( 'NONE',  ( 0.000000000000000000, 0.000000000000000000, -1.000000000000000000 ) ) ;
#7306=EDGE_LOOP ( 'NONE', ( #10900, #487, #5301, #2660 ) ) ;
#7308=ORIENTED_EDGE ( 'NONE', *, *, #5738, .F. ) ;
#7310=DIRECTION ( 'NONE',  ( 0.000000000000000000, -1.000000000000000000, 0.000000000000000000 ) ) ;
#7316=FACE_OUTER_BOUND ( 'NONE', #8244, .T. ) ;
#7318=DIRECTION ( 'NONE',  ( 0.000000000000000000, 0.000000000000000000, -1.000000000000000000 ) ) ;
#7320=CARTESIAN_POINT ( 'NONE',  ( -62.02799568714584666, 103.6741184958669919, -73.34256232478206528 ) ) ;
#7321=DIRECTION ( 'NONE',  ( 0.000000000000000000, -1.000000000000000000, 0.000000000000000000 ) ) ;
#7323=DIRECTION ( 'NONE',  ( 0.000000000000000000, 0.000000000000000000, 1.000000000000000000 ) ) ;
#7324=ADVANCED_FACE ( 'NONE', ( #12558 ), #5427, .T. ) ;
#7326=CIRCLE ( 'NONE', #9281, 4.250000000000003553 ) ;
#7328=CIRCLE ( 'NONE', #10521, 2.042000000000002036 ) ;
#7334=DIRECTION ( 'NONE',  ( 1.000000000000000000, 0.000000000000000000, 0.000000000000000000 ) ) ;
#7336=VECTOR ( 'NONE', #3326, 1000.000000000000000 ) ;
#7338=VECTOR ( 'NONE', #2636, 1000.000000000000000 ) ;
#7341=EDGE_CURVE ( 'NONE', #13910, #12014, #3160, .T. ) ;
#7342=FACE_BOUND ( 'NONE', #4820, .T. ) ;
#7343=EDGE_CURVE ( 'NONE', #9479, #6326, #676, .T. ) ;
#7347=CIRCLE ( 'NONE', #642, 16.06499999999999773 ) ;
#7348=FILL_AREA_STYLE ('',( #15314 ) ) ;
#7351=AXIS2_PLACEMENT_3D ( 'NONE', #12087, #4878, #13252 ) ;
#7354=EDGE_CURVE ( 'NONE', #384, #6165, #7631, .T. ) ;
#7355=CIRCLE ( 'NONE', #651, 2.500000000000002220 ) ;
#7358=CARTESIAN_POINT ( 'NONE',  ( -69.77438362644002723, 75.17411849587348627, -43.99847958364158984 ) ) ;
#7359=CYLINDRICAL_SURFACE ( 'NONE', #14185, 4.500000000000003553 ) ;
#7362=EDGE_CURVE ( 'NONE', #1952, #10812, #9122, .T. ) ;
#7363=DIRECTION ( 'NONE',  ( 1.000000000000000000, 0.000000000000000000, 0.000000000000000000 ) ) ;
#7364=ORIENTED_EDGE ( 'NONE', *, *, #12068, .F. ) ;
#7366=ORIENTED_EDGE ( 'NONE', *, *, #9893, .T. ) ;
#7368=DIRECTION ( 'NONE',  ( 1.000000000000000000, 0.000000000000000000, 0.000000000000000000 ) ) ;
#7369=ADVANCED_FACE ( 'NONE', ( #15086 ), #1172, .T. ) ;
#7373=ORIENTED_EDGE ( 'NONE', *, *, #11682, .F. ) ;
#7376=DIRECTION ( 'NONE',  ( -0.7071067811865474617, 8.659560562354921765E-17, 0.7071067811865474617 ) ) ;
#7378=DIRECTION ( 'NONE',  ( 1.000000000000000000, 0.000000000000000000, 0.000000000000000000 ) ) ;
#7380=PLANE ( 'NONE',  #2179 ) ;
#7382=DIRECTION ( 'NONE',  ( 0.7071067811865474617, 0.000000000000000000, 0.7071067811865474617 ) ) ;
#7383=ADVANCED_FACE ( 'NONE', ( #13384 ), #9580, .F. ) ;
#7384=LINE ( 'NONE', #11091, #13229 ) ;
#7385=VECTOR ( 'NONE', #3390, 1000.000000000000000 ) ;
#7387=CYLINDRICAL_SURFACE ( 'NONE', #12218, 8.124999999999992895 ) ;
#7388=ORIENTED_EDGE ( 'NONE', *, *, #8222, .T. ) ;
#7390=ORIENTED_EDGE ( 'NONE', *, *, #7580, .F. ) ;
#7394=CIRCLE ( 'NONE', #7643, 3.749999999999996447 ) ;
#7397=CARTESIAN_POINT ( 'NONE',  ( -38.27438362644000591, 60.67411849586700612, 0.000000000000000000 ) ) ;
#7398=DIRECTION ( 'NONE',  ( -0.000000000000000000, -0.000000000000000000, 1.000000000000000000 ) ) ;
#7399=LINE ( 'NONE', #10717, #11842 ) ;
#7400=DIRECTION ( 'NONE',  ( -0.000000000000000000, -0.000000000000000000, 1.000000000000000000 ) ) ;
#7401=FACE_OUTER_BOUND ( 'NONE', #3954, .T. ) ;
#7402=DIRECTION ( 'NONE',  ( 0.000000000000000000, 1.000000000000000000, 0.000000000000000000 ) ) ;
#7403=DIRECTION ( 'NONE',  ( 0.000000000000000000, 0.000000000000000000, 1.000000000000000000 ) ) ;
#7406=ORIENTED_EDGE ( 'NONE', *, *, #9043, .T. ) ;
#7410=CARTESIAN_POINT ( 'NONE',  ( -71.13655333277205273, 90.17411849586699191, -58.99847958357693756 ) ) ;
#7413=CARTESIAN_POINT ( 'NONE',  ( -55.27438362643999881, 65.17411849586700612, -79.59847958357700293 ) ) ;
#7415=CIRCLE ( 'NONE', #1205, 2.500000000000002220 ) ;
#7416=DIRECTION ( 'NONE',  ( 0.000000000000000000, 0.000000000000000000, -1.000000000000000000 ) ) ;
#7420=PLANE ( 'NONE',  #12566 ) ;
#7422=VERTEX_POINT ( 'NONE', #9275 ) ;
#7423=CIRCLE ( 'NONE', #5953, 2.042000000000002036 ) ;
#7426=EDGE_LOOP ( 'NONE', ( #2866, #9972 ) ) ;
#7430=EDGE_CURVE ( 'NONE', #1293, #12917, #3398, .T. ) ;
#7431=DIRECTION ( 'NONE',  ( 0.000000000000000000, 0.000000000000000000, 1.000000000000000000 ) ) ;
#7437=DIRECTION ( 'NONE',  ( -1.000000000000000000, 0.000000000000000000, 0.000000000000000000 ) ) ;
#7438=DIRECTION ( 'NONE',  ( 0.000000000000000000, -0.000000000000000000, 1.000000000000000000 ) ) ;
#7439=VERTEX_POINT ( 'NONE', #3625 ) ;
#7440=EDGE_LOOP ( 'NONE', ( #5134, #13110, #10467 ) ) ;
#7442=ORIENTED_EDGE ( 'NONE', *, *, #3091, .F. ) ;
#7445=ORIENTED_EDGE ( 'NONE', *, *, #894, .T. ) ;
#7451=EDGE_CURVE ( 'NONE', #11316, #10367, #9422, .T. ) ;
#7454=CARTESIAN_POINT ( 'NONE',  ( -59.27438362644000591, 82.17411849586700612, -182.1969643934119745 ) ) ;
#7458=ORIENTED_EDGE ( 'NONE', *, *, #13994, .T. ) ;
#7459=EDGE_CURVE ( 'NONE', #3281, #9205, #10596, .T. ) ;
#7462=ORIENTED_EDGE ( 'NONE', *, *, #7986, .F. ) ;
#7466=B_SPLINE_CURVE_WITH_KNOTS ( 'NONE', 3,
 ( #2999, #6582, #4169, #665, #7671, #6728, #6808, #11216, #5418, #13633, #5649, #10119, #11524, #3154, #3218, #10193, #5333, #14782 ),
 .UNSPECIFIED., .F., .F.,
 ( 4, 2, 2, 2, 2, 2, 2, 2, 4 ),
 ( 0.01135168602782440743, 0.01221517698400053330, 0.01307866794017665917, 0.01394215889635278677, 0.01480564985252891264, 0.01566914080870503850, 0.01653263176488116437, 0.01739612272105729024, 0.01825961367723341611 ),
 .UNSPECIFIED. ) ;
#7467=FILL_AREA_STYLE_COLOUR ( '', #5338 ) ;
#7469=CARTESIAN_POINT ( 'NONE',  ( -86.77438362644100778, 99.17411849586700612, -150.4984795835770228 ) ) ;
#7471=ADVANCED_FACE ( 'NONE', ( #11845 ), #1212, .F. ) ;
#7472=EDGE_CURVE ( 'NONE', #10684, #8823, #12138, .T. ) ;
#7477=CYLINDRICAL_SURFACE ( 'NONE', #5052, 8.050000000000000711 ) ;
#7478=VECTOR ( 'NONE', #13394, 1000.000000000000000 ) ;
#7482=AXIS2_PLACEMENT_3D ( 'NONE', #1210, #13013, #4550 ) ;
#7483=ORIENTED_EDGE ( 'NONE', *, *, #725, .T. ) ;
#7488=CIRCLE ( 'NONE', #771, 10.49999999999999467 ) ;
#7489=LINE ( 'NONE', #11122, #14033 ) ;
#7490=CARTESIAN_POINT ( 'NONE',  ( -52.77438362644000591, 65.17411849586700612, -145.4984795835769660 ) ) ;
#7491=CARTESIAN_POINT ( 'NONE',  ( -69.77438362644001302, 82.17411849586700612, -80.44847958357698303 ) ) ;
#7494=CARTESIAN_POINT ( 'NONE',  ( -85.77438362644001302, 82.17411849586700612, -138.4984795835769944 ) ) ;
#7495=CIRCLE ( 'NONE', #779, 2.042000000000002036 ) ;
#7499=AXIS2_PLACEMENT_3D ( 'NONE', #10245, #1014, #2183 ) ;
#7500=ORIENTED_EDGE ( 'NONE', *, *, #15012, .T. ) ;
#7501=AXIS2_PLACEMENT_3D ( 'NONE', #11346, #1011, #5460 ) ;
#7504=AXIS2_PLACEMENT_3D ( 'NONE', #11372, #739, #10587 ) ;
#7506=DIRECTION ( 'NONE',  ( 1.000000000000000000, 0.000000000000000000, 0.000000000000000000 ) ) ;
#7507=DIRECTION ( 'NONE',  ( 1.000000000000000000, 0.000000000000000000, 0.000000000000000000 ) ) ;
#7509=DIRECTION ( 'NONE',  ( 0.000000000000000000, 0.000000000000000000, 1.000000000000000000 ) ) ;
#7510=CARTESIAN_POINT ( 'NONE',  ( -83.02438362643998460, 65.17411849586700612, -150.4984795835770228 ) ) ;
#7512=CARTESIAN_POINT ( 'NONE',  ( -52.77438362644100067, 99.17411849586700612, -79.59847958357700293 ) ) ;
#7515=DIRECTION ( 'NONE',  ( -1.000000000000000000, 0.000000000000000000, 0.000000000000000000 ) ) ;
#7517=VERTEX_POINT ( 'NONE', #12441 ) ;
#7519=EDGE_CURVE ( 'NONE', #3577, #14784, #719, .T. ) ;
#7522=CARTESIAN_POINT ( 'NONE',  ( -91.27438362643999881, 99.17411849586700612, -86.49847958357699440 ) ) ;
#7524=VERTEX_POINT ( 'NONE', #2979 ) ;
#7525=ADVANCED_FACE ( 'NONE', ( #3982 ), #563, .F. ) ;
#7526=LINE ( 'NONE', #8745, #8201 ) ;
#7527=AXIS2_PLACEMENT_3D ( 'NONE', #2639, #14273, #9679 ) ;
#7530=AXIS2_PLACEMENT_3D ( 'NONE', #10461, #10544, #10700 ) ;
#7538=EDGE_CURVE ( 'NONE', #10872, #14575, #1664, .T. ) ;
#7539=AXIS2_PLACEMENT_3D ( 'NONE', #15250, #2226, #15092 ) ;
#7541=VERTEX_POINT ( 'NONE', #5229 ) ;
#7546=AXIS2_PLACEMENT_3D ( 'NONE', #10584, #9566, #3685 ) ;
#7551=CIRCLE ( 'NONE', #12244, 16.00000000000000000 ) ;
#7554=DIRECTION ( 'NONE',  ( -1.000000000000000000, 0.000000000000000000, 0.000000000000000000 ) ) ;
#7555=DIRECTION ( 'NONE',  ( 0.000000000000000000, 1.000000000000000000, 0.000000000000000000 ) ) ;
#7556=DIRECTION ( 'NONE',  ( 0.000000000000000000, 0.000000000000000000, -1.000000000000000000 ) ) ;
#7557=DIRECTION ( 'NONE',  ( 0.000000000000000000, 0.000000000000000000, -1.000000000000000000 ) ) ;
#7558=ORIENTED_EDGE ( 'NONE', *, *, #13592, .F. ) ;
#7562=VERTEX_POINT ( 'NONE', #13461 ) ;
#7563=ORIENTED_EDGE ( 'NONE', *, *, #393, .T. ) ;
#7564=AXIS2_PLACEMENT_3D ( 'NONE', #3818, #6175, #10883 ) ;
#7565=CIRCLE ( 'NONE', #11508, 17.00000000000000000 ) ;
#7566=EDGE_CURVE ( 'NONE', #14784, #5278, #1803, .T. ) ;
#7568=EDGE_CURVE ( 'NONE', #3958, #9995, #11084, .T. ) ;
#7573=ADVANCED_FACE ( 'NONE', ( #11277 ), #8713, .T. ) ;
#7574=CARTESIAN_POINT ( 'NONE',  ( -69.77438362644001302, 74.17411849586699191, -29.37106258560738681 ) ) ;
#7575=DIRECTION ( 'NONE',  ( 0.000000000000000000, -1.000000000000000000, 0.000000000000000000 ) ) ;
#7577=ORIENTED_EDGE ( 'NONE', *, *, #5432, .F. ) ;
#7579=CARTESIAN_POINT ( 'NONE',  ( -82.27438362643999881, 99.17411849586700612, -145.4984795835769660 ) ) ;
#7580=EDGE_CURVE ( 'NONE', #15237, #2560, #7791, .T. ) ;
#7581=ORIENTED_EDGE ( 'NONE', *, *, #8222, .F. ) ;
#7583=ORIENTED_EDGE ( 'NONE', *, *, #4711, .F. ) ;
#7584=AXIS2_PLACEMENT_3D ( 'NONE', #10378, #8425, #13167 ) ;
#7586=FACE_OUTER_BOUND ( 'NONE', #14309, .T. ) ;
#7587=CARTESIAN_POINT ( 'NONE',  ( -69.77438362644001302, 82.17411849586700612, -51.99847958357699440 ) ) ;
#7588=CARTESIAN_POINT ( 'NONE',  ( -82.27438362643999881, 65.17411849586700612, -86.49847958357699440 ) ) ;
#7589=DIRECTION ( 'NONE',  ( 0.000000000000000000, 0.000000000000000000, -1.000000000000000000 ) ) ;
#7590=CARTESIAN_POINT ( 'NONE',  ( -54.81638362644000040, 63.99516924618178848, -147.9984795835769944 ) ) ;
#7591=DIRECTION ( 'NONE',  ( 0.000000000000000000, 0.000000000000000000, -1.000000000000000000 ) ) ;
#7593=PLANE ( 'NONE',  #14998 ) ;
#7596=CIRCLE ( 'NONE', #13784, 4.249999999999996447 ) ;
#7599=DIRECTION ( 'NONE',  ( 0.000000000000000000, 0.000000000000000000, -1.000000000000000000 ) ) ;
#7601=ORIENTED_EDGE ( 'NONE', *, *, #7566, .F. ) ;
#7602=VECTOR ( 'NONE', #6842, 1000.000000000000000 ) ;
#7604=AXIS2_PLACEMENT_3D ( 'NONE', #8238, #2418, #1100 ) ;
#7605=AXIS2_PLACEMENT_3D ( 'NONE', #4063, #12207, #1581 ) ;
#7607=DIRECTION ( 'NONE',  ( 1.000000000000000000, 0.000000000000000000, 0.000000000000000000 ) ) ;
#7609=CARTESIAN_POINT ( 'NONE',  ( -69.77438362644001302, 82.17411849586700612, -150.4984795835769944 ) ) ;
#7613=ORIENTED_EDGE ( 'NONE', *, *, #8658, .F. ) ;
#7616=B_SPLINE_CURVE_WITH_KNOTS ( 'NONE', 3,
 ( #1963, #4151, #6712, #4291, #8873, #7792, #2980, #3275 ),
 .UNSPECIFIED., .F., .F.,
 ( 4, 2, 2, 4 ),
 ( 0.04105254269951071067, 0.04300721795512767176, 0.04398455558293615231, 0.04496189321074463285 ),
 .UNSPECIFIED. ) ;
#7617=VECTOR ( 'NONE', #5989, 1000.000000000000000 ) ;
#7620=ORIENTED_EDGE ( 'NONE', *, *, #7986, .T. ) ;
#7621=VERTEX_POINT ( 'NONE', #4150 ) ;
#7628=CARTESIAN_POINT ( 'NONE',  ( -86.77438362644100778, 96.81621999649657084, -147.9984795835769944 ) ) ;
#7629=EDGE_CURVE ( 'NONE', #10445, #5739, #9874, .T. ) ;
#7631=CIRCLE ( 'NONE', #12817, 10.49999999999999467 ) ;
#7635=LINE ( 'NONE', #1870, #1125 ) ;
#7636=CARTESIAN_POINT ( 'NONE',  ( -67.13357088346970158, 89.17411849586699191, -44.45439862457462965 ) ) ;
#7637=ORIENTED_EDGE ( 'NONE', *, *, #3623, .T. ) ;
#7640=ORIENTED_EDGE ( 'NONE', *, *, #3009, .T. ) ;
#7643=AXIS2_PLACEMENT_3D ( 'NONE', #4217, #423, #14602 ) ;
#7645=CARTESIAN_POINT ( 'NONE',  ( -52.77438362643999881, 65.17411849586700612, -145.4984795835769944 ) ) ;
#7647=EDGE_CURVE ( 'NONE', #2744, #2455, #14307, .T. ) ;
#7648=CARTESIAN_POINT ( 'NONE',  ( -52.77438362644000591, 99.17411849586700612, -152.4984795835769944 ) ) ;
#7649=CARTESIAN_POINT ( 'NONE',  ( -86.77438362644100778, 101.5320169952374414, -150.4984795835770228 ) ) ;
#7651=EDGE_CURVE ( 'NONE', #6323, #8857, #1926, .T. ) ;
#7654=ADVANCED_FACE ( 'NONE', ( #11353 ), #11193, .F. ) ;
#7658=ORIENTED_EDGE ( 'NONE', *, *, #1086, .T. ) ;
#7660=EDGE_CURVE ( 'NONE', #5822, #13943, #7394, .T. ) ;
#7662=ORIENTED_EDGE ( 'NONE', *, *, #3510, .F. ) ;
#7664=CARTESIAN_POINT ( 'NONE',  ( -54.81638362644000040, 63.99516924618178848, -147.9984795835769944 ) ) ;
#7665=EDGE_CURVE ( 'NONE', #6231, #9550, #11501, .T. ) ;
#7667=CARTESIAN_POINT ( 'NONE',  ( -61.64938362644000591, 82.17411849586700612, -79.49847958357700861 ) ) ;
#7668=EDGE_CURVE ( 'NONE', #5306, #7524, #3351, .T. ) ;
#7669=CARTESIAN_POINT ( 'NONE',  ( -69.77438362644001302, 82.17411849586700612, -117.9984795835769944 ) ) ;
#7671=CARTESIAN_POINT ( 'NONE',  ( -67.81379359564340348, 98.05581852273024879, -94.29007922354536220 ) ) ;
#7673=ORIENTED_EDGE ( 'NONE', *, *, #393, .F. ) ;
#7674=EDGE_LOOP ( 'NONE', ( #9992, #11267 ) ) ;
#7675=DIRECTION ( 'NONE',  ( -1.000000000000000000, 0.000000000000000000, 0.000000000000000000 ) ) ;
#7677=ORIENTED_EDGE ( 'NONE', *, *, #13873, .F. ) ;
#7678=CARTESIAN_POINT ( 'NONE',  ( -86.77438362644100778, 99.17411849586700612, -79.59847958357700293 ) ) ;
#7681=DIRECTION ( 'NONE',  ( 0.000000000000000000, 0.000000000000000000, 1.000000000000000000 ) ) ;
#7684=FACE_OUTER_BOUND ( 'NONE', #10520, .T. ) ;
#7687=ORIENTED_EDGE ( 'NONE', *, *, #3062, .F. ) ;
#7691=ORIENTED_EDGE ( 'NONE', *, *, #3458, .T. ) ;
#7692=( BOUNDED_CURVE ( )  B_SPLINE_CURVE ( 3, ( #12822, #12599, #14977, #13834 ),
 .UNSPECIFIED., .F., .T. ) 
 B_SPLINE_CURVE_WITH_KNOTS ( ( 4, 4 ),
 ( 5.777824796895650650, 6.283185307179590673 ),
 .UNSPECIFIED. ) 
 CURVE ( )  GEOMETRIC_REPRESENTATION_ITEM ( )  RATIONAL_B_SPLINE_CURVE ( ( 1.000000000000000000, 0.9788305577012550440, 0.9788305577012550440, 1.000000000000000000 ) ) 
 REPRESENTATION_ITEM ( '' )  );
#7694=ADVANCED_FACE ( 'NONE', ( #11734 ), #3130, .F. ) ;
#7698=LINE ( 'NONE', #10079, #1906 ) ;
#7699=CARTESIAN_POINT ( 'NONE',  ( -54.81638362644000040, 63.99516924618178848, -147.9984795835769944 ) ) ;
#7701=DIRECTION ( 'NONE',  ( 1.000000000000000000, 0.000000000000000000, 0.000000000000000000 ) ) ;
#7703=DIRECTION ( 'NONE',  ( -1.287488025362404182E-15, -1.000000000000000000, 0.000000000000000000 ) ) ;
#7705=LINE ( 'NONE', #11406, #6293 ) ;
#7709=EDGE_CURVE ( 'NONE', #8931, #2834, #7008, .T. ) ;
#7712=EDGE_CURVE ( 'NONE', #12468, #7562, #15286, .T. ) ;
#7713=CARTESIAN_POINT ( 'NONE',  ( -96.77438362643999881, 59.67411849586700612, -152.4984795835769944 ) ) ;
#7716=DIRECTION ( 'NONE',  ( 1.287488025362404182E-15, 1.000000000000000000, 0.000000000000000000 ) ) ;
#7717=CARTESIAN_POINT ( 'NONE',  ( -38.27438362644000591, 60.67411849586700612, -67.49847958357700861 ) ) ;
#7723=AXIS2_PLACEMENT_3D ( 'NONE', #5243, #4162, #575 ) ;
#7726=ORIENTED_EDGE ( 'NONE', *, *, #13327, .F. ) ;
#7731=AXIS2_PLACEMENT_3D ( 'NONE', #6028, #8482, #7334 ) ;
#7732=ADVANCED_FACE ( 'NONE', ( #4681 ), #10336, .F. ) ;
#7737=DIRECTION ( 'NONE',  ( 0.000000000000000000, 0.000000000000000000, 1.000000000000000000 ) ) ;
#7738=CARTESIAN_POINT ( 'NONE',  ( -52.77438362643999881, 65.17411849586700612, -145.4984795835769944 ) ) ;
#7740=CIRCLE ( 'NONE', #5255, 2.700000000000001066 ) ;
#7742=VERTEX_POINT ( 'NONE', #11650 ) ;
#7744=FACE_OUTER_BOUND ( 'NONE', #4452, .T. ) ;
#7749=EDGE_CURVE ( 'NONE', #3577, #8760, #5546, .T. ) ;
#7750=DIRECTION ( 'NONE',  ( 0.000000000000000000, 0.000000000000000000, -1.000000000000000000 ) ) ;
#7751=DIRECTION ( 'NONE',  ( 1.000000000000000000, 0.000000000000000000, 0.000000000000000000 ) ) ;
#7752=TOROIDAL_SURFACE ( 'NONE', #10708, 2.700000000000000178, 0.2000000000000000111 ) ;
#7759=ORIENTED_EDGE ( 'NONE', *, *, #14404, .F. ) ;
#7761=EDGE_CURVE ( 'NONE', #6139, #3708, #7692, .T. ) ;
#7765=EDGE_LOOP ( 'NONE', ( #12070, #7445, #7620, #631, #8509, #10215, #10292, #6383, #13115, #11692 ) ) ;
#7766=VECTOR ( 'NONE', #10005, 1000.000000000000000 ) ;
#7767=VERTEX_POINT ( 'NONE', #14061 ) ;
#7773=FACE_OUTER_BOUND ( 'NONE', #5441, .T. ) ;
#7776=CARTESIAN_POINT ( 'NONE',  ( -89.47438362643998744, 65.17411849586700612, -145.2984795835770058 ) ) ;
#7780=ORIENTED_EDGE ( 'NONE', *, *, #8692, .F. ) ;
#7781=DIRECTION ( 'NONE',  ( 0.000000000000000000, 1.000000000000000000, 0.000000000000000000 ) ) ;
#7782=ORIENTED_EDGE ( 'NONE', *, *, #8922, .F. ) ;
#7783=EDGE_LOOP ( 'NONE', ( #12156, #10996, #5998, #2043, #13604, #2638 ) ) ;
#7784=ORIENTED_EDGE ( 'NONE', *, *, #2147, .T. ) ;
#7788=FACE_OUTER_BOUND ( 'NONE', #13453, .T. ) ;
#7789=DIRECTION ( 'NONE',  ( 0.000000000000000000, 0.000000000000000000, 1.000000000000000000 ) ) ;
#7790=DIRECTION ( 'NONE',  ( -1.000000000000000000, 0.000000000000000000, 0.000000000000000000 ) ) ;
#7791=LINE ( 'NONE', #7649, #1672 ) ;
#7792=CARTESIAN_POINT ( 'NONE',  ( -70.45539183192724408, 75.17411849586700612, -44.02377680093038492 ) ) ;
#7793=EDGE_CURVE ( 'NONE', #3281, #10624, #3913, .T. ) ;
#7794=FACE_OUTER_BOUND ( 'NONE', #10423, .T. ) ;
#7797=AXIS2_PLACEMENT_3D ( 'NONE', #13027, #6058, #7209 ) ;
#7799=ADVANCED_FACE ( 'NONE', ( #3429 ), #13579, .F. ) ;
#7800=AXIS2_PLACEMENT_3D ( 'NONE', #7287, #1143, #12091 ) ;
#7801=EDGE_LOOP ( 'NONE', ( #9264, #6000, #7581, #6440 ) ) ;
#7802=VERTEX_POINT ( 'NONE', #1018 ) ;
#7804=ORIENTED_EDGE ( 'NONE', *, *, #1640, .F. ) ;
#7805=LINE ( 'NONE', #8808, #13902 ) ;
#7807=FACE_OUTER_BOUND ( 'NONE', #228, .T. ) ;
#7812=DIRECTION ( 'NONE',  ( 1.000000000000000000, 0.000000000000000000, 0.000000000000000000 ) ) ;
#7814=EDGE_LOOP ( 'NONE', ( #12239, #5094, #3278, #2557 ) ) ;
#7815=AXIS2_PLACEMENT_3D ( 'NONE', #508, #9733, #577 ) ;
#7816=DIRECTION ( 'NONE',  ( 0.8660254037844383745, -0.5000000000000003331, 0.000000000000000000 ) ) ;
#7820=EDGE_CURVE ( 'NONE', #9398, #6550, #5061, .T. ) ;
#7822=VECTOR ( 'NONE', #6268, 1000.000000000000000 ) ;
#7824=CARTESIAN_POINT ( 'NONE',  ( -52.77438362644000591, 65.17411849586700612, -86.49847958357699440 ) ) ;
#7828=EDGE_CURVE ( 'NONE', #8472, #11860, #14068, .T. ) ;
#7831=ORIENTED_EDGE ( 'NONE', *, *, #416, .F. ) ;
#7834=ORIENTED_EDGE ( 'NONE', *, *, #2795, .F. ) ;
#7835=VERTEX_POINT ( 'NONE', #13289 ) ;
#7836=VECTOR ( 'NONE', #4130, 1000.000000000000000 ) ;
#7837=EDGE_LOOP ( 'NONE', ( #5320, #9209, #1832, #1545 ) ) ;
#7841=ADVANCED_FACE ( 'NONE', ( #4834 ), #14559, .T. ) ;
#7842=VECTOR ( 'NONE', #8481, 1000.000000000000114 ) ;
#7846=ADVANCED_FACE ( 'NONE', ( #14129 ), #9623, .F. ) ;
#7850=AXIS2_PLACEMENT_3D ( 'NONE', #9823, #3486, #5023 ) ;
#7851=DIRECTION ( 'NONE',  ( 1.224646799147351975E-16, 1.000000000000000000, 0.000000000000000000 ) ) ;
#7858=EDGE_LOOP ( 'NONE', ( #14312, #10370 ) ) ;
#7860=AXIS2_PLACEMENT_3D ( 'NONE', #11447, #7737, #14852 ) ;
#7862=CARTESIAN_POINT ( 'NONE',  ( -38.27438362644000591, 111.1741184958670061, -67.49847958357700861 ) ) ;
#7865=CARTESIAN_POINT ( 'NONE',  ( -52.77438362644100067, 101.5320169952374414, -147.9984795835769944 ) ) ;
#7869=ORIENTED_EDGE ( 'NONE', *, *, #12101, .T. ) ;
#7870=LINE ( 'NONE', #4072, #13063 ) ;
#7871=EDGE_LOOP ( 'NONE', ( #14480, #10108, #612 ) ) ;
#7872=CONICAL_SURFACE ( 'NONE', #4648, 2.042000000000002036, 1.047197551196596965 ) ;
#7874=ORIENTED_EDGE ( 'NONE', *, *, #10334, .T. ) ;
#7876=ORIENTED_EDGE ( 'NONE', *, *, #14799, .T. ) ;
#7878=DIRECTION ( 'NONE',  ( -1.000000000000000000, 0.000000000000000000, 0.000000000000000000 ) ) ;
#7879=EDGE_CURVE ( 'NONE', #4260, #6663, #7399, .T. ) ;
#7880=DIRECTION ( 'NONE',  ( -1.000000000000000000, 0.000000000000000000, 0.000000000000000000 ) ) ;
#7883=CARTESIAN_POINT ( 'NONE',  ( -50.27438362644100067, 59.67411849586700612, -79.59847958357700293 ) ) ;
#7887=ORIENTED_EDGE ( 'NONE', *, *, #12089, .F. ) ;
#7888=AXIS2_PLACEMENT_3D ( 'NONE', #2883, #14739, #4125 ) ;
#7891=EDGE_CURVE ( 'NONE', #7923, #6403, #7146, .T. ) ;
#7892=PLANE ( 'NONE',  #3005 ) ;
#7895=CIRCLE ( 'NONE', #9616, 4.500000000000003553 ) ;
#7898=CARTESIAN_POINT ( 'NONE',  ( -69.77438362644001302, 82.17411849586700612, -3.496191900462991775 ) ) ;
#7902=ORIENTED_EDGE ( 'NONE', *, *, #3372, .T. ) ;
#7906=EDGE_LOOP ( 'NONE', ( #10925, #9203, #7558, #11151 ) ) ;
#7908=ADVANCED_FACE ( 'NONE', ( #14430 ), #6174, .F. ) ;
#7912=CARTESIAN_POINT ( 'NONE',  ( -86.77438362643999881, 65.17411849586700612, -145.2984795835770058 ) ) ;
#7915=DIRECTION ( 'NONE',  ( -1.000000000000000000, 0.000000000000000000, 0.000000000000000000 ) ) ;
#7917=DIRECTION ( 'NONE',  ( 0.000000000000000000, 0.000000000000000000, 1.000000000000000000 ) ) ;
#7920=FACE_OUTER_BOUND ( 'NONE', #2558, .T. ) ;
#7921=ORIENTED_EDGE ( 'NONE', *, *, #14987, .T. ) ;
#7922=EDGE_LOOP ( 'NONE', ( #3870, #14969, #12923, #1929 ) ) ;
#7923=VERTEX_POINT ( 'NONE', #11813 ) ;
#7926=DIRECTION ( 'NONE',  ( 1.000000000000000000, 0.000000000000000000, 0.000000000000000000 ) ) ;
#7928=EDGE_CURVE ( 'NONE', #13728, #5260, #13209, .T. ) ;
#7929=EDGE_CURVE ( 'NONE', #11895, #13653, #9099, .T. ) ;
#7932=DIRECTION ( 'NONE',  ( 0.000000000000000000, 0.000000000000000000, -1.000000000000000000 ) ) ;
#7935=CARTESIAN_POINT ( 'NONE',  ( -64.35475059718073965, 66.06115545897766594, -81.84847958357698872 ) ) ;
#7945=DIRECTION ( 'NONE',  ( -0.000000000000000000, -0.000000000000000000, 1.000000000000000000 ) ) ;
#7947=CARTESIAN_POINT ( 'NONE',  ( -52.77438362643999881, 65.17411849586700612, -145.2984795835770058 ) ) ;
#7949=DIRECTION ( 'NONE',  ( -0.000000000000000000, -0.000000000000000000, 1.000000000000000000 ) ) ;
#7952=VECTOR ( 'NONE', #12695, 1000.000000000000000 ) ;
#7957=LINE ( 'NONE', #3305, #7952 ) ;
#7959=LINE ( 'NONE', #6670, #4157 ) ;
#7964=EDGE_CURVE ( 'NONE', #12262, #13840, #1249, .T. ) ;
#7965=DIRECTION ( 'NONE',  ( 0.000000000000000000, 0.000000000000000000, -1.000000000000000000 ) ) ;
#7966=ORIENTED_EDGE ( 'NONE', *, *, #7343, .F. ) ;
#7967=DIRECTION ( 'NONE',  ( -1.000000000000000000, 0.000000000000000000, 0.000000000000000000 ) ) ;
#7969=ORIENTED_EDGE ( 'NONE', *, *, #7997, .T. ) ;
#7982=CARTESIAN_POINT ( 'NONE',  ( -86.77438362644100778, 99.17411849586700612, -182.2484795835770228 ) ) ;
#7984=DIRECTION ( 'NONE',  ( 0.000000000000000000, 0.000000000000000000, -1.000000000000000000 ) ) ;
#7985=CARTESIAN_POINT ( 'NONE',  ( -59.27438362644000591, 82.17411849586700612, -150.4984795835769944 ) ) ;
#7986=EDGE_CURVE ( 'NONE', #8986, #8947, #13517, .T. ) ;
#7987=CARTESIAN_POINT ( 'NONE',  ( -52.77438362643999881, 62.81621999649657084, -147.9984795835769944 ) ) ;
#7989=VERTEX_POINT ( 'NONE', #9855 ) ;
#7990=FACE_OUTER_BOUND ( 'NONE', #11115, .T. ) ;
#7994=ORIENTED_EDGE ( 'NONE', *, *, #6526, .T. ) ;
#7997=EDGE_CURVE ( 'NONE', #11281, #2023, #6406, .T. ) ;
#8002=CARTESIAN_POINT ( 'NONE',  ( -69.77438362644001302, 82.17411849586700612, -85.04847958357700577 ) ) ;
#8003=DIRECTION ( 'NONE',  ( 0.000000000000000000, 0.000000000000000000, -1.000000000000000000 ) ) ;
#8006=EDGE_CURVE ( 'NONE', #13082, #3491, #9352, .T. ) ;
#8007=AXIS2_PLACEMENT_3D ( 'NONE', #6843, #12885, #5922 ) ;
#8009=FACE_OUTER_BOUND ( 'NONE', #3443, .T. ) ;
#8012=EDGE_CURVE ( 'NONE', #11318, #11895, #5421, .T. ) ;
#8014=LINE ( 'NONE', #4378, #15130 ) ;
#8015=VECTOR ( 'NONE', #6241, 1000.000000000000114 ) ;
#8016=VERTEX_POINT ( 'NONE', #12352 ) ;
#8017=VECTOR ( 'NONE', #1928, 1000.000000000000000 ) ;
#8023=DIRECTION ( 'NONE',  ( 0.000000000000000000, 0.000000000000000000, -1.000000000000000000 ) ) ;
#8025=VECTOR ( 'NONE', #3711, 1000.000000000000000 ) ;
#8027=EDGE_CURVE ( 'NONE', #11570, #13566, #195, .T. ) ;
#8030=DIRECTION ( 'NONE',  ( 0.000000000000000000, 0.000000000000000000, -1.000000000000000000 ) ) ;
#8032=EDGE_LOOP ( 'NONE', ( #3171, #5616, #11078, #226 ) ) ;
#8034=ORIENTED_EDGE ( 'NONE', *, *, #10095, .T. ) ;
#8039=LINE ( 'NONE', #743, #519 ) ;
#8041=DIRECTION ( 'NONE',  ( -1.000000000000000000, 0.000000000000000000, 0.000000000000000000 ) ) ;
#8044=DIRECTION ( 'NONE',  ( -1.000000000000000000, 0.000000000000000000, 0.000000000000000000 ) ) ;
#8045=TOROIDAL_SURFACE ( 'NONE', #2139, 11.50000000000000000, 1.000000000000000000 ) ;
#8047=VECTOR ( 'NONE', #8926, 1000.000000000000114 ) ;
#8054=EDGE_LOOP ( 'NONE', ( #4449, #14024, #4089, #10995 ) ) ;
#8057=CIRCLE ( 'NONE', #12525, 1.250000000000001110 ) ;
#8058=DIRECTION ( 'NONE',  ( 0.000000000000000000, 0.000000000000000000, -1.000000000000000000 ) ) ;
#8061=DIRECTION ( 'NONE',  ( 0.000000000000000000, 0.000000000000000000, -1.000000000000000000 ) ) ;
#8064=DIRECTION ( 'NONE',  ( -1.000000000000000000, -1.541976423090494894E-16, 0.000000000000000000 ) ) ;
#8068=CARTESIAN_POINT ( 'NONE',  ( -86.77438362644100778, 99.17411849586700612, -145.4984795835769944 ) ) ;
#8069=ORIENTED_EDGE ( 'NONE', *, *, #14409, .F. ) ;
#8070=LINE ( 'NONE', #5924, #11230 ) ;
#8073=VERTEX_POINT ( 'NONE', #13594 ) ;
#8074=VECTOR ( 'NONE', #5732, 1000.000000000000000 ) ;
#8077=EDGE_CURVE ( 'NONE', #12917, #7621, #10601, .T. ) ;
#8082=LINE ( 'NONE', #942, #6515 ) ;
#8084=AXIS2_PLACEMENT_3D ( 'NONE', #13756, #8939, #9239 ) ;
#8087=CIRCLE ( 'NONE', #5385, 3.000000000000002665 ) ;
#8088=LINE ( 'NONE', #12824, #13751 ) ;
#8089=CARTESIAN_POINT ( 'NONE',  ( -73.13733409597239188, 66.60412428008086749, -81.84847958357697451 ) ) ;
#8091=LINE ( 'NONE', #2265, #10832 ) ;
#8092=ORIENTED_EDGE ( 'NONE', *, *, #4793, .T. ) ;
#8093=ORIENTED_EDGE ( 'NONE', *, *, #13202, .F. ) ;
#8094=DIRECTION ( 'NONE',  ( 0.000000000000000000, 0.000000000000000000, -1.000000000000000000 ) ) ;
#8095=AXIS2_PLACEMENT_3D ( 'NONE', #3916, #1510, #342 ) ;
#8096=ORIENTED_EDGE ( 'NONE', *, *, #1755, .T. ) ;
#8097=VECTOR ( 'NONE', #5828, 1000.000000000000000 ) ;
#8099=ORIENTED_EDGE ( 'NONE', *, *, #6968, .T. ) ;
#8100=EDGE_CURVE ( 'NONE', #1813, #2834, #3180, .T. ) ;
#8102=FACE_OUTER_BOUND ( 'NONE', #10707, .T. ) ;
#8103=EDGE_CURVE ( 'NONE', #191, #389, #9361, .T. ) ;
#8104=CARTESIAN_POINT ( 'NONE',  ( -69.77438362644001302, 82.17411849586700612, -152.4984795835769944 ) ) ;
#8106=CYLINDRICAL_SURFACE ( 'NONE', #8502, 4.499999999999997335 ) ;
#8111=DIRECTION ( 'NONE',  ( 0.000000000000000000, 0.000000000000000000, -1.000000000000000000 ) ) ;
#8112=CYLINDRICAL_SURFACE ( 'NONE', #4019, 1.500000000000001332 ) ;
#8113=EDGE_CURVE ( 'NONE', #4822, #2764, #13837, .T. ) ;
#8115=ORIENTED_EDGE ( 'NONE', *, *, #13338, .T. ) ;
#8119=EDGE_CURVE ( 'NONE', #14049, #1813, #12841, .T. ) ;
#8123=EDGE_CURVE ( 'NONE', #1795, #14279, #3675, .T. ) ;
#8124=ADVANCED_FACE ( 'NONE', ( #2167 ), #11562, .F. ) ;
#8125=DIRECTION ( 'NONE',  ( 1.000000000000000000, 0.000000000000000000, 0.000000000000000000 ) ) ;
#8126=CARTESIAN_POINT ( 'NONE',  ( -48.27438362644000591, 99.17411849586700612, -86.49847958357699440 ) ) ;
#8127=DIRECTION ( 'NONE',  ( 0.000000000000000000, -0.000000000000000000, 1.000000000000000000 ) ) ;
#8129=FACE_OUTER_BOUND ( 'NONE', #12889, .T. ) ;
#8134=VERTEX_POINT ( 'NONE', #14960 ) ;
#8135=ORIENTED_EDGE ( 'NONE', *, *, #6475, .F. ) ;
#8138=EDGE_LOOP ( 'NONE', ( #3710, #7780, #12326, #9173, #5222 ) ) ;
#8141=CYLINDRICAL_SURFACE ( 'NONE', #9261, 10.49999999999999467 ) ;
#8143=CARTESIAN_POINT ( 'NONE',  ( -69.77438362644001302, 82.17411849586700612, -79.49847958357700861 ) ) ;
#8147=DIRECTION ( 'NONE',  ( -1.000000000000000000, 0.000000000000000000, 0.000000000000000000 ) ) ;
#8148=DIRECTION ( 'NONE',  ( 1.224646799147351975E-16, 1.000000000000000000, 0.000000000000000000 ) ) ;
#8153=DIRECTION ( 'NONE',  ( 0.000000000000000000, 0.000000000000000000, -1.000000000000000000 ) ) ;
#8154=VERTEX_POINT ( 'NONE', #6840 ) ;
#8156=ORIENTED_EDGE ( 'NONE', *, *, #5277, .F. ) ;
#8159=CARTESIAN_POINT ( 'NONE',  ( -50.07438362644099783, 99.17411849586700612, -145.4984795835769944 ) ) ;
#8160=CARTESIAN_POINT ( 'NONE',  ( -62.02799568714584666, 164.3482369917340122, -79.59847958357700293 ) ) ;
#8161=CARTESIAN_POINT ( 'NONE',  ( -73.13733409597239188, 66.60412428008086749, -83.44847958357698303 ) ) ;
#8164=CARTESIAN_POINT ( 'NONE',  ( -86.77438362644001302, 99.17411849586700612, -145.4984795835769660 ) ) ;
#8165=DIRECTION ( 'NONE',  ( -1.000000000000000000, 0.000000000000000000, 0.000000000000000000 ) ) ;
#8167=EDGE_LOOP ( 'NONE', ( #3887, #10605 ) ) ;
#8168=CYLINDRICAL_SURFACE ( 'NONE', #6876, 16.06499999999999773 ) ;
#8173=EDGE_LOOP ( 'NONE', ( #9365, #275, #9572, #15222 ) ) ;
#8179=FACE_BOUND ( 'NONE', #8491, .T. ) ;
#8181=CARTESIAN_POINT ( 'NONE',  ( -86.77438362643999881, 65.17411849586700612, -182.2484795835770228 ) ) ;
#8182=VERTEX_POINT ( 'NONE', #5605 ) ;
#8183=LINE ( 'NONE', #8260, #4887 ) ;
#8186=VERTEX_POINT ( 'NONE', #4352 ) ;
#8191=CARTESIAN_POINT ( 'NONE',  ( -69.77438362644001302, 79.67411849586700612, -51.99847958357699440 ) ) ;
#8193=EDGE_CURVE ( 'NONE', #13653, #2626, #11851, .T. ) ;
#8195=DIRECTION ( 'NONE',  ( -2.065146995210485003E-17, -4.130293990420970006E-17, -1.000000000000000000 ) ) ;
#8197=LINE ( 'NONE', #1214, #1951 ) ;
#8199=EDGE_CURVE ( 'NONE', #7742, #5984, #1444, .T. ) ;
#8200=DIRECTION ( 'NONE',  ( -1.000000000000000000, 0.000000000000000000, 0.000000000000000000 ) ) ;
#8201=VECTOR ( 'NONE', #7376, 1000.000000000000114 ) ;
#8202=EDGE_LOOP ( 'NONE', ( #15275, #5420 ) ) ;
#8203=CARTESIAN_POINT ( 'NONE',  ( -69.77438362644001302, 82.17411849586700612, -152.4984795835769944 ) ) ;
#8204=ORIENTED_EDGE ( 'NONE', *, *, #6232, .F. ) ;
#8206=ORIENTED_EDGE ( 'NONE', *, *, #8298, .F. ) ;
#8207=EDGE_CURVE ( 'NONE', #7422, #13506, #3251, .T. ) ;
#8208=EDGE_LOOP ( 'NONE', ( #9083, #6367, #14087, #15312, #14197, #10776, #6880, #12339, #2543, #5927, #4718, #12785, #9919, #6327, #12282, #13448, #6744, #14724, #2813, #4990, #4188 ) ) ;
#8209=ORIENTED_EDGE ( 'NONE', *, *, #6046, .F. ) ;
#8210=VERTEX_POINT ( 'NONE', #13957 ) ;
#8211=AXIS2_PLACEMENT_3D ( 'NONE', #11191, #6478, #6640 ) ;
#8213=CARTESIAN_POINT ( 'NONE',  ( -52.77438362644000591, 65.17411849586700612, -79.59847958357700293 ) ) ;
#8218=CARTESIAN_POINT ( 'NONE',  ( -62.02799568714584666, 60.67411849586701322, -152.4984795835769944 ) ) ;
#8222=EDGE_CURVE ( 'NONE', #13652, #9914, #2091, .T. ) ;
#8225=CIRCLE ( 'NONE', #1286, 4.500000000000003553 ) ;
#8227=DIRECTION ( 'NONE',  ( 1.000000000000000000, 0.000000000000000000, 0.000000000000000000 ) ) ;
#8228=ORIENTED_EDGE ( 'NONE', *, *, #14693, .F. ) ;
#8231=ORIENTED_EDGE ( 'NONE', *, *, #8027, .F. ) ;
#8234=VECTOR ( 'NONE', #14638, 1000.000000000000000 ) ;
#8237=DIRECTION ( 'NONE',  ( 0.000000000000000000, 0.000000000000000000, -1.000000000000000000 ) ) ;
#8238=CARTESIAN_POINT ( 'NONE',  ( -84.07438362644101915, 99.17411849586700612, -145.2984795835770058 ) ) ;
#8239=DIRECTION ( 'NONE',  ( 0.000000000000000000, 1.000000000000000000, 0.000000000000000000 ) ) ;
#8240=CARTESIAN_POINT ( 'NONE',  ( -42.77438362644000591, 59.67411849586700612, -79.59847958357700293 ) ) ;
#8241=DIRECTION ( 'NONE',  ( -1.000000000000000000, 0.000000000000000000, 0.000000000000000000 ) ) ;
#8242=CIRCLE ( 'NONE', #555, 4.500000000000003553 ) ;
#8244=EDGE_LOOP ( 'NONE', ( #4547, #6420, #10089, #7577 ) ) ;
#8245=PLANE ( 'NONE',  #672 ) ;
#8247=ORIENTED_EDGE ( 'NONE', *, *, #6427, .F. ) ;
#8252=AXIS2_PLACEMENT_3D ( 'NONE', #6697, #11112, #14669 ) ;
#8254=DIRECTION ( 'NONE',  ( 0.000000000000000000, 0.000000000000000000, 1.000000000000000000 ) ) ;
#8255=VECTOR ( 'NONE', #8732, 1000.000000000000000 ) ;
#8256=DIRECTION ( 'NONE',  ( 1.287488025362404182E-15, 1.000000000000000000, 0.000000000000000000 ) ) ;
#8259=ORIENTED_EDGE ( 'NONE', *, *, #3658, .T. ) ;
#8260=CARTESIAN_POINT ( 'NONE',  ( -48.27438362644000591, 65.17411849586700612, -145.4984795835769660 ) ) ;
#8263=FACE_OUTER_BOUND ( 'NONE', #4803, .T. ) ;
#8265=CIRCLE ( 'NONE', #10994, 4.499999999999997335 ) ;
#8269=EDGE_LOOP ( 'NONE', ( #6382, #15007, #13465, #5206 ) ) ;
#8274=AXIS2_PLACEMENT_3D ( 'NONE', #2535, #3780, #12942 ) ;
#8277=DIRECTION ( 'NONE',  ( 1.000000000000000000, 0.000000000000000000, 0.000000000000000000 ) ) ;
#8278=DIRECTION ( 'NONE',  ( 1.000000000000000000, 0.000000000000000000, 0.000000000000000000 ) ) ;
#8280=VERTEX_POINT ( 'NONE', #4964 ) ;
#8281=CARTESIAN_POINT ( 'NONE',  ( -91.27438362643999881, 65.17411849586700612, -145.4984795835769660 ) ) ;
#8282=VECTOR ( 'NONE', #12099, 1000.000000000000000 ) ;
#8283=AXIS2_PLACEMENT_3D ( 'NONE', #976, #8195, #15087 ) ;
#8291=DIRECTION ( 'NONE',  ( 0.000000000000000000, 0.000000000000000000, -1.000000000000000000 ) ) ;
#8292=EDGE_CURVE ( 'NONE', #8472, #7286, #11868, .T. ) ;
#8294=AXIS2_PLACEMENT_3D ( 'NONE', #10053, #453, #6587 ) ;
#8296=CARTESIAN_POINT ( 'NONE',  ( -78.12438362644000733, 82.17411849586700612, -80.14847958357698587 ) ) ;
#8298=EDGE_CURVE ( 'NONE', #6139, #3101, #14113, .T. ) ;
#8300=CARTESIAN_POINT ( 'NONE',  ( -62.02799568714584666, 110.1741184958670061, -79.59847958357700293 ) ) ;
#8301=CIRCLE ( 'NONE', #14248, 0.1999999999999987899 ) ;
#8302=FACE_BOUND ( 'NONE', #7245, .T. ) ;
#8304=CARTESIAN_POINT ( 'NONE',  ( -86.77438362644001302, 99.17411849586700612, -145.4984795835769660 ) ) ;
#8306=LINE ( 'NONE', #153, #344 ) ;
#8307=ORIENTED_EDGE ( 'NONE', *, *, #11227, .F. ) ;
#8308=EDGE_CURVE ( 'NONE', #3516, #11145, #9116, .T. ) ;
#8312=CIRCLE ( 'NONE', #12535, 2.000000000000001776 ) ;
#8313=CARTESIAN_POINT ( 'NONE',  ( -83.02438362644100778, 99.17411849586700612, -150.4984795835770228 ) ) ;
#8314=CIRCLE ( 'NONE', #1621, 3.750000000000003553 ) ;
#8317=LINE ( 'NONE', #13062, #1407 ) ;
#8319=CARTESIAN_POINT ( 'NONE',  ( -101.2743836264399988, 60.67411849586700612, -15.85886927678779834 ) ) ;
#8320=DIRECTION ( 'NONE',  ( 0.000000000000000000, 0.7071067811865441310, -0.7071067811865510144 ) ) ;
#8321=DIRECTION ( 'NONE',  ( 0.000000000000000000, 0.000000000000000000, 1.000000000000000000 ) ) ;
#8322=CARTESIAN_POINT ( 'NONE',  ( -69.77438362643999881, 89.17411849586052597, -43.99847958364157563 ) ) ;
#8324=DIRECTION ( 'NONE',  ( -1.000000000000000000, 0.000000000000000000, 0.000000000000000000 ) ) ;
#8325=CARTESIAN_POINT ( 'NONE',  ( -69.77438362644001302, 82.17411849586700612, -79.59847958357700293 ) ) ;
#8327=AXIS2_PLACEMENT_3D ( 'NONE', #14305, #7024, #11750 ) ;
#8329=VECTOR ( 'NONE', #445, 1000.000000000000000 ) ;
#8330=FACE_OUTER_BOUND ( 'NONE', #6885, .T. ) ;
#8331=VERTEX_POINT ( 'NONE', #8218 ) ;
#8341=CIRCLE ( 'NONE', #15002, 4.500000000000003553 ) ;
#8342=CYLINDRICAL_SURFACE ( 'NONE', #8961, 4.250000000000003553 ) ;
#8343=FACE_OUTER_BOUND ( 'NONE', #13600, .T. ) ;
#8344=FACE_OUTER_BOUND ( 'NONE', #4704, .T. ) ;
#8345=DIRECTION ( 'NONE',  ( 0.000000000000000000, 1.000000000000000000, 0.000000000000000000 ) ) ;
#8346=ORIENTED_EDGE ( 'NONE', *, *, #8077, .F. ) ;
#8352=ORIENTED_EDGE ( 'NONE', *, *, #5065, .F. ) ;
#8356=VECTOR ( 'NONE', #10033, 1000.000000000000000 ) ;
#8359=LINE ( 'NONE', #11847, #5942 ) ;
#8361=CARTESIAN_POINT ( 'NONE',  ( -52.77438362644000591, 99.17411849586700612, -145.4984795835769660 ) ) ;
#8362=ORIENTED_EDGE ( 'NONE', *, *, #10152, .T. ) ;
#8363=LINE ( 'NONE', #15326, #12490 ) ;
#8366=ORIENTED_EDGE ( 'NONE', *, *, #14252, .F. ) ;
#8367=VECTOR ( 'NONE', #15127, 1000.000000000000000 ) ;
#8368=FACE_OUTER_BOUND ( 'NONE', #3212, .T. ) ;
#8373=EDGE_LOOP ( 'NONE', ( #6182, #3403, #12888, #14106 ) ) ;
#8377=CARTESIAN_POINT ( 'NONE',  ( -90.85838362644101096, 99.17411849586700612, -147.9984795835769944 ) ) ;
#8378=CONICAL_SURFACE ( 'NONE', #3422, 3.750000000000003553, 0.7853981633974476129 ) ;
#8379=DIRECTION ( 'NONE',  ( 0.000000000000000000, 0.000000000000000000, -1.000000000000000000 ) ) ;
#8380=CARTESIAN_POINT ( 'NONE',  ( 0.000000000000000000, 0.000000000000000000, -79.59847958357700293 ) ) ;
#8383=DIRECTION ( 'NONE',  ( 0.000000000000000000, 0.000000000000000000, -1.000000000000000000 ) ) ;
#8384=ORIENTED_EDGE ( 'NONE', *, *, #3372, .F. ) ;
#8385=CARTESIAN_POINT ( 'NONE',  ( -50.73238362643999722, 66.35306774555222376, -147.9984795835769944 ) ) ;
#8386=ADVANCED_FACE ( 'NONE', ( #9448 ), #5669, .T. ) ;
#8390=ADVANCED_FACE ( 'NONE', ( #14338 ), #7380, .T. ) ;
#8393=DIRECTION ( 'NONE',  ( 1.000000000000000000, 0.000000000000000000, 0.000000000000000000 ) ) ;
#8395=ADVANCED_FACE ( 'NONE', ( #1232 ), #3714, .F. ) ;
#8396=CARTESIAN_POINT ( 'NONE',  ( -69.77438362644001302, 82.17411849586700612, -112.9984795835769944 ) ) ;
#8397=DIRECTION ( 'NONE',  ( 0.000000000000000000, -0.000000000000000000, 1.000000000000000000 ) ) ;
#8398=DIRECTION ( 'NONE',  ( 0.8660254037844383745, -0.5000000000000003331, 0.000000000000000000 ) ) ;
#8402=ORIENTED_EDGE ( 'NONE', *, *, #8838, .F. ) ;
#8405=ORIENTED_EDGE ( 'NONE', *, *, #8867, .F. ) ;
#8408=ADVANCED_FACE ( 'NONE', ( #8443 ), #5991, .F. ) ;
#8410=ORIENTED_EDGE ( 'NONE', *, *, #8123, .F. ) ;
#8413=LINE ( 'NONE', #4769, #15243 ) ;
#8414=DIRECTION ( 'NONE',  ( -1.000000000000000000, 0.000000000000000000, 0.000000000000000000 ) ) ;
#8420=VERTEX_POINT ( 'NONE', #11942 ) ;
#8421=CARTESIAN_POINT ( 'NONE',  ( -69.77438362644001302, 84.67411849586700612, -67.69567958357700377 ) ) ;
#8425=DIRECTION ( 'NONE',  ( 0.000000000000000000, 0.000000000000000000, -1.000000000000000000 ) ) ;
#8426=DIRECTION ( 'NONE',  ( 0.000000000000000000, 0.000000000000000000, -1.000000000000000000 ) ) ;
#8428=DIRECTION ( 'NONE',  ( -1.000000000000000000, 0.000000000000000000, 0.000000000000000000 ) ) ;
#8430=ORIENTED_EDGE ( 'NONE', *, *, #10582, .F. ) ;
#8433=CARTESIAN_POINT ( 'NONE',  ( -64.53565528768383786, 67.29799558322736175, -83.44847958357698303 ) ) ;
#8436=VERTEX_POINT ( 'NONE', #2634 ) ;
#8439=CARTESIAN_POINT ( 'NONE',  ( -73.64736697264332577, 89.17411849586700612, -58.99847958357700151 ) ) ;
#8441=CARTESIAN_POINT ( 'NONE',  ( -84.73238362644100619, 100.3530677455522238, -147.9984795835769944 ) ) ;
#8442=CIRCLE ( 'NONE', #2750, 8.000000000000007105 ) ;
#8443=FACE_OUTER_BOUND ( 'NONE', #3157, .T. ) ;
#8446=ADVANCED_FACE ( 'NONE', ( #9837 ), #8378, .T. ) ;
#8449=VERTEX_POINT ( 'NONE', #5198 ) ;
#8450=CARTESIAN_POINT ( 'NONE',  ( -69.77438362644001302, 84.67411849586700612, -43.99847958357699440 ) ) ;
#8451=ORIENTED_EDGE ( 'NONE', *, *, #9530, .F. ) ;
#8452=CIRCLE ( 'NONE', #7723, 17.00000000000000000 ) ;
#8454=ORIENTED_EDGE ( 'NONE', *, *, #8600, .T. ) ;
#8455=ORIENTED_EDGE ( 'NONE', *, *, #6623, .F. ) ;
#8456=VECTOR ( 'NONE', #14675, 1000.000000000000000 ) ;
#8460=CARTESIAN_POINT ( 'NONE',  ( -69.77438362644001302, 82.17411849586700612, -138.4984795835769944 ) ) ;
#8462=ADVANCED_FACE ( 'NONE', ( #3013 ), #6517, .F. ) ;
#8465=DIRECTION ( 'NONE',  ( 0.000000000000000000, 0.000000000000000000, -1.000000000000000000 ) ) ;
#8467=CARTESIAN_POINT ( 'NONE',  ( -65.90140028023257912, 89.17411849586700612, -29.37106258560738681 ) ) ;
#8468=DIRECTION ( 'NONE',  ( 0.000000000000000000, 0.000000000000000000, -1.000000000000000000 ) ) ;
#8470=CARTESIAN_POINT ( 'NONE',  ( -69.77438362644001302, 82.17411849586700612, -67.69567958357700377 ) ) ;
#8472=VERTEX_POINT ( 'NONE', #5352 ) ;
#8475=AXIS2_PLACEMENT_3D ( 'NONE', #6856, #2107, #2255 ) ;
#8476=EDGE_CURVE ( 'NONE', #10367, #9170, #7415, .T. ) ;
#8481=DIRECTION ( 'NONE',  ( 0.8660254037844383745, -0.5000000000000003331, 0.000000000000000000 ) ) ;
#8482=DIRECTION ( 'NONE',  ( 0.000000000000000000, 0.000000000000000000, 1.000000000000000000 ) ) ;
#8485=DIRECTION ( 'NONE',  ( 0.000000000000000000, 0.000000000000000000, -1.000000000000000000 ) ) ;
#8491=EDGE_LOOP ( 'NONE', ( #9729, #4394, #8627, #3803, #12792, #5903 ) ) ;
#8492=DIRECTION ( 'NONE',  ( 0.000000000000000000, 0.000000000000000000, 1.000000000000000000 ) ) ;
#8493=CIRCLE ( 'NONE', #11964, 16.00000000000000000 ) ;
#8494=ORIENTED_EDGE ( 'NONE', *, *, #689, .F. ) ;
#8497=VERTEX_POINT ( 'NONE', #12405 ) ;
#8502=AXIS2_PLACEMENT_3D ( 'NONE', #12842, #10498, #2205 ) ;
#8503=FACE_OUTER_BOUND ( 'NONE', #538, .T. ) ;
#8504=AXIS2_PLACEMENT_3D ( 'NONE', #2810, #4135, #13601 ) ;
#8506=DIRECTION ( 'NONE',  ( 0.5000000000000003331, 0.8660254037844384856, 0.000000000000000000 ) ) ;
#8508=CARTESIAN_POINT ( 'NONE',  ( -52.77438362644100067, 99.17411849586700612, -150.4984795835770228 ) ) ;
#8509=ORIENTED_EDGE ( 'NONE', *, *, #12089, .T. ) ;
#8510=CARTESIAN_POINT ( 'NONE',  ( -52.77438362644100067, 99.17411849586700612, -147.9984795835769944 ) ) ;
#8512=ORIENTED_EDGE ( 'NONE', *, *, #6202, .F. ) ;
#8516=ORIENTED_EDGE ( 'NONE', *, *, #8113, .T. ) ;
#8517=CIRCLE ( 'NONE', #6062, 2.042000000000002036 ) ;
#8520=DIRECTION ( 'NONE',  ( -0.000000000000000000, -0.000000000000000000, 1.000000000000000000 ) ) ;
#8522=LINE ( 'NONE', #144, #13491 ) ;
#8523=CARTESIAN_POINT ( 'NONE',  ( -69.77438362644001302, 82.17411849586700612, -83.44847958357698303 ) ) ;
#8524=FACE_OUTER_BOUND ( 'NONE', #5257, .T. ) ;
#8525=AXIS2_PLACEMENT_3D ( 'NONE', #11250, #1634, #6385 ) ;
#8528=LINE ( 'NONE', #2637, #6084 ) ;
#8530=LINE ( 'NONE', #8385, #7022 ) ;
#8531=ORIENTED_EDGE ( 'NONE', *, *, #5246, .F. ) ;
#8532=EDGE_LOOP ( 'NONE', ( #8860, #29 ) ) ;
#8534=ORIENTED_EDGE ( 'NONE', *, *, #14226, .T. ) ;
#8535=LINE ( 'NONE', #9849, #2837 ) ;
#8536=AXIS2_PLACEMENT_3D ( 'NONE', #14481, #2621, #11931 ) ;
#8538=EDGE_CURVE ( 'NONE', #12177, #3363, #11863, .T. ) ;
#8539=VECTOR ( 'NONE', #3276, 1000.000000000000000 ) ;
#8540=CARTESIAN_POINT ( 'NONE',  ( -104.2743836264399988, 0.000000000000000000, 0.000000000000000000 ) ) ;
#8541=PLANE ( 'NONE',  #12687 ) ;
#8543=DIRECTION ( 'NONE',  ( -1.000000000000000000, -1.196012985618917554E-12, 0.000000000000000000 ) ) ;
#8544=DIRECTION ( 'NONE',  ( 0.8660254037844383745, -0.5000000000000003331, 0.000000000000000000 ) ) ;
#8548=ORIENTED_EDGE ( 'NONE', *, *, #4419, .F. ) ;
#8550=ORIENTED_EDGE ( 'NONE', *, *, #5452, .F. ) ;
#8551=VECTOR ( 'NONE', #13607, 1000.000000000000000 ) ;
#8553=VECTOR ( 'NONE', #5379, 1000.000000000000114 ) ;
#8555=ADVANCED_FACE ( 'NONE', ( #5663, #827 ), #15015, .T. ) ;
#8558=EDGE_CURVE ( 'NONE', #10234, #11568, #6189, .T. ) ;
#8559=DIRECTION ( 'NONE',  ( 0.000000000000000000, -1.000000000000000000, 0.000000000000000000 ) ) ;
#8563=AXIS2_PLACEMENT_3D ( 'NONE', #9579, #4492, #10908 ) ;
#8565=CIRCLE ( 'NONE', #1879, 2.042000000000002036 ) ;
#8569=VECTOR ( 'NONE', #13213, 1000.000000000000000 ) ;
#8579=CARTESIAN_POINT ( 'NONE',  ( -86.77438362643999881, 62.81621999649657084, -147.9984795835769944 ) ) ;
#8581=LINE ( 'NONE', #12389, #4035 ) ;
#8583=CIRCLE ( 'NONE', #5622, 6.999999999974082954 ) ;
#8584=CARTESIAN_POINT ( 'NONE',  ( -52.77438362644100067, 99.17411849586700612, -150.4984795835770228 ) ) ;
#8588=DIRECTION ( 'NONE',  ( 1.000000000000000000, 0.000000000000000000, 0.000000000000000000 ) ) ;
#8594=ORIENTED_EDGE ( 'NONE', *, *, #14629, .F. ) ;
#8595=ORIENTED_EDGE ( 'NONE', *, *, #4620, .F. ) ;
#8600=EDGE_CURVE ( 'NONE', #3986, #1856, #11540, .T. ) ;
#8601=CIRCLE ( 'NONE', #4890, 4.499999999999997335 ) ;
#8602=EDGE_CURVE ( 'NONE', #2078, #1481, #13361, .T. ) ;
#8604=CARTESIAN_POINT ( 'NONE',  ( -69.77438362644001302, 82.17411849586700612, -138.4984795835769944 ) ) ;
#8607=CARTESIAN_POINT ( 'NONE',  ( -54.81638362644100226, 97.99516924618178848, -147.9984795835769944 ) ) ;
#8610=EDGE_LOOP ( 'NONE', ( #5005, #14441, #7019, #9096, #13335 ) ) ;
#8611=DIRECTION ( 'NONE',  ( -1.000000000000000000, 0.000000000000000000, 0.000000000000000000 ) ) ;
#8612=ORIENTED_EDGE ( 'NONE', *, *, #416, .T. ) ;
#8613=ORIENTED_EDGE ( 'NONE', *, *, #11226, .F. ) ;
#8614=ORIENTED_EDGE ( 'NONE', *, *, #10146, .F. ) ;
#8615=ORIENTED_EDGE ( 'NONE', *, *, #620, .F. ) ;
#8616=( NAMED_UNIT ( * ) PLANE_ANGLE_UNIT ( ) SI_UNIT ( $, .RADIAN. ) );
#8618=LINE ( 'NONE', #9691, #11703 ) ;
#8620=DIRECTION ( 'NONE',  ( 1.000000000000000000, 0.000000000000000000, 0.000000000000000000 ) ) ;
#8621=DIRECTION ( 'NONE',  ( -1.000000000000000000, 0.000000000000000000, 0.000000000000000000 ) ) ;
#8627=ORIENTED_EDGE ( 'NONE', *, *, #5370, .T. ) ;
#8629=ORIENTED_EDGE ( 'NONE', *, *, #11135, .T. ) ;
#8631=CARTESIAN_POINT ( 'NONE',  ( -72.45546847960517312, 89.83357606928413475, -58.65793715699411592 ) ) ;
#8634=FACE_OUTER_BOUND ( 'NONE', #1130, .T. ) ;
#8643=ORIENTED_EDGE ( 'NONE', *, *, #10286, .T. ) ;
#8644=VECTOR ( 'NONE', #2924, 1000.000000000000000 ) ;
#8645=( NAMED_UNIT ( * ) SI_UNIT ( $, .STERADIAN. ) SOLID_ANGLE_UNIT ( ) );
#8650=DIRECTION ( 'NONE',  ( 3.996802888650560011E-13, -1.000000000000000000, 0.000000000000000000 ) ) ;
#8652=EDGE_CURVE ( 'NONE', #6998, #13840, #1455, .T. ) ;
#8655=DIRECTION ( 'NONE',  ( 0.000000000000000000, 0.000000000000000000, -1.000000000000000000 ) ) ;
#8657=CARTESIAN_POINT ( 'NONE',  ( -90.85838362644000199, 65.17411849586700612, -147.9984795835769944 ) ) ;
#8658=EDGE_CURVE ( 'NONE', #10868, #2784, #8359, .T. ) ;
#8661=ORIENTED_EDGE ( 'NONE', *, *, #7820, .F. ) ;
#8662=ORIENTED_EDGE ( 'NONE', *, *, #12434, .F. ) ;
#8665=ORIENTED_EDGE ( 'NONE', *, *, #3849, .T. ) ;
#8666=ORIENTED_EDGE ( 'NONE', *, *, #4326, .F. ) ;
#8669=ADVANCED_FACE ( 'NONE', ( #11768 ), #14098, .F. ) ;
#8671=FACE_OUTER_BOUND ( 'NONE', #2788, .T. ) ;
#8673=PLANE ( 'NONE',  #9262 ) ;
#8676=CARTESIAN_POINT ( 'NONE',  ( -87.79538362643998539, 66.94254237039483257, -147.9984795835769944 ) ) ;
#8677=EDGE_CURVE ( 'NONE', #7517, #1574, #1369, .T. ) ;
#8678=FACE_OUTER_BOUND ( 'NONE', #14767, .T. ) ;
#8681=DIRECTION ( 'NONE',  ( 0.000000000000000000, 0.000000000000000000, 1.000000000000000000 ) ) ;
#8684=ORIENTED_EDGE ( 'NONE', *, *, #1189, .T. ) ;
#8685=EDGE_LOOP ( 'NONE', ( #7831, #3956, #3078 ) ) ;
#8686=ORIENTED_EDGE ( 'NONE', *, *, #15198, .T. ) ;
#8689=CARTESIAN_POINT ( 'NONE',  ( -50.73238362644099197, 100.3530677455522238, -147.9984795835769944 ) ) ;
#8692=EDGE_CURVE ( 'NONE', #15148, #10983, #8197, .T. ) ;
#8696=DIRECTION ( 'NONE',  ( 0.000000000000000000, 0.000000000000000000, -1.000000000000000000 ) ) ;
#8697=CARTESIAN_POINT ( 'NONE',  ( -50.07438362644099783, 99.17411849586700612, -145.2984795835770058 ) ) ;
#8698=CARTESIAN_POINT ( 'NONE',  ( -69.77438362644001302, 82.17411849586700612, -80.14847958357698587 ) ) ;
#8699=AXIS2_PLACEMENT_3D ( 'NONE', #12213, #14376, #5233 ) ;
#8704=EDGE_LOOP ( 'NONE', ( #8531, #10593, #10487 ) ) ;
#8709=CARTESIAN_POINT ( 'NONE',  ( -38.27438362644000591, 57.67411849586700612, -67.49847958357700861 ) ) ;
#8712=VECTOR ( 'NONE', #13379, 1000.000000000000000 ) ;
#8713=CYLINDRICAL_SURFACE ( 'NONE', #10324, 2.000000000000001776 ) ;
#8714=DIRECTION ( 'NONE',  ( 1.000000000000000000, 0.000000000000000000, 0.000000000000000000 ) ) ;
#8717=VERTEX_POINT ( 'NONE', #6131 ) ;
#8719=VECTOR ( 'NONE', #4965, 1000.000000000000000 ) ;
#8720=ORIENTED_EDGE ( 'NONE', *, *, #4490, .F. ) ;
#8729=DIRECTION ( 'NONE',  ( 0.000000000000000000, 0.000000000000000000, 1.000000000000000000 ) ) ;
#8731=DIRECTION ( 'NONE',  ( 0.000000000000000000, 0.000000000000000000, -1.000000000000000000 ) ) ;
#8732=DIRECTION ( 'NONE',  ( 0.8660254037844387076, 0.4999999999999998890, 0.000000000000000000 ) ) ;
#8734=FACE_OUTER_BOUND ( 'NONE', #4611, .T. ) ;
#8736=DIRECTION ( 'NONE',  ( 0.000000000000000000, 0.000000000000000000, -1.000000000000000000 ) ) ;
#8737=EDGE_LOOP ( 'NONE', ( #13241, #13730, #13177 ) ) ;
#8740=DIRECTION ( 'NONE',  ( 0.000000000000000000, 0.000000000000000000, 1.000000000000000000 ) ) ;
#8742=VERTEX_POINT ( 'NONE', #1053 ) ;
#8743=EDGE_CURVE ( 'NONE', #11184, #6866, #6672, .T. ) ;
#8744=AXIS2_PLACEMENT_3D ( 'NONE', #15305, #3684, #8414 ) ;
#8745=CARTESIAN_POINT ( 'NONE',  ( -56.52438362643999170, 65.17411849586700612, -150.4984795835770228 ) ) ;
#8749=AXIS2_PLACEMENT_3D ( 'NONE', #11638, #11795, #4735 ) ;
#8750=DIRECTION ( 'NONE',  ( 0.000000000000000000, 0.000000000000000000, 1.000000000000000000 ) ) ;
#8754=ADVANCED_FACE ( 'NONE', ( #9357 ), #2452, .F. ) ;
#8755=ORIENTED_EDGE ( 'NONE', *, *, #7580, .T. ) ;
#8760=VERTEX_POINT ( 'NONE', #10672 ) ;
#8761=ORIENTED_EDGE ( 'NONE', *, *, #4711, .T. ) ;
#8766=CARTESIAN_POINT ( 'NONE',  ( -38.27438362644000591, 60.67411849586700612, -79.49847958357700861 ) ) ;
#8769=EDGE_CURVE ( 'NONE', #5984, #7742, #7895, .T. ) ;
#8774=VECTOR ( 'NONE', #1841, 1000.000000000000000 ) ;
#8775=DIRECTION ( 'NONE',  ( 1.000000000000000000, 0.000000000000000000, 0.000000000000000000 ) ) ;
#8778=CARTESIAN_POINT ( 'NONE',  ( -86.77438362644100778, 101.5320169952374414, -147.9984795835769944 ) ) ;
#8779=FACE_OUTER_BOUND ( 'NONE', #451, .T. ) ;
#8783=VERTEX_POINT ( 'NONE', #4790 ) ;
#8788=AXIS2_PLACEMENT_3D ( 'NONE', #12031, #8907, #10291 ) ;
#8790=DIRECTION ( 'NONE',  ( 0.000000000000000000, 0.000000000000000000, -1.000000000000000000 ) ) ;
#8791=DIRECTION ( 'NONE',  ( -0.000000000000000000, -0.000000000000000000, 1.000000000000000000 ) ) ;
#8792=CARTESIAN_POINT ( 'NONE',  ( -62.02799568714584666, 110.1741184958670061, -152.4984795835769944 ) ) ;
#8793=CARTESIAN_POINT ( 'NONE',  ( -88.81638362644000040, 66.35306774555222376, -147.9984795835769944 ) ) ;
#8797=ORIENTED_EDGE ( 'NONE', *, *, #6056, .F. ) ;
#8798=VECTOR ( 'NONE', #11334, 1000.000000000000000 ) ;
#8799=DIRECTION ( 'NONE',  ( 0.000000000000000000, 0.000000000000000000, 1.000000000000000000 ) ) ;
#8800=VERTEX_POINT ( 'NONE', #10760 ) ;
#8804=ORIENTED_EDGE ( 'NONE', *, *, #1666, .T. ) ;
#8808=CARTESIAN_POINT ( 'NONE',  ( -69.77438362644001302, 74.17411849586699191, -29.37106258560738681 ) ) ;
#8812=CARTESIAN_POINT ( 'NONE',  ( -69.77438362644001302, 82.17411849586700612, -44.99847958358749622 ) ) ;
#8813=DIRECTION ( 'NONE',  ( -0.7071067811865474617, 8.659560562354921765E-17, 0.7071067811865474617 ) ) ;
#8814=FACE_OUTER_BOUND ( 'NONE', #73, .T. ) ;
#8815=DIRECTION ( 'NONE',  ( 0.000000000000000000, 0.000000000000000000, 1.000000000000000000 ) ) ;
#8816=AXIS2_PLACEMENT_3D ( 'NONE', #10345, #15072, #14995 ) ;
#8818=ORIENTED_EDGE ( 'NONE', *, *, #11679, .F. ) ;
#8819=ADVANCED_FACE ( 'NONE', ( #121 ), #3683, .F. ) ;
#8821=CARTESIAN_POINT ( 'NONE',  ( -86.77438362643999881, 67.53201699523744139, -147.9984795835769944 ) ) ;
#8823=VERTEX_POINT ( 'NONE', #3930 ) ;
#8825=CARTESIAN_POINT ( 'NONE',  ( -86.77438362643999881, 67.53201699523744139, -147.9984795835769944 ) ) ;
#8826=CIRCLE ( 'NONE', #7604, 0.2000000000000057288 ) ;
#8827=AXIS2_PLACEMENT_3D ( 'NONE', #15052, #9013, #12737 ) ;
#8831=CARTESIAN_POINT ( 'NONE',  ( -57.27438362644000591, 99.17411849586700612, -86.49847958357699440 ) ) ;
#8835=VERTEX_POINT ( 'NONE', #7358 ) ;
#8838=EDGE_CURVE ( 'NONE', #9550, #14746, #1604, .T. ) ;
#8841=ORIENTED_EDGE ( 'NONE', *, *, #14642, .F. ) ;
#8844=ORIENTED_EDGE ( 'NONE', *, *, #12384, .F. ) ;
#8845=DIRECTION ( 'NONE',  ( 0.000000000000000000, 0.000000000000000000, 1.000000000000000000 ) ) ;
#8847=AXIS2_PLACEMENT_3D ( 'NONE', #4604, #950, #3359 ) ;
#8850=DIRECTION ( 'NONE',  ( 1.000000000000000000, 0.000000000000000000, 0.000000000000000000 ) ) ;
#8853=DIRECTION ( 'NONE',  ( -0.8660254037844387076, -0.4999999999999998890, 0.000000000000000000 ) ) ;
#8854=EDGE_CURVE ( 'NONE', #2626, #8823, #7423, .T. ) ;
#8856=CARTESIAN_POINT ( 'NONE',  ( -76.26311196519618818, 67.29799558322736175, -83.44847958357698303 ) ) ;
#8857=VERTEX_POINT ( 'NONE', #1682 ) ;
#8858=CARTESIAN_POINT ( 'NONE',  ( -77.52077156573416516, 59.67411849586701322, -15.85886927678779834 ) ) ;
#8859=EDGE_CURVE ( 'NONE', #10111, #14573, #11616, .T. ) ;
#8860=ORIENTED_EDGE ( 'NONE', *, *, #2428, .F. ) ;
#8867=EDGE_CURVE ( 'NONE', #4176, #11511, #718, .T. ) ;
#8869=ADVANCED_FACE ( 'NONE', ( #5330 ), #12390, .F. ) ;
#8870=PLANE ( 'NONE',  #8211 ) ;
#8873=CARTESIAN_POINT ( 'NONE',  ( -71.12250604111743257, 75.17411849586699191, -44.11946707556889180 ) ) ;
#8876=ORIENTED_EDGE ( 'NONE', *, *, #15082, .T. ) ;
#8878=EDGE_CURVE ( 'NONE', #8760, #8497, #14832, .T. ) ;
#8884=ORIENTED_EDGE ( 'NONE', *, *, #5955, .F. ) ;
#8888=DIRECTION ( 'NONE',  ( 0.000000000000000000, 1.000000000000000000, 0.000000000000000000 ) ) ;
#8890=CARTESIAN_POINT ( 'NONE',  ( -52.77438362644000591, 65.17411849586700612, -152.4984795835769944 ) ) ;
#8891=DIRECTION ( 'NONE',  ( 0.7071067811865474617, 0.000000000000000000, 0.7071067811865474617 ) ) ;
#8893=PLANE ( 'NONE',  #10573 ) ;
#8898=CARTESIAN_POINT ( 'NONE',  ( -71.13655333277267800, 74.17411849586700612, -58.99847958357691624 ) ) ;
#8900=ORIENTED_EDGE ( 'NONE', *, *, #5170, .F. ) ;
#8902=DIRECTION ( 'NONE',  ( 0.000000000000000000, 0.000000000000000000, 1.000000000000000000 ) ) ;
#8903=PLANE ( 'NONE',  #11255 ) ;
#8905=DIRECTION ( 'NONE',  ( 0.000000000000000000, 0.000000000000000000, 1.000000000000000000 ) ) ;
#8906=CARTESIAN_POINT ( 'NONE',  ( -56.85838362644099675, 99.17411849586700612, -147.9984795835769944 ) ) ;
#8907=DIRECTION ( 'NONE',  ( 1.000000000000000000, 0.000000000000000000, -0.000000000000000000 ) ) ;
#8908=ORIENTED_EDGE ( 'NONE', *, *, #9703, .F. ) ;
#8912=ORIENTED_EDGE ( 'NONE', *, *, #5920, .F. ) ;
#8914=ORIENTED_EDGE ( 'NONE', *, *, #10492, .F. ) ;
#8915=EDGE_LOOP ( 'NONE', ( #12605, #1673, #2330 ) ) ;
#8917=EDGE_CURVE ( 'NONE', #12550, #14746, #6357, .T. ) ;
#8919=DIRECTION ( 'NONE',  ( 0.000000000000000000, 0.000000000000000000, -1.000000000000000000 ) ) ;
#8922=EDGE_CURVE ( 'NONE', #11316, #587, #2202, .T. ) ;
#8924=CARTESIAN_POINT ( 'NONE',  ( -52.77438362644100067, 99.17411849586700612, -149.9984795835770228 ) ) ;
#8926=DIRECTION ( 'NONE',  ( 0.8660254037844383745, -0.5000000000000003331, 0.000000000000000000 ) ) ;
#8927=CARTESIAN_POINT ( 'NONE',  ( -60.52799568714584666, 60.67411849586701322, -79.59847958357700293 ) ) ;
#8928=CARTESIAN_POINT ( 'NONE',  ( -51.75338362644099277, 100.9425423703948326, -147.9984795835769944 ) ) ;
#8930=CARTESIAN_POINT ( 'NONE',  ( -82.52438362644100778, 99.17411849586700612, -145.4984795835769944 ) ) ;
#8931=VERTEX_POINT ( 'NONE', #9738 ) ;
#8935=EDGE_CURVE ( 'NONE', #11838, #15131, #582, .T. ) ;
#8937=DIRECTION ( 'NONE',  ( 0.000000000000000000, 0.000000000000000000, -1.000000000000000000 ) ) ;
#8939=DIRECTION ( 'NONE',  ( 0.000000000000000000, 0.000000000000000000, -1.000000000000000000 ) ) ;
#8941=DIRECTION ( 'NONE',  ( 0.000000000000000000, 1.000000000000000000, 0.000000000000000000 ) ) ;
#8943=VECTOR ( 'NONE', #12929, 1000.000000000000000 ) ;
#8947=VERTEX_POINT ( 'NONE', #510 ) ;
#8948=EDGE_CURVE ( 'NONE', #3237, #11860, #9966, .T. ) ;
#8949=FACE_BOUND ( 'NONE', #14133, .T. ) ;
#8951=VECTOR ( 'NONE', #13473, 1000.000000000000000 ) ;
#8953=ORIENTED_EDGE ( 'NONE', *, *, #12764, .T. ) ;
#8955=VECTOR ( 'NONE', #14070, 1000.000000000000000 ) ;
#8956=DIRECTION ( 'NONE',  ( 0.000000000000000000, 0.000000000000000000, 1.000000000000000000 ) ) ;
#8958=DIRECTION ( 'NONE',  ( 1.000000000000000000, 0.000000000000000000, 0.000000000000000000 ) ) ;
#8961=AXIS2_PLACEMENT_3D ( 'NONE', #1195, #1431, #2586 ) ;
#8962=LINE ( 'NONE', #7883, #6684 ) ;
#8965=DIRECTION ( 'NONE',  ( -1.000000000000000000, 0.000000000000000000, 0.000000000000000000 ) ) ;
#8966=CARTESIAN_POINT ( 'NONE',  ( -84.02438362643999881, 99.17411849586700612, -145.4984795835769944 ) ) ;
#8968=AXIS2_PLACEMENT_3D ( 'NONE', #1925, #749, #10207 ) ;
#8970=ORIENTED_EDGE ( 'NONE', *, *, #2329, .T. ) ;
#8971=FACE_OUTER_BOUND ( 'NONE', #3469, .T. ) ;
#8974=EDGE_CURVE ( 'NONE', #14328, #12810, #12859, .T. ) ;
#8975=CARTESIAN_POINT ( 'NONE',  ( -96.77438362643999881, 110.1741184958670061, -152.4984795835769944 ) ) ;
#8981=VERTEX_POINT ( 'NONE', #4166 ) ;
#8983=ORIENTED_EDGE ( 'NONE', *, *, #10152, .F. ) ;
#8986=VERTEX_POINT ( 'NONE', #2133 ) ;
#8990=CARTESIAN_POINT ( 'NONE',  ( -84.07438362643999596, 65.17411849586700612, -145.4984795835769944 ) ) ;
#8993=CARTESIAN_POINT ( 'NONE',  ( -52.77438362644000591, 65.17411849586700612, -86.49847958357699440 ) ) ;
#8994=DIRECTION ( 'NONE',  ( 1.000000000000000000, 0.000000000000000000, 0.000000000000000000 ) ) ;
#8995=CARTESIAN_POINT ( 'NONE',  ( -52.77438362644000591, 65.17411849586700612, -145.4984795835769660 ) ) ;
#9001=VECTOR ( 'NONE', #9744, 1000.000000000000000 ) ;
#9004=DIRECTION ( 'NONE',  ( 1.000000000000000000, 0.000000000000000000, 0.000000000000000000 ) ) ;
#9006=AXIS2_PLACEMENT_3D ( 'NONE', #2964, #2326, #68 ) ;
#9007=ORIENTED_EDGE ( 'NONE', *, *, #14333, .F. ) ;
#9012=CIRCLE ( 'NONE', #10006, 16.00000000000000000 ) ;
#9013=DIRECTION ( 'NONE',  ( 1.000000000000000000, -1.287488025362404182E-15, 0.000000000000000000 ) ) ;
#9015=LINE ( 'NONE', #3128, #1648 ) ;
#9016=DIRECTION ( 'NONE',  ( -0.000000000000000000, 0.000000000000000000, -1.000000000000000000 ) ) ;
#9020=ORIENTED_EDGE ( 'NONE', *, *, #14548, .T. ) ;
#9021=DIRECTION ( 'NONE',  ( 0.000000000000000000, 0.000000000000000000, -1.000000000000000000 ) ) ;
#9022=AXIS2_PLACEMENT_3D ( 'NONE', #5116, #1611, #520 ) ;
#9023=CIRCLE ( 'NONE', #14956, 2.500000000000002220 ) ;
#9025=VECTOR ( 'NONE', #2707, 1000.000000000000000 ) ;
#9027=ORIENTED_EDGE ( 'NONE', *, *, #6851, .T. ) ;
#9033=PLANE ( 'NONE',  #140 ) ;
#9036=PLANE ( 'NONE',  #6296 ) ;
#9040=DIRECTION ( 'NONE',  ( 1.000000000000000000, 0.000000000000000000, 0.000000000000000000 ) ) ;
#9043=EDGE_CURVE ( 'NONE', #11817, #7059, #8962, .T. ) ;
#9046=ORIENTED_EDGE ( 'NONE', *, *, #8538, .F. ) ;
#9049=ADVANCED_FACE ( 'NONE', ( #4311 ), #13776, .F. ) ;
#9050=DIRECTION ( 'NONE',  ( 0.000000000000000000, 0.000000000000000000, -1.000000000000000000 ) ) ;
#9051=FACE_OUTER_BOUND ( 'NONE', #2097, .T. ) ;
#9053=CARTESIAN_POINT ( 'NONE',  ( -52.77438362643999881, 65.17411849586700612, -147.9984795835769944 ) ) ;
#9054=CARTESIAN_POINT ( 'NONE',  ( -62.02799568714584666, 110.1741184958670061, -15.85886927678779834 ) ) ;
#9057=FACE_OUTER_BOUND ( 'NONE', #2264, .T. ) ;
#9059=DIRECTION ( 'NONE',  ( 0.000000000000000000, 1.000000000000000000, 0.000000000000000000 ) ) ;
#9062=ORIENTED_EDGE ( 'NONE', *, *, #15300, .T. ) ;
#9063=ADVANCED_FACE ( 'NONE', ( #5415 ), #10116, .F. ) ;
#9075=CARTESIAN_POINT ( 'NONE',  ( -86.77438362643999881, 65.17411849586700612, -150.4984795835770228 ) ) ;
#9078=DIRECTION ( 'NONE',  ( 0.000000000000000000, 0.000000000000000000, 1.000000000000000000 ) ) ;
#9079=FACE_OUTER_BOUND ( 'NONE', #8915, .T. ) ;
#9080=VECTOR ( 'NONE', #6067, 1000.000000000000000 ) ;
#9082=DIRECTION ( 'NONE',  ( 0.000000000000000000, 0.000000000000000000, -1.000000000000000000 ) ) ;
#9083=ORIENTED_EDGE ( 'NONE', *, *, #14092, .T. ) ;
#9084=ORIENTED_EDGE ( 'NONE', *, *, #5854, .F. ) ;
#9086=CARTESIAN_POINT ( 'NONE',  ( -69.77438362644001302, 82.17411849586700612, -183.7533135795160320 ) ) ;
#9089=VECTOR ( 'NONE', #6413, 1000.000000000000000 ) ;
#9091=CARTESIAN_POINT ( 'NONE',  ( -68.09912303623742957, 75.17411849586700612, -44.18949531478455128 ) ) ;
#9092=CARTESIAN_POINT ( 'NONE',  ( -69.77438362644001302, 82.17411849586700612, -183.7533135795160320 ) ) ;
#9093=DIRECTION ( 'NONE',  ( 0.000000000000000000, 1.000000000000000000, 0.000000000000000000 ) ) ;
#9095=FACE_OUTER_BOUND ( 'NONE', #11776, .T. ) ;
#9096=ORIENTED_EDGE ( 'NONE', *, *, #9503, .F. ) ;
#9097=CARTESIAN_POINT ( 'NONE',  ( -69.77438362644001302, 82.17411849586700612, -138.4984795835769944 ) ) ;
#9099=CIRCLE ( 'NONE', #10093, 2.042000000000002036 ) ;
#9100=DIRECTION ( 'NONE',  ( 0.000000000000000000, 0.000000000000000000, 1.000000000000000000 ) ) ;
#9106=ADVANCED_FACE ( 'NONE', ( #10268 ), #2057, .F. ) ;
#9109=AXIS2_PLACEMENT_3D ( 'NONE', #14267, #10619, #3483 ) ;
#9110=CARTESIAN_POINT ( 'NONE',  ( -73.64736697264332577, 89.17411849586700612, -44.99847958359595168 ) ) ;
#9111=ADVANCED_FACE ( 'NONE', ( #4391 ), #4066, .F. ) ;
#9112=DIRECTION ( 'NONE',  ( 0.000000000000000000, -1.000000000000000000, 0.000000000000000000 ) ) ;
#9113=FACE_OUTER_BOUND ( 'NONE', #8138, .T. ) ;
#9115=ORIENTED_EDGE ( 'NONE', *, *, #3421, .T. ) ;
#9116=CIRCLE ( 'NONE', #9109, 2.750000000000002665 ) ;
#9122=LINE ( 'NONE', #10127, #6160 ) ;
#9123=CARTESIAN_POINT ( 'NONE',  ( -62.02799568714584666, 60.67411849586701322, -79.59847958357700293 ) ) ;
#9128=CARTESIAN_POINT ( 'NONE',  ( -42.77438362644000591, 65.17411849586700612, -15.85886927678779834 ) ) ;
#9131=ORIENTED_EDGE ( 'NONE', *, *, #7188, .F. ) ;
#9132=ADVANCED_FACE ( 'NONE', ( #4462 ), #9179, .T. ) ;
#9133=ORIENTED_EDGE ( 'NONE', *, *, #1265, .F. ) ;
#9135=ADVANCED_FACE ( 'NONE', ( #4699 ), #14308, .F. ) ;
#9137=ORIENTED_EDGE ( 'NONE', *, *, #4971, .F. ) ;
#9143=CARTESIAN_POINT ( 'NONE',  ( -52.77438362644000591, 99.17411849586700612, -145.4984795835769660 ) ) ;
#9144=DIRECTION ( 'NONE',  ( 1.000000000000000000, 0.000000000000000000, 0.000000000000000000 ) ) ;
#9145=ADVANCED_FACE ( 'NONE', ( #5792 ), #12235, .F. ) ;
#9146=EDGE_CURVE ( 'NONE', #10133, #4759, #2360, .T. ) ;
#9148=CARTESIAN_POINT ( 'NONE',  ( -77.89938362643999881, 82.17411849586700612, -138.4984795835769944 ) ) ;
#9149=CARTESIAN_POINT ( 'NONE',  ( -61.64938362644000591, 82.17411849586700612, -79.49847958357700861 ) ) ;
#9150=CARTESIAN_POINT ( 'NONE',  ( -69.77438362644001302, 82.17411849586700612, -43.99847958357699440 ) ) ;
#9151=EDGE_LOOP ( 'NONE', ( #13650, #9917, #2, #8096, #12569 ) ) ;
#9153=DIRECTION ( 'NONE',  ( -1.000000000000000000, 0.000000000000000000, 0.000000000000000000 ) ) ;
#9154=VERTEX_POINT ( 'NONE', #13088 ) ;
#9158=CARTESIAN_POINT ( 'NONE',  ( -101.2743836264399988, 111.1741184958670061, -67.49847958357700861 ) ) ;
#9163=DIRECTION ( 'NONE',  ( 0.000000000000000000, 0.000000000000000000, -1.000000000000000000 ) ) ;
#9167=ORIENTED_EDGE ( 'NONE', *, *, #13109, .F. ) ;
#9170=VERTEX_POINT ( 'NONE', #105 ) ;
#9171=ORIENTED_EDGE ( 'NONE', *, *, #421, .F. ) ;
#9173=ORIENTED_EDGE ( 'NONE', *, *, #11510, .F. ) ;
#9175=CYLINDRICAL_SURFACE ( 'NONE', #11683, 4.500000000000003553 ) ;
#9179=CYLINDRICAL_SURFACE ( 'NONE', #14212, 8.000000000000007105 ) ;
#9184=ORIENTED_EDGE ( 'NONE', *, *, #9593, .T. ) ;
#9185=CIRCLE ( 'NONE', #4249, 3.000000000000002665 ) ;
#9188=EDGE_LOOP ( 'NONE', ( #10602, #8983, #13300, #1816, #8206 ) ) ;
#9191=LINE ( 'NONE', #3010, #1516 ) ;
#9195=DIRECTION ( 'NONE',  ( 0.000000000000000000, 0.000000000000000000, -1.000000000000000000 ) ) ;
#9196=AXIS2_PLACEMENT_3D ( 'NONE', #9280, #10518, #13021 ) ;
#9197=FACE_OUTER_BOUND ( 'NONE', #10321, .T. ) ;
#9198=ORIENTED_EDGE ( 'NONE', *, *, #4941, .T. ) ;
#9199=CARTESIAN_POINT ( 'NONE',  ( -85.77438362644001302, 82.17411849586700612, -183.7533135795160320 ) ) ;
#9201=VERTEX_POINT ( 'NONE', #14001 ) ;
#9203=ORIENTED_EDGE ( 'NONE', *, *, #4227, .T. ) ;
#9205=VERTEX_POINT ( 'NONE', #6034 ) ;
#9208=ADVANCED_FACE ( 'NONE', ( #3449 ), #10739, .T. ) ;
#9209=ORIENTED_EDGE ( 'NONE', *, *, #14456, .T. ) ;
#9211=VECTOR ( 'NONE', #2443, 1000.000000000000000 ) ;
#9215=CARTESIAN_POINT ( 'NONE',  ( -62.02799568714584666, 59.67411849586701322, -152.4984795835769944 ) ) ;
#9216=CARTESIAN_POINT ( 'NONE',  ( -104.2743836264399988, 72.17411849586700612, -67.49847958357700861 ) ) ;
#9218=DIRECTION ( 'NONE',  ( 0.000000000000000000, 0.000000000000000000, -1.000000000000000000 ) ) ;
#9221=DIRECTION ( 'NONE',  ( 1.000000000000000000, 0.000000000000000000, -0.000000000000000000 ) ) ;
#9222=CARTESIAN_POINT ( 'NONE',  ( -61.64938362644000591, 82.17411849586700612, -138.4984795835769944 ) ) ;
#9228=VERTEX_POINT ( 'NONE', #5959 ) ;
#9229=VERTEX_POINT ( 'NONE', #12844 ) ;
#9230=ADVANCED_FACE ( 'NONE', ( #14228 ), #3609, .F. ) ;
#9231=AXIS2_PLACEMENT_3D ( 'NONE', #6580, #4085, #2997 ) ;
#9233=ADVANCED_FACE ( 'NONE', ( #4538 ), #3376, .T. ) ;
#9239=DIRECTION ( 'NONE',  ( 0.000000000000000000, -1.000000000000000000, 0.000000000000000000 ) ) ;
#9241=FACE_OUTER_BOUND ( 'NONE', #3415, .T. ) ;
#9244=EDGE_LOOP ( 'NONE', ( #6455, #12622 ) ) ;
#9247=VERTEX_POINT ( 'NONE', #1667 ) ;
#9248=DIRECTION ( 'NONE',  ( 0.000000000000000000, 0.000000000000000000, -1.000000000000000000 ) ) ;
#9249=CIRCLE ( 'NONE', #5309, 3.749999999999996447 ) ;
#9250=EDGE_LOOP ( 'NONE', ( #10137, #13145, #13966, #6377 ) ) ;
#9251=CIRCLE ( 'NONE', #3815, 3.750000000000003553 ) ;
#9254=ADVANCED_FACE ( 'NONE', ( #13464 ), #3985, .F. ) ;
#9255=ORIENTED_EDGE ( 'NONE', *, *, #10758, .F. ) ;
#9258=CARTESIAN_POINT ( 'NONE',  ( -38.27438362644000591, 57.67411849586700612, -67.49847958357700861 ) ) ;
#9261=AXIS2_PLACEMENT_3D ( 'NONE', #4655, #8291, #5827 ) ;
#9262=AXIS2_PLACEMENT_3D ( 'NONE', #6373, #7297, #10779 ) ;
#9264=ORIENTED_EDGE ( 'NONE', *, *, #7879, .T. ) ;
#9267=EDGE_LOOP ( 'NONE', ( #4344, #3637, #6402, #14002, #12336 ) ) ;
#9268=DIRECTION ( 'NONE',  ( 0.8660254037844387076, 0.4999999999999998890, 0.000000000000000000 ) ) ;
#9271=CLOSED_SHELL ( 'NONE', ( #6200, #6952, #1761, #5264, #11908, #11232, #13346, #10267, #12652, #12492, #13942, #2602 ) ) ;
#9272=VECTOR ( 'NONE', #3589, 1000.000000000000114 ) ;
#9275=CARTESIAN_POINT ( 'NONE',  ( -69.77438362644001302, 90.17411849586700612, -79.59847958357700293 ) ) ;
#9277=DIRECTION ( 'NONE',  ( 0.000000000000000000, 0.000000000000000000, -1.000000000000000000 ) ) ;
#9279=CARTESIAN_POINT ( 'NONE',  ( -69.77438362644001302, 94.57411849586699759, -89.99847958357699440 ) ) ;
#9280=CARTESIAN_POINT ( 'NONE',  ( -86.77438362644001302, 57.67411849586700612, -15.85886927678779834 ) ) ;
#9281=AXIS2_PLACEMENT_3D ( 'NONE', #11879, #1244, #4591 ) ;
#9282=ORIENTED_EDGE ( 'NONE', *, *, #1640, .T. ) ;
#9285=CARTESIAN_POINT ( 'NONE',  ( -91.27438362643999881, 99.17411849586700612, -79.59847958357700293 ) ) ;
#9287=ORIENTED_EDGE ( 'NONE', *, *, #5767, .T. ) ;
#9294=AXIS2_PLACEMENT_3D ( 'NONE', #8607, #6156, #13191 ) ;
#9295=DIRECTION ( 'NONE',  ( -1.000000000000000000, 0.000000000000000000, 0.000000000000000000 ) ) ;
#9296=DIRECTION ( 'NONE',  ( -0.000000000000000000, -0.000000000000000000, -1.000000000000000000 ) ) ;
#9297=EDGE_CURVE ( 'NONE', #686, #9229, #3989, .T. ) ;
#9302=DIRECTION ( 'NONE',  ( -1.000000000000000000, 0.000000000000000000, 0.000000000000000000 ) ) ;
#9308=ORIENTED_EDGE ( 'NONE', *, *, #4605, .T. ) ;
#9315=DIRECTION ( 'NONE',  ( 1.000000000000000000, 0.000000000000000000, 0.000000000000000000 ) ) ;
#9316=CARTESIAN_POINT ( 'NONE',  ( -75.64713719066081410, 66.22072495173567575, -81.84847958357697451 ) ) ;
#9319=AXIS2_PLACEMENT_3D ( 'NONE', #6781, #11352, #717 ) ;
#9321=PLANE ( 'NONE',  #6792 ) ;
#9322=AXIS2_PLACEMENT_3D ( 'NONE', #10395, #10944, #9923 ) ;
#9329=CARTESIAN_POINT ( 'NONE',  ( -89.27438362644100778, 110.1741184958670061, -79.59847958357700293 ) ) ;
#9330=AXIS2_PLACEMENT_3D ( 'NONE', #3687, #10741, #9801 ) ;
#9334=ORIENTED_EDGE ( 'NONE', *, *, #14709, .F. ) ;
#9337=CARTESIAN_POINT ( 'NONE',  ( -42.77438362644000591, 110.1741184958670061, -152.4984795835769944 ) ) ;
#9340=FACE_OUTER_BOUND ( 'NONE', #13051, .T. ) ;
#9341=ADVANCED_FACE ( 'NONE', ( #187 ), #2674, .F. ) ;
#9343=DIRECTION ( 'NONE',  ( 0.000000000000000000, 1.000000000000000000, 0.000000000000000000 ) ) ;
#9344=EDGE_CURVE ( 'NONE', #4564, #10086, #1017, .T. ) ;
#9345=ORIENTED_EDGE ( 'NONE', *, *, #8769, .F. ) ;
#9346=CARTESIAN_POINT ( 'NONE',  ( -52.77438362644100067, 101.5320169952374414, -147.9984795835769944 ) ) ;
#9347=ORIENTED_EDGE ( 'NONE', *, *, #769, .T. ) ;
#9352=CIRCLE ( 'NONE', #4660, 4.249999999999996447 ) ;
#9355=DIRECTION ( 'NONE',  ( -1.000000000000000000, 0.000000000000000000, 0.000000000000000000 ) ) ;
#9356=DIRECTION ( 'NONE',  ( 1.000000000000000000, 0.000000000000000000, 0.000000000000000000 ) ) ;
#9357=FACE_OUTER_BOUND ( 'NONE', #14366, .T. ) ;
#9359=DIRECTION ( 'NONE',  ( 0.000000000000000000, 0.000000000000000000, 1.000000000000000000 ) ) ;
#9360=DIRECTION ( 'NONE',  ( 0.000000000000000000, 0.000000000000000000, -1.000000000000000000 ) ) ;
#9361=CIRCLE ( 'NONE', #14079, 4.500000000000003553 ) ;
#9362=ORIENTED_EDGE ( 'NONE', *, *, #11325, .T. ) ;
#9363=DIRECTION ( 'NONE',  ( -1.000000000000000000, 0.000000000000000000, 0.000000000000000000 ) ) ;
#9364=ORIENTED_EDGE ( 'NONE', *, *, #2329, .F. ) ;
#9365=ORIENTED_EDGE ( 'NONE', *, *, #10822, .F. ) ;
#9367=ORIENTED_EDGE ( 'NONE', *, *, #2989, .F. ) ;
#9368=VERTEX_POINT ( 'NONE', #6191 ) ;
#9369=VERTEX_POINT ( 'NONE', #9643 ) ;
#9373=FACE_OUTER_BOUND ( 'NONE', #4539, .T. ) ;
#9374=DIRECTION ( 'NONE',  ( 1.000000000000000000, 0.000000000000000000, 0.000000000000000000 ) ) ;
#9377=CARTESIAN_POINT ( 'NONE',  ( -86.77438362644100778, 99.17411849586700612, -147.9984795835769944 ) ) ;
#9379=CARTESIAN_POINT ( 'NONE',  ( -84.73238362644100619, 97.99516924618178848, -150.4984795835770228 ) ) ;
#9385=ORIENTED_EDGE ( 'NONE', *, *, #12379, .T. ) ;
#9387=CARTESIAN_POINT ( 'NONE',  ( -83.02438362643998460, 65.17411849586700612, -150.4984795835770228 ) ) ;
#9395=FACE_OUTER_BOUND ( 'NONE', #15316, .T. ) ;
#9398=VERTEX_POINT ( 'NONE', #14455 ) ;
#9399=CYLINDRICAL_SURFACE ( 'NONE', #179, 2.500000000000002220 ) ;
#9401=ORIENTED_EDGE ( 'NONE', *, *, #11063, .T. ) ;
#9402=EDGE_CURVE ( 'NONE', #12871, #12429, #5999, .T. ) ;
#9406=CARTESIAN_POINT ( 'NONE',  ( -86.77438362644100778, 96.81621999649657084, -147.9984795835769944 ) ) ;
#9411=ORIENTED_EDGE ( 'NONE', *, *, #14252, .T. ) ;
#9412=DIRECTION ( 'NONE',  ( -1.000000000000000000, 0.000000000000000000, 0.000000000000000000 ) ) ;
#9413=DIRECTION ( 'NONE',  ( 1.000000000000000000, 0.000000000000000000, 0.000000000000000000 ) ) ;
#9414=ADVANCED_FACE ( 'NONE', ( #7794 ), #10104, .T. ) ;
#9415=EDGE_LOOP ( 'NONE', ( #14247, #10139, #9062, #9334 ) ) ;
#9416=PRESENTATION_STYLE_ASSIGNMENT (( #4705 ) ) ;
#9418=ORIENTED_EDGE ( 'NONE', *, *, #6346, .F. ) ;
#9422=LINE ( 'NONE', #15159, #1427 ) ;
#9423=CARTESIAN_POINT ( 'NONE',  ( -102.2743836264399988, 104.6741184958670061, -152.4984795835769944 ) ) ;
#9426=CARTESIAN_POINT ( 'NONE',  ( -77.94906324475290660, 70.01464610989972925, -83.44847958357698303 ) ) ;
#9430=AXIS2_PLACEMENT_3D ( 'NONE', #4246, #4327, #11457 ) ;
#9433=ADVANCED_FACE ( 'NONE', ( #9812 ), #11843, .T. ) ;
#9434=EDGE_LOOP ( 'NONE', ( #10391, #7500, #10706, #14650, #15331 ) ) ;
#9438=ORIENTED_EDGE ( 'NONE', *, *, #10132, .T. ) ;
#9440=ORIENTED_EDGE ( 'NONE', *, *, #4785, .F. ) ;
#9442=CARTESIAN_POINT ( 'NONE',  ( -54.81638362644000040, 63.99516924618178848, -150.4984795835770228 ) ) ;
#9444=FACE_OUTER_BOUND ( 'NONE', #9415, .T. ) ;
#9448=FACE_OUTER_BOUND ( 'NONE', #2065, .T. ) ;
#9452=AXIS2_PLACEMENT_3D ( 'NONE', #8540, #12042, #14353 ) ;
#9455=ORIENTED_EDGE ( 'NONE', *, *, #5726, .F. ) ;
#9456=AXIS2_PLACEMENT_3D ( 'NONE', #9086, #2180, #7926 ) ;
#9459=VECTOR ( 'NONE', #1015, 1000.000000000000000 ) ;
#9460=DIRECTION ( 'NONE',  ( -1.000000000000000000, 0.000000000000000000, 0.000000000000000000 ) ) ;
#9462=CARTESIAN_POINT ( 'NONE',  ( -52.77438362644100067, 96.81621999649657084, -147.9984795835769944 ) ) ;
#9465=PLANE ( 'NONE',  #14031 ) ;
#9466=DIRECTION ( 'NONE',  ( -1.000000000000000000, 0.000000000000000000, 0.000000000000000000 ) ) ;
#9467=DIRECTION ( 'NONE',  ( 0.000000000000000000, 0.000000000000000000, 1.000000000000000000 ) ) ;
#9469=AXIS2_PLACEMENT_3D ( 'NONE', #509, #6430, #9816 ) ;
#9470=DIRECTION ( 'NONE',  ( 0.000000000000000000, 0.000000000000000000, -1.000000000000000000 ) ) ;
#9471=DIRECTION ( 'NONE',  ( 1.000000000000000000, 0.000000000000000000, 0.000000000000000000 ) ) ;
#9472=VERTEX_POINT ( 'NONE', #7274 ) ;
#9474=ADVANCED_FACE ( 'NONE', ( #1364 ), #1209, .T. ) ;
#9475=ORIENTED_EDGE ( 'NONE', *, *, #8006, .T. ) ;
#9478=DIRECTION ( 'NONE',  ( 0.8660254037844383745, -0.5000000000000003331, 0.000000000000000000 ) ) ;
#9479=VERTEX_POINT ( 'NONE', #10907 ) ;
#9484=DIRECTION ( 'NONE',  ( 0.000000000000000000, -1.000000000000000000, 0.000000000000000000 ) ) ;
#9485=CIRCLE ( 'NONE', #6053, 2.500000000000002220 ) ;
#9490=DIRECTION ( 'NONE',  ( 1.287488025362404182E-15, 1.000000000000000000, 0.000000000000000000 ) ) ;
#9493=CARTESIAN_POINT ( 'NONE',  ( -59.02799568714584666, 59.67411849586701322, -15.85886927678779834 ) ) ;
#9498=ORIENTED_EDGE ( 'NONE', *, *, #14349, .F. ) ;
#9500=CARTESIAN_POINT ( 'NONE',  ( -48.52438362644100067, 99.17411849586700612, -182.2484795835770228 ) ) ;
#9502=LINE ( 'NONE', #3771, #7336 ) ;
#9503=EDGE_CURVE ( 'NONE', #1313, #9860, #12537, .T. ) ;
#9504=DIRECTION ( 'NONE',  ( 0.000000000000000000, 0.000000000000000000, 1.000000000000000000 ) ) ;
#9507=ADVANCED_FACE ( 'NONE', ( #1818 ), #6426, .F. ) ;
#9508=CARTESIAN_POINT ( 'NONE',  ( -69.77438362644001302, 82.17411849586700612, -82.44847958357698303 ) ) ;
#9512=AXIS2_PLACEMENT_3D ( 'NONE', #721, #5469, #10167 ) ;
#9519=ADVANCED_FACE ( 'NONE', ( #12223 ), #3995, .F. ) ;
#9520=LINE ( 'NONE', #9442, #13000 ) ;
#9521=LINE ( 'NONE', #3712, #15011 ) ;
#9528=ADVANCED_FACE ( 'NONE', ( #4305 ), #6655, .F. ) ;
#9529=DIRECTION ( 'NONE',  ( 0.3469356515732558988, -0.9378889346118975956, 0.000000000000000000 ) ) ;
#9530=EDGE_CURVE ( 'NONE', #5237, #5260, #2249, .T. ) ;
#9534=ORIENTED_EDGE ( 'NONE', *, *, #7175, .T. ) ;
#9535=ORIENTED_EDGE ( 'NONE', *, *, #12083, .T. ) ;
#9537=SHAPE_REPRESENTATION_RELATIONSHIP ( 'NONE' , 'NONE' ,  #5010, #13674 ) ;
#9543=DIRECTION ( 'NONE',  ( 0.000000000000000000, 0.000000000000000000, 1.000000000000000000 ) ) ;
#9545=STYLED_ITEM ( 'NONE', ( #9416 ), #418 ) ;
#9546=CARTESIAN_POINT ( 'NONE',  ( -86.77438362644001302, 110.1741184958670061, -15.85886927678779834 ) ) ;
#9547=DIRECTION ( 'NONE',  ( -1.000000000000000000, 0.000000000000000000, 0.000000000000000000 ) ) ;
#9548=CARTESIAN_POINT ( 'NONE',  ( -55.52438362644000591, 65.17411849586700612, -152.4984795835769944 ) ) ;
#9549=AXIS2_PLACEMENT_3D ( 'NONE', #4618, #12998, #2438 ) ;
#9550=VERTEX_POINT ( 'NONE', #507 ) ;
#9552=FACE_OUTER_BOUND ( 'NONE', #4908, .T. ) ;
#9553=ORIENTED_EDGE ( 'NONE', *, *, #1919, .T. ) ;
#9554=ORIENTED_EDGE ( 'NONE', *, *, #975, .F. ) ;
#9557=ORIENTED_EDGE ( 'NONE', *, *, #521, .F. ) ;
#9560=CIRCLE ( 'NONE', #12557, 16.00000000000000000 ) ;
#9566=DIRECTION ( 'NONE',  ( 0.000000000000000000, 0.000000000000000000, -1.000000000000000000 ) ) ;
#9568=CIRCLE ( 'NONE', #15022, 9.999999999999994671 ) ;
#9569=CARTESIAN_POINT ( 'NONE',  ( -86.77438362644001302, 99.17411849586700612, -86.49847958357699440 ) ) ;
#9572=ORIENTED_EDGE ( 'NONE', *, *, #9146, .T. ) ;
#9574=VERTEX_POINT ( 'NONE', #6493 ) ;
#9575=EDGE_CURVE ( 'NONE', #3708, #6323, #7805, .T. ) ;
#9577=DIRECTION ( 'NONE',  ( 0.000000000000000000, 0.000000000000000000, 1.000000000000000000 ) ) ;
#9578=EDGE_CURVE ( 'NONE', #13840, #10484, #11366, .T. ) ;
#9579=CARTESIAN_POINT ( 'NONE',  ( -69.77438362644001302, 82.17411849586700612, -81.84847958357698872 ) ) ;
#9580=TOROIDAL_SURFACE ( 'NONE', #13326, 2.700000000000000178, 0.2000000000000000111 ) ;
#9582=CARTESIAN_POINT ( 'NONE',  ( -69.77438362644001302, 82.17411849586700612, -183.7533135795160320 ) ) ;
#9583=CARTESIAN_POINT ( 'NONE',  ( -64.53565528768383786, 67.29799558322736175, -81.84847958357697451 ) ) ;
#9586=ORIENTED_EDGE ( 'NONE', *, *, #14000, .T. ) ;
#9588=ORIENTED_EDGE ( 'NONE', *, *, #4090, .T. ) ;
#9590=DIRECTION ( 'NONE',  ( -0.000000000000000000, 0.000000000000000000, -1.000000000000000000 ) ) ;
#9593=EDGE_CURVE ( 'NONE', #13931, #8947, #8452, .T. ) ;
#9594=EDGE_LOOP ( 'NONE', ( #879, #7726 ) ) ;
#9595=EDGE_CURVE ( 'NONE', #2658, #8154, #5745, .T. ) ;
#9596=ORIENTED_EDGE ( 'NONE', *, *, #725, .F. ) ;
#9598=CARTESIAN_POINT ( 'NONE',  ( -62.02799568714584666, 60.67411849586701322, -73.34256232478206528 ) ) ;
#9602=DIRECTION ( 'NONE',  ( -1.000000000000000000, 0.000000000000000000, 0.000000000000000000 ) ) ;
#9604=CARTESIAN_POINT ( 'NONE',  ( -69.77438362644001302, 82.17411849586700612, -152.4984795835769944 ) ) ;
#9610=DIRECTION ( 'NONE',  ( -0.000000000000000000, -0.000000000000000000, 1.000000000000000000 ) ) ;
#9614=ORIENTED_EDGE ( 'NONE', *, *, #12843, .F. ) ;
#9615=EDGE_CURVE ( 'NONE', #1401, #2251, #4230, .T. ) ;
#9616=AXIS2_PLACEMENT_3D ( 'NONE', #10514, #3698, #7281 ) ;
#9617=ADVANCED_FACE ( 'NONE', ( #657 ), #2751, .F. ) ;
#9621=LINE ( 'NONE', #79, #10969 ) ;
#9623=PLANE ( 'NONE',  #3166 ) ;
#9625=CARTESIAN_POINT ( 'NONE',  ( -38.27438362644000591, 114.1741184958670061, -79.49847958357700861 ) ) ;
#9628=VECTOR ( 'NONE', #3775, 1000.000000000000000 ) ;
#9630=ORIENTED_EDGE ( 'NONE', *, *, #2795, .T. ) ;
#9631=CARTESIAN_POINT ( 'NONE',  ( -62.27438362644000591, 75.17411849586699191, -58.99847958357700151 ) ) ;
#9633=ORIENTED_EDGE ( 'NONE', *, *, #13699, .T. ) ;
#9635=ADVANCED_FACE ( 'NONE', ( #882 ), #9175, .F. ) ;
#9638=CARTESIAN_POINT ( 'NONE',  ( -52.77438362643999881, 69.42411849586700612, -145.4984795835769944 ) ) ;
#9639=CARTESIAN_POINT ( 'NONE',  ( -54.81638362644100226, 97.99516924618178848, -147.9984795835769944 ) ) ;
#9640=DIRECTION ( 'NONE',  ( 1.000000000000000000, 0.000000000000000000, 0.000000000000000000 ) ) ;
#9642=CYLINDRICAL_SURFACE ( 'NONE', #12723, 2.500000000000002220 ) ;
#9643=CARTESIAN_POINT ( 'NONE',  ( -82.27438362643999881, 65.17411849586700612, -152.4984795835769944 ) ) ;
#9646=ORIENTED_EDGE ( 'NONE', *, *, #7451, .T. ) ;
#9647=SURFACE_STYLE_USAGE ( .BOTH. , #5011 ) ;
#9651=DIRECTION ( 'NONE',  ( 0.000000000000000000, 1.000000000000000000, 0.000000000000000000 ) ) ;
#9658=DIRECTION ( 'NONE',  ( 3.996802888650560011E-13, 1.000000000000000000, 0.000000000000000000 ) ) ;
#9664=ORIENTED_EDGE ( 'NONE', *, *, #9344, .T. ) ;
#9665=ORIENTED_EDGE ( 'NONE', *, *, #14450, .F. ) ;
#9670=DIRECTION ( 'NONE',  ( 1.000000000000000000, 0.000000000000000000, 0.000000000000000000 ) ) ;
#9672=DIRECTION ( 'NONE',  ( -1.000000000000000000, 1.287488025362404182E-15, 0.000000000000000000 ) ) ;
#9674=PLANE ( 'NONE',  #9294 ) ;
#9677=DIRECTION ( 'NONE',  ( 1.000000000000000000, 0.000000000000000000, 0.000000000000000000 ) ) ;
#9679=DIRECTION ( 'NONE',  ( 1.000000000000000000, 0.000000000000000000, 0.000000000000000000 ) ) ;
#9681=VERTEX_POINT ( 'NONE', #9258 ) ;
#9682=AXIS2_PLACEMENT_3D ( 'NONE', #7260, #11985, #15147 ) ;
#9683=ORIENTED_EDGE ( 'NONE', *, *, #8558, .F. ) ;
#9685=EDGE_LOOP ( 'NONE', ( #6020, #7637, #3058, #1218 ) ) ;
#9686=AXIS2_PLACEMENT_3D ( 'NONE', #12365, #6476, #560 ) ;
#9687=DIRECTION ( 'NONE',  ( 0.000000000000000000, 0.000000000000000000, -1.000000000000000000 ) ) ;
#9689=SURFACE_SIDE_STYLE ('',( #4978 ) ) ;
#9690=DIRECTION ( 'NONE',  ( 0.000000000000000000, 0.000000000000000000, -1.000000000000000000 ) ) ;
#9691=CARTESIAN_POINT ( 'NONE',  ( -52.77438362644100067, 101.5320169952374414, -150.4984795835770228 ) ) ;
#9696=LINE ( 'NONE', #5148, #4588 ) ;
#9700=ORIENTED_EDGE ( 'NONE', *, *, #13848, .T. ) ;
#9702=AXIS2_PLACEMENT_3D ( 'NONE', #515, #4170, #12394 ) ;
#9703=EDGE_CURVE ( 'NONE', #10484, #6998, #12839, .T. ) ;
#9704=VERTEX_POINT ( 'NONE', #9337 ) ;
#9706=ORIENTED_EDGE ( 'NONE', *, *, #13248, .T. ) ;
#9716=FACE_OUTER_BOUND ( 'NONE', #9250, .T. ) ;
#9717=CARTESIAN_POINT ( 'NONE',  ( -69.77438362644001302, 82.17411849586700612, -83.44847958357698303 ) ) ;
#9719=AXIS2_PLACEMENT_3D ( 'NONE', #359, #6132, #5106 ) ;
#9721=ORIENTED_EDGE ( 'NONE', *, *, #2088, .T. ) ;
#9722=CARTESIAN_POINT ( 'NONE',  ( -65.90140028023573393, 75.17411849586525818, -29.37106258560738681 ) ) ;
#9723=ADVANCED_FACE ( 'NONE', ( #1034, #13771 ), #12612, .F. ) ;
#9725=VECTOR ( 'NONE', #4494, 1000.000000000000000 ) ;
#9726=ORIENTED_EDGE ( 'NONE', *, *, #8935, .T. ) ;
#9727=( NAMED_UNIT ( * ) SI_UNIT ( $, .STERADIAN. ) SOLID_ANGLE_UNIT ( ) );
#9729=ORIENTED_EDGE ( 'NONE', *, *, #6965, .T. ) ;
#9731=AXIS2_PLACEMENT_3D ( 'NONE', #9583, #14321, #8588 ) ;
#9733=DIRECTION ( 'NONE',  ( 0.000000000000000000, -1.000000000000000000, 0.000000000000000000 ) ) ;
#9734=CARTESIAN_POINT ( 'NONE',  ( -69.77438362644001302, 82.17411849586700612, -150.4984795835769944 ) ) ;
#9735=AXIS2_PLACEMENT_3D ( 'NONE', #1349, #1268, #13155 ) ;
#9737=CIRCLE ( 'NONE', #6780, 2.042000000000002036 ) ;
#9738=CARTESIAN_POINT ( 'NONE',  ( -63.06767964790545022, 68.65632084656354550, -81.84847958357697451 ) ) ;
#9740=CARTESIAN_POINT ( 'NONE',  ( -86.77438362644001302, 65.17411849586700612, -152.4984795835769944 ) ) ;
#9741=CARTESIAN_POINT ( 'NONE',  ( -50.73238362643999722, 63.99516924618178848, -147.9984795835769944 ) ) ;
#9744=DIRECTION ( 'NONE',  ( 0.000000000000000000, 0.000000000000000000, -1.000000000000000000 ) ) ;
#9745=ORIENTED_EDGE ( 'NONE', *, *, #2627, .F. ) ;
#9746=CARTESIAN_POINT ( 'NONE',  ( -62.02799568714584666, 0.000000000000000000, -73.34256232478206528 ) ) ;
#9749=ORIENTED_EDGE ( 'NONE', *, *, #11349, .F. ) ;
#9751=DIRECTION ( 'NONE',  ( 0.000000000000000000, 0.000000000000000000, -1.000000000000000000 ) ) ;
#9757=VECTOR ( 'NONE', #12858, 1000.000000000000000 ) ;
#9759=ORIENTED_EDGE ( 'NONE', *, *, #3722, .T. ) ;
#9760=CARTESIAN_POINT ( 'NONE',  ( -52.77438362644000591, 65.17411849586700612, -152.4984795835769944 ) ) ;
#9761=ORIENTED_EDGE ( 'NONE', *, *, #10162, .F. ) ;
#9764=ORIENTED_EDGE ( 'NONE', *, *, #14428, .F. ) ;
#9765=DIRECTION ( 'NONE',  ( 0.000000000000000000, 0.000000000000000000, -1.000000000000000000 ) ) ;
#9766=EDGE_CURVE ( 'NONE', #11761, #4585, #13847, .T. ) ;
#9768=CIRCLE ( 'NONE', #15214, 2.500000000000002220 ) ;
#9769=DIRECTION ( 'NONE',  ( -1.000000000000000000, 0.000000000000000000, 0.000000000000000000 ) ) ;
#9771=DIRECTION ( 'NONE',  ( 0.000000000000000000, 0.000000000000000000, 1.000000000000000000 ) ) ;
#9773=DIRECTION ( 'NONE',  ( -1.000000000000000000, 0.000000000000000000, 0.000000000000000000 ) ) ;
#9774=CARTESIAN_POINT ( 'NONE',  ( -69.77438362644001302, 82.17411849586700612, -82.44847958357698303 ) ) ;
#9775=CARTESIAN_POINT ( 'NONE',  ( -69.77438362644001302, 82.17411849586700612, -79.59847958357700293 ) ) ;
#9776=FACE_OUTER_BOUND ( 'NONE', #4707, .T. ) ;
#9777=FACE_OUTER_BOUND ( 'NONE', #9800, .T. ) ;
#9778=FACE_OUTER_BOUND ( 'NONE', #1165, .T. ) ;
#9780=DIRECTION ( 'NONE',  ( 1.000000000000000000, 0.000000000000000000, 0.000000000000000000 ) ) ;
#9781=VECTOR ( 'NONE', #9268, 1000.000000000000000 ) ;
#9782=ORIENTED_EDGE ( 'NONE', *, *, #3186, .F. ) ;
#9783=AXIS2_PLACEMENT_3D ( 'NONE', #5177, #1819, #9885 ) ;
#9785=AXIS2_PLACEMENT_3D ( 'NONE', #2570, #10639, #8241 ) ;
#9792=CIRCLE ( 'NONE', #1630, 0.1999999999999987899 ) ;
#9793=DIRECTION ( 'NONE',  ( 0.000000000000000000, 0.000000000000000000, -1.000000000000000000 ) ) ;
#9794=ADVANCED_FACE ( 'NONE', ( #8102 ), #2203, .F. ) ;
#9796=CIRCLE ( 'NONE', #9549, 11.49999999999999645 ) ;
#9797=CARTESIAN_POINT ( 'NONE',  ( -96.77438362643999881, 59.67411849586700612, -79.59847958357700293 ) ) ;
#9800=EDGE_LOOP ( 'NONE', ( #3601, #14672, #2718, #13825, #5572 ) ) ;
#9801=DIRECTION ( 'NONE',  ( 0.000000000000000000, -1.000000000000000000, 0.000000000000000000 ) ) ;
#9803=ADVANCED_FACE ( 'NONE', ( #7109 ), #13226, .F. ) ;
#9805=CIRCLE ( 'NONE', #6130, 2.000000000000001776 ) ;
#9812=FACE_OUTER_BOUND ( 'NONE', #3337, .T. ) ;
#9813=ADVANCED_FACE ( 'NONE', ( #10651 ), #2669, .F. ) ;
#9814=FACE_OUTER_BOUND ( 'NONE', #2517, .T. ) ;
#9816=DIRECTION ( 'NONE',  ( 0.000000000000000000, 1.000000000000000000, 0.000000000000000000 ) ) ;
#9819=AXIS2_PLACEMENT_3D ( 'NONE', #7982, #6539, #14811 ) ;
#9820=CARTESIAN_POINT ( 'NONE',  ( -77.52077156573416516, 103.6741184958669777, -73.34256232478206528 ) ) ;
#9822=PLANE ( 'NONE',  #4372 ) ;
#9823=CARTESIAN_POINT ( 'NONE',  ( -52.77438362644000591, 65.17411849586700612, -145.4984795835769660 ) ) ;
#9824=DIRECTION ( 'NONE',  ( -0.4999999999999998890, 0.8660254037844387076, 0.000000000000000000 ) ) ;
#9825=ORIENTED_EDGE ( 'NONE', *, *, #15220, .T. ) ;
#9826=ORIENTED_EDGE ( 'NONE', *, *, #13985, .T. ) ;
#9830=ORIENTED_EDGE ( 'NONE', *, *, #12957, .F. ) ;
#9833=EDGE_CURVE ( 'NONE', #1912, #4210, #14399, .T. ) ;
#9835=CARTESIAN_POINT ( 'NONE',  ( -86.77438362644001302, 110.1741184958670061, -15.85886927678779834 ) ) ;
#9837=FACE_OUTER_BOUND ( 'NONE', #6530, .T. ) ;
#9838=PLANE ( 'NONE',  #5113 ) ;
#9840=VECTOR ( 'NONE', #13611, 1000.000000000000114 ) ;
#9842=LINE ( 'NONE', #1701, #7044 ) ;
#9843=EDGE_LOOP ( 'NONE', ( #5711, #13669 ) ) ;
#9844=ORIENTED_EDGE ( 'NONE', *, *, #11625, .F. ) ;
#9845=VERTEX_POINT ( 'NONE', #13153 ) ;
#9846=VERTEX_POINT ( 'NONE', #10735 ) ;
#9847=VERTEX_POINT ( 'NONE', #7413 ) ;
#9849=CARTESIAN_POINT ( 'NONE',  ( -57.27438362644000591, 65.17411849586700612, -145.4984795835769660 ) ) ;
#9851=AXIS2_PLACEMENT_3D ( 'NONE', #5774, #6711, #9093 ) ;
#9853=CARTESIAN_POINT ( 'NONE',  ( -64.53565528768383786, 67.29799558322736175, -83.44847958357698303 ) ) ;
#9855=CARTESIAN_POINT ( 'NONE',  ( -63.28565528768381654, 67.29799558322736175, -83.44847958357698303 ) ) ;
#9856=FACE_OUTER_BOUND ( 'NONE', #1811, .T. ) ;
#9857=CARTESIAN_POINT ( 'NONE',  ( -69.77438362644001302, 82.17411849586700612, -69.19783113114588957 ) ) ;
#9858=CARTESIAN_POINT ( 'NONE',  ( -84.73238362644100619, 100.3530677455522238, -147.9984795835769944 ) ) ;
#9860=VERTEX_POINT ( 'NONE', #4695 ) ;
#9861=DIRECTION ( 'NONE',  ( 1.000000000000000000, 0.000000000000000000, 0.000000000000000000 ) ) ;
#9862=EDGE_LOOP ( 'NONE', ( #10136, #14594, #15020, #7834 ) ) ;
#9863=AXIS2_PLACEMENT_3D ( 'NONE', #2801, #479, #7554 ) ;
#9864=ORIENTED_EDGE ( 'NONE', *, *, #11799, .T. ) ;
#9867=ADVANCED_FACE ( 'NONE', ( #12136 ), #8342, .T. ) ;
#9871=DIRECTION ( 'NONE',  ( -1.000000000000000000, 0.000000000000000000, 0.000000000000000000 ) ) ;
#9874=LINE ( 'NONE', #7574, #12593 ) ;
#9875=CARTESIAN_POINT ( 'NONE',  ( -69.77438362644001302, 90.17411849586700612, -112.9984795835769944 ) ) ;
#9878=ORIENTED_CLOSED_SHELL ( 'NONE', *, #10003, .F. );
#9879=LINE ( 'NONE', #259, #415 ) ;
#9882=ADVANCED_FACE ( 'NONE', ( #14373 ), #4850, .T. ) ;
#9884=ORIENTED_EDGE ( 'NONE', *, *, #5180, .F. ) ;
#9885=DIRECTION ( 'NONE',  ( 0.000000000000000000, -0.000000000000000000, -1.000000000000000000 ) ) ;
#9890=DIRECTION ( 'NONE',  ( -1.000000000000000000, 0.000000000000000000, 0.000000000000000000 ) ) ;
#9893=EDGE_CURVE ( 'NONE', #4480, #13685, #2504, .T. ) ;
#9894=DIRECTION ( 'NONE',  ( 0.000000000000000000, 0.000000000000000000, -1.000000000000000000 ) ) ;
#9897=ORIENTED_EDGE ( 'NONE', *, *, #8948, .T. ) ;
#9900=LINE ( 'NONE', #10123, #2599 ) ;
#9903=ORIENTED_EDGE ( 'NONE', *, *, #11212, .F. ) ;
#9906=EDGE_CURVE ( 'NONE', #15133, #8823, #6108, .T. ) ;
#9911=CARTESIAN_POINT ( 'NONE',  ( -89.47438362643998744, 65.17411849586700612, -145.4984795835769944 ) ) ;
#9914=VERTEX_POINT ( 'NONE', #3835 ) ;
#9916=VERTEX_POINT ( 'NONE', #14600 ) ;
#9917=ORIENTED_EDGE ( 'NONE', *, *, #12700, .F. ) ;
#9919=ORIENTED_EDGE ( 'NONE', *, *, #11915, .F. ) ;
#9920=EDGE_LOOP ( 'NONE', ( #13687, #7869, #5129 ) ) ;
#9921=CARTESIAN_POINT ( 'NONE',  ( -84.73238362643999722, 63.99516924618178848, -147.9984795835769944 ) ) ;
#9923=DIRECTION ( 'NONE',  ( -1.000000000000000000, 0.000000000000000000, 0.000000000000000000 ) ) ;
#9926=CARTESIAN_POINT ( 'NONE',  ( -86.77438362644001302, 65.17411849586700612, -79.59847958357700293 ) ) ;
#9927=DIRECTION ( 'NONE',  ( 0.000000000000000000, 0.000000000000000000, -1.000000000000000000 ) ) ;
#9932=ORIENTED_EDGE ( 'NONE', *, *, #5754, .F. ) ;
#9934=ORIENTED_EDGE ( 'NONE', *, *, #8878, .T. ) ;
#9935=CIRCLE ( 'NONE', #7218, 17.85000000000000497 ) ;
#9940=LINE ( 'NONE', #14755, #8456 ) ;
#9948=AXIS2_PLACEMENT_3D ( 'NONE', #4185, #11383, #5356 ) ;
#9951=DIRECTION ( 'NONE',  ( 0.000000000000000000, 0.000000000000000000, -1.000000000000000000 ) ) ;
#9952=VECTOR ( 'NONE', #3188, 1000.000000000000000 ) ;
#9954=VECTOR ( 'NONE', #3264, 1000.000000000000114 ) ;
#9957=EDGE_LOOP ( 'NONE', ( #4279, #9027, #9287, #2675 ) ) ;
#9958=CIRCLE ( 'NONE', #10449, 1.250000000000001110 ) ;
#9961=EDGE_CURVE ( 'NONE', #1753, #8331, #10948, .T. ) ;
#9962=PLANE ( 'NONE',  #7815 ) ;
#9963=AXIS2_PLACEMENT_3D ( 'NONE', #8380, #2635, #12104 ) ;
#9964=DIRECTION ( 'NONE',  ( 1.000000000000000000, 0.000000000000000000, 0.000000000000000000 ) ) ;
#9966=LINE ( 'NONE', #2842, #9628 ) ;
#9971=CARTESIAN_POINT ( 'NONE',  ( -82.27438362643999881, 65.17411849586700612, -79.59847958357700293 ) ) ;
#9972=ORIENTED_EDGE ( 'NONE', *, *, #1623, .F. ) ;
#9973=ORIENTED_EDGE ( 'NONE', *, *, #14454, .F. ) ;
#9975=CARTESIAN_POINT ( 'NONE',  ( -69.77438362644001302, 79.67411849586700612, -67.69567958357700377 ) ) ;
#9977=EDGE_LOOP ( 'NONE', ( #12533, #347, #2853, #7056, #6452, #4054 ) ) ;
#9978=AXIS2_PLACEMENT_3D ( 'NONE', #7144, #11865, #10693 ) ;
#9980=CIRCLE ( 'NONE', #12477, 16.00000000000000000 ) ;
#9982=DIRECTION ( 'NONE',  ( 0.000000000000000000, 0.000000000000000000, -1.000000000000000000 ) ) ;
#9983=ADVANCED_FACE ( 'NONE', ( #8634 ), #8870, .F. ) ;
#9988=EDGE_LOOP ( 'NONE', ( #1777, #1236, #9498, #3575 ) ) ;
#9989=DIRECTION ( 'NONE',  ( -0.000000000000000000, -0.000000000000000000, -1.000000000000000000 ) ) ;
#9990=AXIS2_PLACEMENT_3D ( 'NONE', #14587, #8397, #7555 ) ;
#9992=ORIENTED_EDGE ( 'NONE', *, *, #12900, .T. ) ;
#9993=EDGE_CURVE ( 'NONE', #8016, #9681, #3980, .T. ) ;
#9994=ORIENTED_EDGE ( 'NONE', *, *, #7275, .T. ) ;
#9995=VERTEX_POINT ( 'NONE', #561 ) ;
#9996=ORIENTED_EDGE ( 'NONE', *, *, #8123, .T. ) ;
#9997=ORIENTED_EDGE ( 'NONE', *, *, #436, .F. ) ;
#10001=EDGE_CURVE ( 'NONE', #2062, #2658, #13680, .T. ) ;
#10003=CLOSED_SHELL ( 'NONE', ( #15176, #8754, #3808, #6004, #2391, #6386, #8869 ) ) ;
#10004=CIRCLE ( 'NONE', #4827, 3.000000000000002665 ) ;
#10005=DIRECTION ( 'NONE',  ( -0.000000000000000000, 0.000000000000000000, -1.000000000000000000 ) ) ;
#10006=AXIS2_PLACEMENT_3D ( 'NONE', #14405, #3791, #745 ) ;
#10009=EDGE_CURVE ( 'NONE', #8182, #7017, #7488, .T. ) ;
#10011=CARTESIAN_POINT ( 'NONE',  ( -50.27438362644099357, 99.17411849586700612, -145.2984795835770058 ) ) ;
#10012=LINE ( 'NONE', #13444, #11522 ) ;
#10015=DIRECTION ( 'NONE',  ( -1.000000000000000000, 0.000000000000000000, 0.000000000000000000 ) ) ;
#10016=ORIENTED_EDGE ( 'NONE', *, *, #3653, .T. ) ;
#10021=AXIS2_PLACEMENT_3D ( 'NONE', #1382, #10849, #209 ) ;
#10022=AXIS2_PLACEMENT_3D ( 'NONE', #6276, #10838, #10909 ) ;
#10027=CARTESIAN_POINT ( 'NONE',  ( -52.77438362644000591, 65.17411849586700612, -145.4984795835769660 ) ) ;
#10032=CIRCLE ( 'NONE', #4096, 1.500000000000001332 ) ;
#10033=DIRECTION ( 'NONE',  ( 0.8660254037844387076, 0.4999999999999998890, 0.000000000000000000 ) ) ;
#10035=DIRECTION ( 'NONE',  ( 0.8660254037844383745, -0.5000000000000003331, 0.000000000000000000 ) ) ;
#10037=VERTEX_POINT ( 'NONE', #1582 ) ;
#10039=VECTOR ( 'NONE', #1474, 1000.000000000000000 ) ;
#10040=DIRECTION ( 'NONE',  ( -1.000000000000000000, 0.000000000000000000, 0.000000000000000000 ) ) ;
#10041=CARTESIAN_POINT ( 'NONE',  ( -49.02438362643999881, 65.17411849586700612, -150.4984795835770228 ) ) ;
#10042=DIRECTION ( 'NONE',  ( 0.000000000000000000, 0.000000000000000000, -1.000000000000000000 ) ) ;
#10044=DIRECTION ( 'NONE',  ( 0.000000000000000000, 0.000000000000000000, 1.000000000000000000 ) ) ;
#10046=CIRCLE ( 'NONE', #4115, 8.000000000000007105 ) ;
#10049=CIRCLE ( 'NONE', #12051, 2.750000000000002665 ) ;
#10051=EDGE_CURVE ( 'NONE', #15273, #3516, #10097, .T. ) ;
#10053=CARTESIAN_POINT ( 'NONE',  ( -52.77438362644100067, 99.17411849586700612, -145.4984795835769944 ) ) ;
#10055=EDGE_LOOP ( 'NONE', ( #6215, #465 ) ) ;
#10056=ADVANCED_FACE ( 'NONE', ( #13458 ), #11047, .F. ) ;
#10062=FACE_OUTER_BOUND ( 'NONE', #12411, .T. ) ;
#10063=DIRECTION ( 'NONE',  ( 0.000000000000000000, 0.000000000000000000, -1.000000000000000000 ) ) ;
#10064=ORIENTED_EDGE ( 'NONE', *, *, #13848, .F. ) ;
#10065=CARTESIAN_POINT ( 'NONE',  ( -38.27438362644000591, 111.1741184958670061, 0.000000000000000000 ) ) ;
#10067=EDGE_CURVE ( 'NONE', #13261, #7517, #11946, .T. ) ;
#10070=AXIS2_PLACEMENT_3D ( 'NONE', #3110, #5604, #13740 ) ;
#10071=VERTEX_POINT ( 'NONE', #495 ) ;
#10072=ORIENTED_EDGE ( 'NONE', *, *, #13202, .T. ) ;
#10073=ORIENTED_EDGE ( 'NONE', *, *, #3623, .F. ) ;
#10079=CARTESIAN_POINT ( 'NONE',  ( -80.27438362643999881, 82.17411849586700612, -80.14847958357698587 ) ) ;
#10080=EDGE_CURVE ( 'NONE', #4585, #913, #14830, .T. ) ;
#10083=CARTESIAN_POINT ( 'NONE',  ( -52.77438362643999881, 67.53201699523744139, -150.4984795835770228 ) ) ;
#10084=CARTESIAN_POINT ( 'NONE',  ( -50.73238362644099197, 100.3530677455522238, -147.9984795835769944 ) ) ;
#10086=VERTEX_POINT ( 'NONE', #5227 ) ;
#10087=DIRECTION ( 'NONE',  ( 0.000000000000000000, 0.000000000000000000, 1.000000000000000000 ) ) ;
#10088=ADVANCED_FACE ( 'NONE', ( #2738, #1800 ), #640, .T. ) ;
#10089=ORIENTED_EDGE ( 'NONE', *, *, #11679, .T. ) ;
#10091=VERTEX_POINT ( 'NONE', #12208 ) ;
#10092=EDGE_CURVE ( 'NONE', #11817, #3095, #12291, .T. ) ;
#10093=AXIS2_PLACEMENT_3D ( 'NONE', #1178, #2568, #14207 ) ;
#10095=EDGE_CURVE ( 'NONE', #5739, #13506, #6747, .T. ) ;
#10096=CARTESIAN_POINT ( 'NONE',  ( -91.27438362643999881, 65.17411849586700612, -152.4984795835769944 ) ) ;
#10097=LINE ( 'NONE', #13382, #3031 ) ;
#10098=PLANE ( 'NONE',  #8084 ) ;
#10099=EDGE_CURVE ( 'NONE', #1401, #9574, #1786, .T. ) ;
#10104=CYLINDRICAL_SURFACE ( 'NONE', #4241, 5.499999999999998224 ) ;
#10105=VERTEX_POINT ( 'NONE', #15123 ) ;
#10108=ORIENTED_EDGE ( 'NONE', *, *, #9906, .T. ) ;
#10111=VERTEX_POINT ( 'NONE', #12597 ) ;
#10112=AXIS2_PLACEMENT_3D ( 'NONE', #7824, #905, #15088 ) ;
#10113=CARTESIAN_POINT ( 'NONE',  ( -52.77438362644000591, 99.17411849586700612, -152.4984795835769944 ) ) ;
#10116=PLANE ( 'NONE',  #3445 ) ;
#10119=CARTESIAN_POINT ( 'NONE',  ( -70.92217029502012338, 98.13548005602207525, -94.57530113422089357 ) ) ;
#10120=DIRECTION ( 'NONE',  ( 1.000000000000000000, 0.000000000000000000, 0.000000000000000000 ) ) ;
#10123=CARTESIAN_POINT ( 'NONE',  ( -54.81638362644100226, 97.99516924618178848, -150.4984795835770228 ) ) ;
#10125=ORIENTED_EDGE ( 'NONE', *, *, #14984, .T. ) ;
#10126=CARTESIAN_POINT ( 'NONE',  ( -60.52799568714584666, 103.6741184958669919, -152.4984795835769944 ) ) ;
#10127=CARTESIAN_POINT ( 'NONE',  ( -73.76311196519618818, 67.29799558322736175, -83.44847958357698303 ) ) ;
#10128=CARTESIAN_POINT ( 'NONE',  ( -84.73238362644100619, 100.3530677455522238, -147.9984795835769944 ) ) ;
#10130=DIRECTION ( 'NONE',  ( 1.000000000000000000, 0.000000000000000000, 0.000000000000000000 ) ) ;
#10131=DIRECTION ( 'NONE',  ( 0.000000000000000000, 1.000000000000000000, 0.000000000000000000 ) ) ;
#10132=EDGE_CURVE ( 'NONE', #4413, #11099, #10441, .T. ) ;
#10133=VERTEX_POINT ( 'NONE', #3269 ) ;
#10135=EDGE_LOOP ( 'NONE', ( #14857, #1738, #8247, #7139 ) ) ;
#10136=ORIENTED_EDGE ( 'NONE', *, *, #6475, .T. ) ;
#10137=ORIENTED_EDGE ( 'NONE', *, *, #1623, .T. ) ;
#10139=ORIENTED_EDGE ( 'NONE', *, *, #12964, .T. ) ;
#10145=DIRECTION ( 'NONE',  ( 0.000000000000000000, 0.000000000000000000, 1.000000000000000000 ) ) ;
#10146=EDGE_CURVE ( 'NONE', #7767, #12014, #14975, .T. ) ;
#10151=CARTESIAN_POINT ( 'NONE',  ( -89.27438362644100778, 99.17411849586700612, -79.59847958357700293 ) ) ;
#10152=EDGE_CURVE ( 'NONE', #8835, #4666, #989, .T. ) ;
#10153=DIRECTION ( 'NONE',  ( 0.000000000000000000, 0.000000000000000000, -1.000000000000000000 ) ) ;
#10156=ORIENTED_EDGE ( 'NONE', *, *, #7629, .F. ) ;
#10157=ORIENTED_EDGE ( 'NONE', *, *, #14428, .T. ) ;
#10159=CARTESIAN_POINT ( 'NONE',  ( -69.77438362644001302, 82.17411849586700612, -112.9984795835769944 ) ) ;
#10160=DIRECTION ( 'NONE',  ( 0.000000000000000000, 0.000000000000000000, 1.000000000000000000 ) ) ;
#10161=CARTESIAN_POINT ( 'NONE',  ( -85.75338362643999801, 63.40569462133917256, -147.9984795835769944 ) ) ;
#10162=EDGE_CURVE ( 'NONE', #12096, #7439, #13832, .T. ) ;
#10164=AXIS2_PLACEMENT_3D ( 'NONE', #8181, #6949, #12916 ) ;
#10165=DIRECTION ( 'NONE',  ( 0.000000000000000000, 0.000000000000000000, 1.000000000000000000 ) ) ;
#10167=DIRECTION ( 'NONE',  ( 1.000000000000000000, 0.000000000000000000, 0.000000000000000000 ) ) ;
#10169=CIRCLE ( 'NONE', #3495, 2.699999999999993960 ) ;
#10171=EDGE_CURVE ( 'NONE', #1058, #2748, #5698, .T. ) ;
#10172=ORIENTED_EDGE ( 'NONE', *, *, #14456, .F. ) ;
#10175=FACE_OUTER_BOUND ( 'NONE', #14149, .T. ) ;
#10176=EDGE_LOOP ( 'NONE', ( #6164, #10486, #3260, #2231 ) ) ;
#10178=EDGE_CURVE ( 'NONE', #3597, #2640, #11201, .T. ) ;
#10182=CONICAL_SURFACE ( 'NONE', #35, 7.999999999994774846, 0.7853981634258691003 ) ;
#10183=DIRECTION ( 'NONE',  ( 0.000000000000000000, 0.000000000000000000, 1.000000000000000000 ) ) ;
#10185=CYLINDRICAL_SURFACE ( 'NONE', #6847, 16.06499999999999773 ) ;
#10186=DIRECTION ( 'NONE',  ( 1.000000000000000000, 0.000000000000000000, 0.000000000000000000 ) ) ;
#10192=CARTESIAN_POINT ( 'NONE',  ( -56.85838362644099675, 99.17411849586700612, -147.9984795835769944 ) ) ;
#10193=CARTESIAN_POINT ( 'NONE',  ( -72.48501812485920937, 97.94478668810718602, -93.86045013995706654 ) ) ;
#10200=AXIS2_PLACEMENT_3D ( 'NONE', #11158, #6447, #10130 ) ;
#10201=CARTESIAN_POINT ( 'NONE',  ( -86.77438362643999881, 69.42411849586700612, -145.4984795835769944 ) ) ;
#10202=AXIS2_PLACEMENT_3D ( 'NONE', #11810, #8237, #2340 ) ;
#10203=CARTESIAN_POINT ( 'NONE',  ( -73.64736697264743270, 75.17411849586699191, -57.99847958357699440 ) ) ;
#10205=CARTESIAN_POINT ( 'NONE',  ( -77.52077156573416516, 164.3482369917340122, -152.4984795835769944 ) ) ;
#10207=DIRECTION ( 'NONE',  ( -1.000000000000000000, 0.000000000000000000, 0.000000000000000000 ) ) ;
#10208=VECTOR ( 'NONE', #11369, 1000.000000000000000 ) ;
#10210=LINE ( 'NONE', #9199, #1326 ) ;
#10211=EDGE_LOOP ( 'NONE', ( #13113, #11474, #1900, #9897 ) ) ;
#10212=ORIENTED_EDGE ( 'NONE', *, *, #10924, .F. ) ;
#10215=ORIENTED_EDGE ( 'NONE', *, *, #11915, .T. ) ;
#10221=CIRCLE ( 'NONE', #3806, 3.750000000000003553 ) ;
#10222=DIRECTION ( 'NONE',  ( 0.000000000000000000, 0.000000000000000000, 1.000000000000000000 ) ) ;
#10224=FACE_OUTER_BOUND ( 'NONE', #8373, .T. ) ;
#10225=DIRECTION ( 'NONE',  ( 1.000000000000000000, 0.000000000000000000, 0.000000000000000000 ) ) ;
#10226=DIRECTION ( 'NONE',  ( -1.000000000000000000, 0.000000000000000000, 0.000000000000000000 ) ) ;
#10231=DIRECTION ( 'NONE',  ( -1.000000000000000000, 0.000000000000000000, 0.000000000000000000 ) ) ;
#10233=LINE ( 'NONE', #11265, #10734 ) ;
#10234=VERTEX_POINT ( 'NONE', #10161 ) ;
#10236=ORIENTED_EDGE ( 'NONE', *, *, #13695, .T. ) ;
#10239=CARTESIAN_POINT ( 'NONE',  ( -88.81638362644000040, 63.99516924618178848, -150.4984795835770228 ) ) ;
#10240=AXIS2_PLACEMENT_3D ( 'NONE', #14130, #946, #5775 ) ;
#10242=EDGE_CURVE ( 'NONE', #2764, #4822, #8225, .T. ) ;
#10244=CARTESIAN_POINT ( 'NONE',  ( -52.77438362644000591, 99.17411849586700612, -86.49847958357699440 ) ) ;
#10245=CARTESIAN_POINT ( 'NONE',  ( -86.77438362643999881, 65.17411849586700612, -147.9984795835769944 ) ) ;
#10246=DIRECTION ( 'NONE',  ( -1.000000000000000000, 0.000000000000000000, 0.000000000000000000 ) ) ;
#10247=( BOUNDED_CURVE ( )  B_SPLINE_CURVE ( 3, ( #11665, #5715, #15144, #12681 ),
 .UNSPECIFIED., .F., .T. ) 
 B_SPLINE_CURVE_WITH_KNOTS ( ( 4, 4 ),
 ( 0.000000000000000000, 0.5053605102841580710 ),
 .UNSPECIFIED. ) 
 CURVE ( )  GEOMETRIC_REPRESENTATION_ITEM ( )  RATIONAL_B_SPLINE_CURVE ( ( 1.000000000000000000, 0.9788305577012359482, 0.9788305577012359482, 1.000000000000000000 ) ) 
 REPRESENTATION_ITEM ( '' )  );
#10257=DIRECTION ( 'NONE',  ( 1.000000000000000000, 0.000000000000000000, 0.000000000000000000 ) ) ;
#10259=ORIENTED_EDGE ( 'NONE', *, *, #1096, .F. ) ;
#10266=AXIS2_PLACEMENT_3D ( 'NONE', #11108, #2886, #6176 ) ;
#10267=ADVANCED_FACE ( 'NONE', ( #14202 ), #235, .T. ) ;
#10268=FACE_OUTER_BOUND ( 'NONE', #4295, .T. ) ;
#10276=ORIENTED_EDGE ( 'NONE', *, *, #6056, .T. ) ;
#10281=DIRECTION ( 'NONE',  ( 0.000000000000000000, 0.000000000000000000, -1.000000000000000000 ) ) ;
#10282=DIRECTION ( 'NONE',  ( -1.000000000000000000, 0.000000000000000000, 0.000000000000000000 ) ) ;
#10283=COLOUR_RGB ( '', 0.72549020, 0.75294118, 0.79215686) ;
#10286=EDGE_CURVE ( 'NONE', #5822, #3491, #11809, .T. ) ;
#10291=DIRECTION ( 'NONE',  ( -0.000000000000000000, 0.000000000000000000, -1.000000000000000000 ) ) ;
#10292=ORIENTED_EDGE ( 'NONE', *, *, #3736, .T. ) ;
#10294=ADVANCED_FACE ( 'NONE', ( #1413 ), #1323, .F. ) ;
#10295=ORIENTED_EDGE ( 'NONE', *, *, #143, .F. ) ;
#10299=AXIS2_PLACEMENT_3D ( 'NONE', #5689, #11565, #9302 ) ;
#10301=ORIENTED_EDGE ( 'NONE', *, *, #7175, .F. ) ;
#10302=AXIS2_PLACEMENT_3D ( 'NONE', #11419, #4289, #10328 ) ;
#10308=DIRECTION ( 'NONE',  ( -1.000000000000000000, 0.000000000000000000, 0.000000000000000000 ) ) ;
#10309=DIRECTION ( 'NONE',  ( 1.000000000000000000, 0.000000000000000000, 0.000000000000000000 ) ) ;
#10312=CIRCLE ( 'NONE', #5637, 2.000000000000001776 ) ;
#10314=CARTESIAN_POINT ( 'NONE',  ( -85.83938362643999653, 81.46011849586699327, -83.44847958357698303 ) ) ;
#10315=LINE ( 'NONE', #5529, #4304 ) ;
#10318=DIRECTION ( 'NONE',  ( -1.000000000000000000, 0.000000000000000000, -0.000000000000000000 ) ) ;
#10320=EDGE_LOOP ( 'NONE', ( #9171, #5119, #8643, #15253 ) ) ;
#10321=EDGE_LOOP ( 'NONE', ( #5595, #3922, #5154, #2267 ) ) ;
#10324=AXIS2_PLACEMENT_3D ( 'NONE', #6480, #10165, #12523 ) ;
#10325=LINE ( 'NONE', #4441, #1860 ) ;
#10328=DIRECTION ( 'NONE',  ( 1.000000000000000000, 0.000000000000000000, 0.000000000000000000 ) ) ;
#10330=DIRECTION ( 'NONE',  ( -1.000000000000000000, 1.287488025362404182E-15, 0.000000000000000000 ) ) ;
#10331=DIRECTION ( 'NONE',  ( 0.8660254037844387076, 0.4999999999999998890, 0.000000000000000000 ) ) ;
#10334=EDGE_CURVE ( 'NONE', #11511, #4176, #3772, .T. ) ;
#10336=CONICAL_SURFACE ( 'NONE', #11587, 2.042000000000002036, 1.047197551196596965 ) ;
#10337=ORIENTED_EDGE ( 'NONE', *, *, #11344, .T. ) ;
#10341=ORIENTED_EDGE ( 'NONE', *, *, #12644, .F. ) ;
#10343=( BOUNDED_CURVE ( )  B_SPLINE_CURVE ( 3, ( #4093, #8898, #13568, #5258 ),
 .UNSPECIFIED., .F., .T. ) 
 B_SPLINE_CURVE_WITH_KNOTS ( ( 4, 4 ),
 ( 0.000000000000000000, 0.5053605102841570718 ),
 .UNSPECIFIED. ) 
 CURVE ( )  GEOMETRIC_REPRESENTATION_ITEM ( )  RATIONAL_B_SPLINE_CURVE ( ( 1.000000000000000000, 0.9788305577012359482, 0.9788305577012359482, 1.000000000000000000 ) ) 
 REPRESENTATION_ITEM ( '' )  );
#10345=CARTESIAN_POINT ( 'NONE',  ( -69.77438362644001302, 82.17411849586700612, -152.4984795835769944 ) ) ;
#10348=EDGE_CURVE ( 'NONE', #1588, #10872, #6006, .T. ) ;
#10352=ORIENTED_EDGE ( 'NONE', *, *, #8113, .F. ) ;
#10358=CYLINDRICAL_SURFACE ( 'NONE', #10415, 4.250000000000003553 ) ;
#10363=CARTESIAN_POINT ( 'NONE',  ( -52.77438362644100067, 101.5320169952374414, -150.4984795835770228 ) ) ;
#10365=LINE ( 'NONE', #2152, #12198 ) ;
#10367=VERTEX_POINT ( 'NONE', #10011 ) ;
#10370=ORIENTED_EDGE ( 'NONE', *, *, #4679, .T. ) ;
#10373=ORIENTED_EDGE ( 'NONE', *, *, #10952, .F. ) ;
#10374=VERTEX_POINT ( 'NONE', #4270 ) ;
#10378=CARTESIAN_POINT ( 'NONE',  ( -69.77438362644001302, 82.17411849586700612, -80.14847958357698587 ) ) ;
#10381=EDGE_CURVE ( 'NONE', #686, #8016, #14961, .T. ) ;
#10384=DIRECTION ( 'NONE',  ( 0.000000000000000000, 0.000000000000000000, 1.000000000000000000 ) ) ;
#10385=CARTESIAN_POINT ( 'NONE',  ( -50.73238362643999722, 66.35306774555222376, -150.4984795835770228 ) ) ;
#10386=DIRECTION ( 'NONE',  ( 0.000000000000000000, 0.000000000000000000, -1.000000000000000000 ) ) ;
#10387=ORIENTED_EDGE ( 'NONE', *, *, #10092, .F. ) ;
#10388=LINE ( 'NONE', #13965, #2556 ) ;
#10389=ORIENTED_EDGE ( 'NONE', *, *, #13441, .T. ) ;
#10390=ORIENTED_EDGE ( 'NONE', *, *, #13615, .T. ) ;
#10391=ORIENTED_EDGE ( 'NONE', *, *, #14188, .F. ) ;
#10395=CARTESIAN_POINT ( 'NONE',  ( -52.77438362644100067, 99.17411849586700612, -149.9984795835770228 ) ) ;
#10396=DIRECTION ( 'NONE',  ( -1.000000000000000000, 0.000000000000000000, 0.000000000000000000 ) ) ;
#10398=FACE_OUTER_BOUND ( 'NONE', #11674, .T. ) ;
#10401=DIRECTION ( 'NONE',  ( 0.4999999999999998890, -0.8660254037844387076, 0.000000000000000000 ) ) ;
#10403=DIRECTION ( 'NONE',  ( 1.000000000000000000, 0.000000000000000000, 0.000000000000000000 ) ) ;
#10405=ORIENTED_EDGE ( 'NONE', *, *, #2994, .T. ) ;
#10406=DIRECTION ( 'NONE',  ( -0.000000000000000000, -0.000000000000000000, -1.000000000000000000 ) ) ;
#10410=ORIENTED_EDGE ( 'NONE', *, *, #7629, .T. ) ;
#10415=AXIS2_PLACEMENT_3D ( 'NONE', #1986, #7750, #12555 ) ;
#10417=DIRECTION ( 'NONE',  ( 0.000000000000000000, 1.000000000000000000, 0.000000000000000000 ) ) ;
#10418=VERTEX_POINT ( 'NONE', #13958 ) ;
#10420=FACE_OUTER_BOUND ( 'NONE', #3323, .T. ) ;
#10421=AXIS2_PLACEMENT_3D ( 'NONE', #4933, #6263, #2741 ) ;
#10423=EDGE_LOOP ( 'NONE', ( #6099, #11878, #5719, #14345 ) ) ;
#10427=VERTEX_POINT ( 'NONE', #8300 ) ;
#10428=EDGE_CURVE ( 'NONE', #9846, #3619, #3267, .T. ) ;
#10433=DIRECTION ( 'NONE',  ( 0.000000000000000000, 0.000000000000000000, 1.000000000000000000 ) ) ;
#10434=DIRECTION ( 'NONE',  ( 0.000000000000000000, 0.000000000000000000, -1.000000000000000000 ) ) ;
#10436=CARTESIAN_POINT ( 'NONE',  ( -86.77438362644100778, 99.17411849586700612, -150.4984795835770228 ) ) ;
#10437=DIRECTION ( 'NONE',  ( 0.000000000000000000, 0.000000000000000000, -1.000000000000000000 ) ) ;
#10440=ORIENTED_EDGE ( 'NONE', *, *, #14344, .T. ) ;
#10441=CIRCLE ( 'NONE', #7499, 2.042000000000002036 ) ;
#10444=ORIENTED_EDGE ( 'NONE', *, *, #438, .T. ) ;
#10445=VERTEX_POINT ( 'NONE', #14040 ) ;
#10447=ORIENTED_EDGE ( 'NONE', *, *, #6623, .T. ) ;
#10449=AXIS2_PLACEMENT_3D ( 'NONE', #9853, #14584, #2485 ) ;
#10451=EDGE_CURVE ( 'NONE', #7767, #12872, #15146, .T. ) ;
#10454=DIRECTION ( 'NONE',  ( 0.000000000000000000, 0.000000000000000000, -1.000000000000000000 ) ) ;
#10459=CARTESIAN_POINT ( 'NONE',  ( -77.52077156573416516, 0.000000000000000000, -73.34256232478206528 ) ) ;
#10461=CARTESIAN_POINT ( 'NONE',  ( -64.53565528768383786, 67.29799558322736175, -83.44847958357698303 ) ) ;
#10462=ADVANCED_FACE ( 'NONE', ( #12881 ), #5992, .F. ) ;
#10463=ORIENTED_EDGE ( 'NONE', *, *, #4090, .F. ) ;
#10465=DIRECTION ( 'NONE',  ( -1.000000000000000000, 0.000000000000000000, 0.000000000000000000 ) ) ;
#10466=AXIS2_PLACEMENT_3D ( 'NONE', #578, #2397, #2923 ) ;
#10467=ORIENTED_EDGE ( 'NONE', *, *, #15156, .F. ) ;
#10470=EDGE_CURVE ( 'NONE', #4759, #10610, #12930, .T. ) ;
#10472=FACE_OUTER_BOUND ( 'NONE', #4956, .T. ) ;
#10474=DIRECTION ( 'NONE',  ( -1.287488025362404182E-15, -1.000000000000000000, 0.000000000000000000 ) ) ;
#10475=DIRECTION ( 'NONE',  ( 0.000000000000000000, 0.000000000000000000, 1.000000000000000000 ) ) ;
#10478=VECTOR ( 'NONE', #7781, 1000.000000000000000 ) ;
#10479=DIRECTION ( 'NONE',  ( 0.000000000000000000, -0.000000000000000000, 1.000000000000000000 ) ) ;
#10480=DIRECTION ( 'NONE',  ( 1.000000000000000000, 0.000000000000000000, 0.000000000000000000 ) ) ;
#10481=DIRECTION ( 'NONE',  ( 0.000000000000000000, 0.000000000000000000, 1.000000000000000000 ) ) ;
#10484=VERTEX_POINT ( 'NONE', #15039 ) ;
#10486=ORIENTED_EDGE ( 'NONE', *, *, #12451, .F. ) ;
#10487=ORIENTED_EDGE ( 'NONE', *, *, #8193, .F. ) ;
#10488=CARTESIAN_POINT ( 'NONE',  ( -77.52077156573416516, 0.000000000000000000, -79.59847958357700293 ) ) ;
#10492=EDGE_CURVE ( 'NONE', #1313, #4888, #4428, .T. ) ;
#10494=VERTEX_POINT ( 'NONE', #3715 ) ;
#10496=DIRECTION ( 'NONE',  ( 1.000000000000000000, 0.000000000000000000, 0.000000000000000000 ) ) ;
#10498=DIRECTION ( 'NONE',  ( 0.000000000000000000, 0.000000000000000000, 1.000000000000000000 ) ) ;
#10500=AXIS2_PLACEMENT_3D ( 'NONE', #2547, #2859, #7607 ) ;
#10505=ORIENTED_EDGE ( 'NONE', *, *, #12470, .F. ) ;
#10512=DIRECTION ( 'NONE',  ( 0.000000000000000000, -1.000000000000000000, 0.000000000000000000 ) ) ;
#10514=CARTESIAN_POINT ( 'NONE',  ( -86.77438362644001302, 65.17411849586700612, -145.4984795835769660 ) ) ;
#10516=LINE ( 'NONE', #14099, #12284 ) ;
#10518=DIRECTION ( 'NONE',  ( -0.000000000000000000, 1.000000000000000000, 0.000000000000000000 ) ) ;
#10519=CIRCLE ( 'NONE', #9322, 4.249999999999996447 ) ;
#10520=EDGE_LOOP ( 'NONE', ( #12260, #4725, #15078, #6525 ) ) ;
#10521=AXIS2_PLACEMENT_3D ( 'NONE', #13883, #7149, #12962 ) ;
#10529=ORIENTED_EDGE ( 'NONE', *, *, #5742, .F. ) ;
#10532=CARTESIAN_POINT ( 'NONE',  ( -86.27438362644001302, 82.17411849586700612, -150.4984795835769944 ) ) ;
#10537=FACE_OUTER_BOUND ( 'NONE', #14867, .T. ) ;
#10538=DIRECTION ( 'NONE',  ( 0.000000000000000000, -1.000000000000000000, 0.000000000000000000 ) ) ;
#10544=DIRECTION ( 'NONE',  ( 0.000000000000000000, 0.000000000000000000, 1.000000000000000000 ) ) ;
#10548=ORIENTED_EDGE ( 'NONE', *, *, #3849, .F. ) ;
#10549=VECTOR ( 'NONE', #4065, 1000.000000000000000 ) ;
#10550=VERTEX_POINT ( 'NONE', #13120 ) ;
#10551=ORIENTED_EDGE ( 'NONE', *, *, #6993, .F. ) ;
#10554=ADVANCED_FACE ( 'NONE', ( #378, #6154, #14407, #220, #12169, #8524 ), #14268, .F. ) ;
#10555=DIRECTION ( 'NONE',  ( 0.000000000000000000, 0.000000000000000000, -1.000000000000000000 ) ) ;
#10556=AXIS2_PLACEMENT_3D ( 'NONE', #6135, #10843, #8965 ) ;
#10558=DIRECTION ( 'NONE',  ( 1.287488025362404182E-15, 1.000000000000000000, 0.000000000000000000 ) ) ;
#10559=CARTESIAN_POINT ( 'NONE',  ( -56.85838362643999488, 65.17411849586700612, -147.9984795835769944 ) ) ;
#10560=AXIS2_PLACEMENT_3D ( 'NONE', #7491, #2670, #12210 ) ;
#10563=CARTESIAN_POINT ( 'NONE',  ( -69.77438362644001302, 82.17411849586700612, -81.84847958357698872 ) ) ;
#10567=CARTESIAN_POINT ( 'NONE',  ( -69.77438362644001302, 82.17411849586700612, -51.99847958357699440 ) ) ;
#10572=FACE_OUTER_BOUND ( 'NONE', #7674, .T. ) ;
#10573=AXIS2_PLACEMENT_3D ( 'NONE', #738, #2927, #9112 ) ;
#10574=AXIS2_PLACEMENT_3D ( 'NONE', #9075, #12643, #9144 ) ;
#10575=CARTESIAN_POINT ( 'NONE',  ( -101.2743836264399988, 60.67411849586700612, -67.49847958357700861 ) ) ;
#10576=ORIENTED_EDGE ( 'NONE', *, *, #6408, .F. ) ;
#10578=EDGE_CURVE ( 'NONE', #9247, #8981, #6518, .T. ) ;
#10581=CARTESIAN_POINT ( 'NONE',  ( -84.02438362643999881, 65.17411849586700612, -145.4984795835769944 ) ) ;
#10582=EDGE_CURVE ( 'NONE', #6231, #10427, #11089, .T. ) ;
#10583=AXIS2_PLACEMENT_3D ( 'NONE', #5971, #10669, #2450 ) ;
#10584=CARTESIAN_POINT ( 'NONE',  ( -52.77438362644100067, 99.17411849586700612, -147.9984795835769944 ) ) ;
#10585=ORIENTED_EDGE ( 'NONE', *, *, #8854, .T. ) ;
#10587=DIRECTION ( 'NONE',  ( 1.000000000000000000, 0.000000000000000000, 0.000000000000000000 ) ) ;
#10591=LINE ( 'NONE', #8421, #5108 ) ;
#10593=ORIENTED_EDGE ( 'NONE', *, *, #13959, .F. ) ;
#10594=VECTOR ( 'NONE', #866, 1000.000000000000000 ) ;
#10596=LINE ( 'NONE', #1133, #7385 ) ;
#10600=DIRECTION ( 'NONE',  ( -1.000000000000000000, 0.000000000000000000, 0.000000000000000000 ) ) ;
#10601=CIRCLE ( 'NONE', #13349, 10.50000000000000178 ) ;
#10602=ORIENTED_EDGE ( 'NONE', *, *, #1466, .F. ) ;
#10605=ORIENTED_EDGE ( 'NONE', *, *, #6161, .T. ) ;
#10606=ORIENTED_EDGE ( 'NONE', *, *, #2992, .F. ) ;
#10608=ORIENTED_EDGE ( 'NONE', *, *, #3510, .T. ) ;
#10610=VERTEX_POINT ( 'NONE', #14792 ) ;
#10613=DIRECTION ( 'NONE',  ( 0.000000000000000000, 1.000000000000000000, 0.000000000000000000 ) ) ;
#10614=VECTOR ( 'NONE', #1842, 1000.000000000000000 ) ;
#10616=DIRECTION ( 'NONE',  ( 0.000000000000000000, 0.000000000000000000, 1.000000000000000000 ) ) ;
#10618=DIRECTION ( 'NONE',  ( -1.000000000000000000, 0.000000000000000000, 0.000000000000000000 ) ) ;
#10619=DIRECTION ( 'NONE',  ( 0.000000000000000000, 0.000000000000000000, -1.000000000000000000 ) ) ;
#10621=FACE_BOUND ( 'NONE', #12018, .T. ) ;
#10624=VERTEX_POINT ( 'NONE', #8831 ) ;
#10625=CYLINDRICAL_SURFACE ( 'NONE', #13726, 2.500000000000002220 ) ;
#10629=EDGE_CURVE ( 'NONE', #11758, #1067, #11455, .T. ) ;
#10631=PLANE ( 'NONE',  #2601 ) ;
#10633=LINE ( 'NONE', #7005, #9459 ) ;
#10634=EDGE_CURVE ( 'NONE', #11284, #4095, #10973, .T. ) ;
#10639=DIRECTION ( 'NONE',  ( 0.000000000000000000, 0.000000000000000000, -1.000000000000000000 ) ) ;
#10640=CARTESIAN_POINT ( 'NONE',  ( -86.77438362643999881, 65.17411849586700612, -147.9984795835769944 ) ) ;
#10643=FACE_OUTER_BOUND ( 'NONE', #14, .T. ) ;
#10644=ORIENTED_EDGE ( 'NONE', *, *, #1466, .T. ) ;
#10645=ORIENTED_EDGE ( 'NONE', *, *, #14987, .F. ) ;
#10648=EDGE_LOOP ( 'NONE', ( #588, #6925 ) ) ;
#10651=FACE_OUTER_BOUND ( 'NONE', #3848, .T. ) ;
#10653=DIRECTION ( 'NONE',  ( 1.000000000000000000, 0.000000000000000000, 0.000000000000000000 ) ) ;
#10655=CARTESIAN_POINT ( 'NONE',  ( -50.02438362644000591, 99.17411849586700612, -152.4984795835769944 ) ) ;
#10658=DIRECTION ( 'NONE',  ( 0.000000000000000000, -1.000000000000000000, 0.000000000000000000 ) ) ;
#10661=( NAMED_UNIT ( * ) PLANE_ANGLE_UNIT ( ) SI_UNIT ( $, .RADIAN. ) );
#10665=DIRECTION ( 'NONE',  ( 0.000000000000000000, 1.000000000000000000, 0.000000000000000000 ) ) ;
#10669=DIRECTION ( 'NONE',  ( 1.000000000000000000, -1.287488025362404182E-15, 0.000000000000000000 ) ) ;
#10670=FACE_OUTER_BOUND ( 'NONE', #8208, .T. ) ;
#10672=CARTESIAN_POINT ( 'NONE',  ( -84.73238362644100619, 99.17411849586700612, -147.9984795835769944 ) ) ;
#10674=DIRECTION ( 'NONE',  ( 0.000000000000000000, 0.000000000000000000, -1.000000000000000000 ) ) ;
#10675=VECTOR ( 'NONE', #11229, 1000.000000000000000 ) ;
#10681=LINE ( 'NONE', #2459, #12748 ) ;
#10683=EDGE_LOOP ( 'NONE', ( #14986, #11877 ) ) ;
#10684=VERTEX_POINT ( 'NONE', #11541 ) ;
#10691=CARTESIAN_POINT ( 'NONE',  ( -37.27438362644000591, 99.17411849586700612, -152.4984795835769944 ) ) ;
#10692=VECTOR ( 'NONE', #10437, 1000.000000000000000 ) ;
#10693=DIRECTION ( 'NONE',  ( -1.000000000000000000, 0.000000000000000000, 0.000000000000000000 ) ) ;
#10694=DIRECTION ( 'NONE',  ( 0.000000000000000000, -0.000000000000000000, 1.000000000000000000 ) ) ;
#10698=CARTESIAN_POINT ( 'NONE',  ( -69.77438362644001302, 90.17411849586700612, -29.37106258560738681 ) ) ;
#10700=DIRECTION ( 'NONE',  ( 1.000000000000000000, 0.000000000000000000, 0.000000000000000000 ) ) ;
#10702=ORIENTED_EDGE ( 'NONE', *, *, #2512, .T. ) ;
#10703=FACE_OUTER_BOUND ( 'NONE', #2534, .T. ) ;
#10706=ORIENTED_EDGE ( 'NONE', *, *, #10009, .T. ) ;
#10707=EDGE_LOOP ( 'NONE', ( #3992, #2429, #9973, #1105 ) ) ;
#10708=AXIS2_PLACEMENT_3D ( 'NONE', #1272, #3688, #14231 ) ;
#10709=( LENGTH_UNIT ( ) NAMED_UNIT ( * ) SI_UNIT ( .MILLI., .METRE. ) );
#10717=CARTESIAN_POINT ( 'NONE',  ( -47.27438362644100778, 114.1741184958670061, -79.49847958357700861 ) ) ;
#10719=PLANE ( 'NONE',  #10783 ) ;
#10720=CIRCLE ( 'NONE', #9469, 16.00000000000000000 ) ;
#10721=DIRECTION ( 'NONE',  ( 0.5000000000000003331, 0.8660254037844384856, 0.000000000000000000 ) ) ;
#10722=FACE_OUTER_BOUND ( 'NONE', #13023, .T. ) ;
#10726=ORIENTED_EDGE ( 'NONE', *, *, #8600, .F. ) ;
#10728=ORIENTED_EDGE ( 'NONE', *, *, #6437, .F. ) ;
#10732=AXIS2_PLACEMENT_3D ( 'NONE', #5791, #5957, #1037 ) ;
#10734=VECTOR ( 'NONE', #773, 1000.000000000000000 ) ;
#10735=CARTESIAN_POINT ( 'NONE',  ( -87.79538362644099436, 100.9425423703948326, -147.9984795835769944 ) ) ;
#10738=LINE ( 'NONE', #15227, #14686 ) ;
#10739=CYLINDRICAL_SURFACE ( 'NONE', #87, 8.000000000000007105 ) ;
#10741=DIRECTION ( 'NONE',  ( 0.000000000000000000, 0.000000000000000000, -1.000000000000000000 ) ) ;
#10744=AXIS2_PLACEMENT_3D ( 'NONE', #5815, #4479, #7967 ) ;
#10745=FACE_OUTER_BOUND ( 'NONE', #3339, .T. ) ;
#10747=ORIENTED_EDGE ( 'NONE', *, *, #10451, .F. ) ;
#10748=AXIS2_PLACEMENT_3D ( 'NONE', #1039, #13002, #10417 ) ;
#10749=( LENGTH_UNIT ( ) NAMED_UNIT ( * ) SI_UNIT ( .MILLI., .METRE. ) );
#10751=ORIENTED_EDGE ( 'NONE', *, *, #5087, .T. ) ;
#10757=ADVANCED_FACE ( 'NONE', ( #13103 ), #1370, .F. ) ;
#10758=EDGE_CURVE ( 'NONE', #10494, #11099, #13019, .T. ) ;
#10759=CARTESIAN_POINT ( 'NONE',  ( -89.52438362644001302, 65.17411849586700612, -86.49847958357699440 ) ) ;
#10760=CARTESIAN_POINT ( 'NONE',  ( -48.27438362644000591, 65.17411849586700612, -79.59847958357700293 ) ) ;
#10761=CARTESIAN_POINT ( 'NONE',  ( -55.52438362644000591, 99.17411849586700612, -152.4984795835769944 ) ) ;
#10763=ADVANCED_FACE ( 'NONE', ( #2453 ), #2377, .T. ) ;
#10764=ORIENTED_EDGE ( 'NONE', *, *, #7828, .T. ) ;
#10765=LINE ( 'NONE', #3865, #824 ) ;
#10766=VECTOR ( 'NONE', #14560, 1000.000000000000114 ) ;
#10767=CIRCLE ( 'NONE', #102, 4.499999999999997335 ) ;
#10771=DIRECTION ( 'NONE',  ( 1.000000000000000000, 0.000000000000000000, 0.000000000000000000 ) ) ;
#10772=ADVANCED_FACE ( 'NONE', ( #14387 ), #7359, .F. ) ;
#10774=VERTEX_POINT ( 'NONE', #1215 ) ;
#10775=EDGE_LOOP ( 'NONE', ( #6607, #4740, #7364, #742 ) ) ;
#10776=ORIENTED_EDGE ( 'NONE', *, *, #14454, .T. ) ;
#10777=EDGE_CURVE ( 'NONE', #1406, #877, #5974, .T. ) ;
#10779=DIRECTION ( 'NONE',  ( 0.000000000000000000, 1.000000000000000000, 0.000000000000000000 ) ) ;
#10781=DIRECTION ( 'NONE',  ( -1.287488025362404182E-15, -1.000000000000000000, 0.000000000000000000 ) ) ;
#10783=AXIS2_PLACEMENT_3D ( 'NONE', #9546, #14292, #3668 ) ;
#10787=CARTESIAN_POINT ( 'NONE',  ( -52.77438362644100067, 96.81621999649657084, -147.9984795835769944 ) ) ;
#10790=ORIENTED_EDGE ( 'NONE', *, *, #698, .F. ) ;
#10795=LINE ( 'NONE', #15278, #7253 ) ;
#10796=AXIS2_PLACEMENT_3D ( 'NONE', #9279, #1140, #3311 ) ;
#10808=VERTEX_POINT ( 'NONE', #10911 ) ;
#10811=ORIENTED_EDGE ( 'NONE', *, *, #8652, .T. ) ;
#10812=VERTEX_POINT ( 'NONE', #270 ) ;
#10816=AXIS2_PLACEMENT_3D ( 'NONE', #10459, #9221, #6918 ) ;
#10819=DIRECTION ( 'NONE',  ( 0.000000000000000000, 0.000000000000000000, -1.000000000000000000 ) ) ;
#10820=LINE ( 'NONE', #184, #2630 ) ;
#10821=FACE_OUTER_BOUND ( 'NONE', #6491, .T. ) ;
#10822=EDGE_CURVE ( 'NONE', #13729, #10610, #5021, .T. ) ;
#10825=VECTOR ( 'NONE', #2362, 1000.000000000000000 ) ;
#10826=FACE_OUTER_BOUND ( 'NONE', #14801, .T. ) ;
#10829=ORIENTED_EDGE ( 'NONE', *, *, #8199, .T. ) ;
#10832=VECTOR ( 'NONE', #11818, 1000.000000000000000 ) ;
#10836=DIRECTION ( 'NONE',  ( 0.000000000000000000, 1.000000000000000000, 0.000000000000000000 ) ) ;
#10837=AXIS2_PLACEMENT_3D ( 'NONE', #7045, #4787, #9355 ) ;
#10838=DIRECTION ( 'NONE',  ( 1.000000000000000000, 0.000000000000000000, 0.000000000000000000 ) ) ;
#10839=EDGE_CURVE ( 'NONE', #3573, #14050, #1307, .T. ) ;
#10841=CARTESIAN_POINT ( 'NONE',  ( -86.77438362643999881, 67.53201699523744139, -147.9984795835769944 ) ) ;
#10843=DIRECTION ( 'NONE',  ( 0.000000000000000000, 0.000000000000000000, 1.000000000000000000 ) ) ;
#10844=DIRECTION ( 'NONE',  ( 0.000000000000000000, 0.000000000000000000, 1.000000000000000000 ) ) ;
#10845=ORIENTED_EDGE ( 'NONE', *, *, #14794, .F. ) ;
#10846=CARTESIAN_POINT ( 'NONE',  ( -42.77438362644000591, 59.67411849586700612, -15.85886927678779834 ) ) ;
#10849=DIRECTION ( 'NONE',  ( 0.000000000000000000, 0.000000000000000000, -1.000000000000000000 ) ) ;
#10852=ORIENTED_EDGE ( 'NONE', *, *, #8103, .T. ) ;
#10853=ORIENTED_EDGE ( 'NONE', *, *, #1919, .F. ) ;
#10855=EDGE_CURVE ( 'NONE', #1795, #3176, #583, .T. ) ;
#10856=DIRECTION ( 'NONE',  ( 0.000000000000000000, 0.000000000000000000, -1.000000000000000000 ) ) ;
#10857=CARTESIAN_POINT ( 'NONE',  ( -56.85838362643999488, 65.17411849586700612, -147.9984795835769944 ) ) ;
#10858=EDGE_CURVE ( 'NONE', #12262, #11654, #5331, .T. ) ;
#10859=AXIS2_PLACEMENT_3D ( 'NONE', #6069, #9672, #10781 ) ;
#10867=CARTESIAN_POINT ( 'NONE',  ( -84.73238362644100619, 97.99516924618178848, -147.9984795835769944 ) ) ;
#10868=VERTEX_POINT ( 'NONE', #6659 ) ;
#10870=ORIENTED_EDGE ( 'NONE', *, *, #5326, .T. ) ;
#10872=VERTEX_POINT ( 'NONE', #6358 ) ;
#10873=AXIS2_PLACEMENT_3D ( 'NONE', #4405, #11309, #15162 ) ;
#10879=DIRECTION ( 'NONE',  ( 0.000000000000000000, 0.000000000000000000, -1.000000000000000000 ) ) ;
#10880=ADVANCED_FACE ( 'NONE', ( #14923 ), #13218, .F. ) ;
#10881=EDGE_CURVE ( 'NONE', #11082, #13238, #11465, .T. ) ;
#10883=DIRECTION ( 'NONE',  ( 0.000000000000000000, 1.000000000000000000, 0.000000000000000000 ) ) ;
#10886=CARTESIAN_POINT ( 'NONE',  ( -68.42626121176255083, 89.17411849586700612, -44.11946707556887759 ) ) ;
#10887=AXIS2_PLACEMENT_3D ( 'NONE', #7669, #13250, #5181 ) ;
#10888=EDGE_LOOP ( 'NONE', ( #2118, #8352 ) ) ;
#10889=LINE ( 'NONE', #2730, #427 ) ;
#10891=ORIENTED_EDGE ( 'NONE', *, *, #7362, .T. ) ;
#10895=CARTESIAN_POINT ( 'NONE',  ( -86.77438362644100778, 101.5320169952374414, -147.9984795835769944 ) ) ;
#10900=ORIENTED_EDGE ( 'NONE', *, *, #2320, .F. ) ;
#10901=DIRECTION ( 'NONE',  ( 0.000000000000000000, 0.000000000000000000, -1.000000000000000000 ) ) ;
#10903=FILL_AREA_STYLE ('',( #6197 ) ) ;
#10907=CARTESIAN_POINT ( 'NONE',  ( -52.77438362643999881, 65.17411849586700612, -146.8195303338917768 ) ) ;
#10908=DIRECTION ( 'NONE',  ( -1.000000000000000000, 0.000000000000000000, 0.000000000000000000 ) ) ;
#10909=DIRECTION ( 'NONE',  ( 0.000000000000000000, -0.000000000000000000, -1.000000000000000000 ) ) ;
#10910=DIRECTION ( 'NONE',  ( 0.000000000000000000, 1.000000000000000000, 0.000000000000000000 ) ) ;
#10911=CARTESIAN_POINT ( 'NONE',  ( -77.52077156573416516, 110.1741184958670061, -79.59847958357700293 ) ) ;
#10912=LINE ( 'NONE', #13479, #7108 ) ;
#10913=DIRECTION ( 'NONE',  ( 1.000000000000000000, 0.000000000000000000, 0.000000000000000000 ) ) ;
#10917=EDGE_CURVE ( 'NONE', #2062, #13986, #13710, .T. ) ;
#10924=EDGE_CURVE ( 'NONE', #10037, #6718, #3053, .T. ) ;
#10925=ORIENTED_EDGE ( 'NONE', *, *, #12195, .F. ) ;
#10928=CYLINDRICAL_SURFACE ( 'NONE', #10500, 1.250000000000001110 ) ;
#10932=CARTESIAN_POINT ( 'NONE',  ( -102.2743836264399988, 65.17411849586700612, -79.59847958357700293 ) ) ;
#10934=CARTESIAN_POINT ( 'NONE',  ( -85.83938362643999653, 81.46011849586699327, -83.44847958357698303 ) ) ;
#10935=ADVANCED_FACE ( 'NONE', ( #14850 ), #11222, .F. ) ;
#10938=EDGE_LOOP ( 'NONE', ( #13785, #9440 ) ) ;
#10940=ORIENTED_EDGE ( 'NONE', *, *, #2791, .F. ) ;
#10944=DIRECTION ( 'NONE',  ( 0.000000000000000000, 0.000000000000000000, -1.000000000000000000 ) ) ;
#10948=CIRCLE ( 'NONE', #4247, 1.500000000000001332 ) ;
#10949=EDGE_CURVE ( 'NONE', #5814, #8154, #11141, .T. ) ;
#10950=DIRECTION ( 'NONE',  ( -0.000000000000000000, 0.000000000000000000, -1.000000000000000000 ) ) ;
#10951=LINE ( 'NONE', #5062, #846 ) ;
#10952=EDGE_CURVE ( 'NONE', #13871, #8497, #11214, .T. ) ;
#10954=CARTESIAN_POINT ( 'NONE',  ( -54.81638362644000040, 66.35306774555222376, -150.4984795835770228 ) ) ;
#10955=CARTESIAN_POINT ( 'NONE',  ( -69.77438362644001302, 82.17411849586700612, -80.14847958357698587 ) ) ;
#10956=ORIENTED_EDGE ( 'NONE', *, *, #7082, .T. ) ;
#10957=DIRECTION ( 'NONE',  ( 1.287488025362404182E-15, 1.000000000000000000, 0.000000000000000000 ) ) ;
#10963=VECTOR ( 'NONE', #15282, 1000.000000000000114 ) ;
#10967=DIRECTION ( 'NONE',  ( 0.000000000000000000, -0.000000000000000000, 1.000000000000000000 ) ) ;
#10968=DIRECTION ( 'NONE',  ( -1.000000000000000000, 0.000000000000000000, 0.000000000000000000 ) ) ;
#10969=VECTOR ( 'NONE', #13365, 1000.000000000000000 ) ;
#10971=DIRECTION ( 'NONE',  ( -0.8660254037844381525, 0.000000000000000000, -0.5000000000000007772 ) ) ;
#10973=CIRCLE ( 'NONE', #1048, 10.50000000000000178 ) ;
#10975=ORIENTED_EDGE ( 'NONE', *, *, #10067, .F. ) ;
#10976=CARTESIAN_POINT ( 'NONE',  ( -66.03636180653452925, 65.59017466835990717, -81.84847958357697451 ) ) ;
#10977=EDGE_CURVE ( 'NONE', #10684, #11895, #2262, .T. ) ;
#10980=CIRCLE ( 'NONE', #4288, 2.500000000000002220 ) ;
#10983=VERTEX_POINT ( 'NONE', #5859 ) ;
#10987=CARTESIAN_POINT ( 'NONE',  ( -69.77438362644001302, 74.17411849586699191, -112.9984795835769944 ) ) ;
#10992=CARTESIAN_POINT ( 'NONE',  ( -59.02799568714584666, 110.1741184958670061, -152.4984795835769944 ) ) ;
#10993=FACE_OUTER_BOUND ( 'NONE', #471, .T. ) ;
#10994=AXIS2_PLACEMENT_3D ( 'NONE', #11336, #1947, #10231 ) ;
#10995=ORIENTED_EDGE ( 'NONE', *, *, #10582, .T. ) ;
#10996=ORIENTED_EDGE ( 'NONE', *, *, #1948, .F. ) ;
#11004=AXIS2_PLACEMENT_3D ( 'NONE', #1213, #3463, #5972 ) ;
#11005=DIRECTION ( 'NONE',  ( 0.000000000000000000, 0.000000000000000000, -1.000000000000000000 ) ) ;
#11006=DIRECTION ( 'NONE',  ( 0.000000000000000000, -1.000000000000000000, 0.000000000000000000 ) ) ;
#11014=DIRECTION ( 'NONE',  ( 0.000000000000000000, 0.000000000000000000, -1.000000000000000000 ) ) ;
#11016=VERTEX_POINT ( 'NONE', #15290 ) ;
#11018=VERTEX_POINT ( 'NONE', #8089 ) ;
#11022=( NAMED_UNIT ( * ) SI_UNIT ( $, .STERADIAN. ) SOLID_ANGLE_UNIT ( ) );
#11026=EDGE_CURVE ( 'NONE', #14103, #14684, #14132, .T. ) ;
#11027=CARTESIAN_POINT ( 'NONE',  ( -48.27438362644000591, 65.17411849586700612, -145.4984795835769660 ) ) ;
#11031=DIRECTION ( 'NONE',  ( 0.000000000000000000, 0.000000000000000000, 1.000000000000000000 ) ) ;
#11032=DIRECTION ( 'NONE',  ( 1.000000000000000000, 0.000000000000000000, 0.000000000000000000 ) ) ;
#11034=DIRECTION ( 'NONE',  ( 0.000000000000000000, 0.000000000000000000, 1.000000000000000000 ) ) ;
#11036=VERTEX_POINT ( 'NONE', #13071 ) ;
#11037=CIRCLE ( 'NONE', #8563, 17.00000000000000000 ) ;
#11038=EDGE_LOOP ( 'NONE', ( #11547, #6888 ) ) ;
#11039=ORIENTED_EDGE ( 'NONE', *, *, #13156, .T. ) ;
#11043=CARTESIAN_POINT ( 'NONE',  ( -86.77438362643999881, 65.17411849586700612, -145.2984795835770058 ) ) ;
#11047=PLANE ( 'NONE',  #14161 ) ;
#11048=EDGE_CURVE ( 'NONE', #13889, #15148, #12985, .T. ) ;
#11052=CARTESIAN_POINT ( 'NONE',  ( -69.77438362644001302, 81.46011849586699327, -81.84847958357697451 ) ) ;
#11054=ADVANCED_FACE ( 'NONE', ( #7096 ), #5536, .F. ) ;
#11056=EDGE_CURVE ( 'NONE', #11016, #1481, #14211, .T. ) ;
#11058=DIRECTION ( 'NONE',  ( 0.000000000000000000, 0.000000000000000000, 1.000000000000000000 ) ) ;
#11059=AXIS2_PLACEMENT_3D ( 'NONE', #482, #5217, #14665 ) ;
#11062=CARTESIAN_POINT ( 'NONE',  ( -80.27438362643999881, 82.17411849586700612, -182.1969643934119745 ) ) ;
#11063=EDGE_CURVE ( 'NONE', #7989, #4013, #1183, .T. ) ;
#11065=ORIENTED_EDGE ( 'NONE', *, *, #11415, .T. ) ;
#11070=DIRECTION ( 'NONE',  ( 1.000000000000000000, 0.000000000000000000, 0.000000000000000000 ) ) ;
#11073=DIRECTION ( 'NONE',  ( -1.000000000000000000, 0.000000000000000000, 0.000000000000000000 ) ) ;
#11075=CARTESIAN_POINT ( 'NONE',  ( -69.77438362644001302, 82.17411849586700612, -80.14847958357698587 ) ) ;
#11076=DIRECTION ( 'NONE',  ( 0.000000000000000000, 0.000000000000000000, -1.000000000000000000 ) ) ;
#11078=ORIENTED_EDGE ( 'NONE', *, *, #13048, .F. ) ;
#11079=EDGE_LOOP ( 'NONE', ( #8613, #13485, #6793, #8841 ) ) ;
#11082=VERTEX_POINT ( 'NONE', #7171 ) ;
#11084=CIRCLE ( 'NONE', #4390, 8.124999999999992895 ) ;
#11085=CARTESIAN_POINT ( 'NONE',  ( -56.85838362643999488, 65.17411849586700612, -147.9984795835769944 ) ) ;
#11087=CARTESIAN_POINT ( 'NONE',  ( -91.27438362643999881, 99.17411849586700612, -145.4984795835769660 ) ) ;
#11089=LINE ( 'NONE', #9054, #8234 ) ;
#11091=CARTESIAN_POINT ( 'NONE',  ( -86.77438362643999881, 67.53201699523744139, -147.9984795835769944 ) ) ;
#11092=VECTOR ( 'NONE', #2960, 1000.000000000000114 ) ;
#11094=LINE ( 'NONE', #12565, #14460 ) ;
#11095=ORIENTED_EDGE ( 'NONE', *, *, #9578, .F. ) ;
#11096=ORIENTED_EDGE ( 'NONE', *, *, #10242, .F. ) ;
#11097=VERTEX_POINT ( 'NONE', #11890 ) ;
#11099=VERTEX_POINT ( 'NONE', #1253 ) ;
#11100=CARTESIAN_POINT ( 'NONE',  ( -48.52438362643999881, 65.17411849586700612, -145.4984795835769944 ) ) ;
#11105=DIRECTION ( 'NONE',  ( 0.000000000000000000, 0.000000000000000000, -1.000000000000000000 ) ) ;
#11106=DIRECTION ( 'NONE',  ( 1.000000000000000000, 0.000000000000000000, 0.000000000000000000 ) ) ;
#11108=CARTESIAN_POINT ( 'NONE',  ( -52.77438362643999881, 67.53201699523744139, -147.9984795835769944 ) ) ;
#11109=PLANE ( 'NONE',  #11059 ) ;
#11110=CARTESIAN_POINT ( 'NONE',  ( -76.48108760497456160, 68.65632084656354550, -83.44847958357698303 ) ) ;
#11112=DIRECTION ( 'NONE',  ( 0.000000000000000000, 1.000000000000000000, 0.000000000000000000 ) ) ;
#11113=ORIENTED_EDGE ( 'NONE', *, *, #438, .F. ) ;
#11115=EDGE_LOOP ( 'NONE', ( #484, #4116, #6772, #11165 ) ) ;
#11118=ADVANCED_FACE ( 'NONE', ( #10722 ), #14064, .T. ) ;
#11122=CARTESIAN_POINT ( 'NONE',  ( -91.02438362644100778, 99.17411849586700612, -182.2484795835770228 ) ) ;
#11126=FACE_OUTER_BOUND ( 'NONE', #5888, .T. ) ;
#11127=CARTESIAN_POINT ( 'NONE',  ( -86.77438362644100778, 99.17411849586700612, -149.9984795835770228 ) ) ;
#11129=DIRECTION ( 'NONE',  ( 0.000000000000000000, 0.000000000000000000, -1.000000000000000000 ) ) ;
#11130=ADVANCED_FACE ( 'NONE', ( #11737, #4312 ), #9036, .T. ) ;
#11132=CARTESIAN_POINT ( 'NONE',  ( -50.73238362643999722, 66.35306774555222376, -147.9984795835769944 ) ) ;
#11134=ORIENTED_EDGE ( 'NONE', *, *, #3280, .T. ) ;
#11135=EDGE_CURVE ( 'NONE', #14025, #8800, #15210, .T. ) ;
#11136=CARTESIAN_POINT ( 'NONE',  ( -79.02077156573416516, 60.67411849586702743, -73.34256232478206528 ) ) ;
#11137=CARTESIAN_POINT ( 'NONE',  ( -86.77438362644001302, 99.17411849586700612, -152.4984795835769944 ) ) ;
#11139=EDGE_CURVE ( 'NONE', #9846, #5278, #1420, .T. ) ;
#11140=DIRECTION ( 'NONE',  ( -1.000000000000000000, 0.000000000000000000, 0.000000000000000000 ) ) ;
#11141=LINE ( 'NONE', #11294, #15165 ) ;
#11143=DIRECTION ( 'NONE',  ( 0.000000000000000000, 0.000000000000000000, -1.000000000000000000 ) ) ;
#11145=VERTEX_POINT ( 'NONE', #242 ) ;
#11147=ADVANCED_FACE ( 'NONE', ( #3970 ), #4781, .F. ) ;
#11151=ORIENTED_EDGE ( 'NONE', *, *, #667, .F. ) ;
#11158=CARTESIAN_POINT ( 'NONE',  ( -86.77438362644100778, 99.17411849586700612, -145.2984795835770058 ) ) ;
#11161=EDGE_LOOP ( 'NONE', ( #6457, #3472 ) ) ;
#11164=ORIENTED_EDGE ( 'NONE', *, *, #13793, .F. ) ;
#11165=ORIENTED_EDGE ( 'NONE', *, *, #1144, .F. ) ;
#11170=AXIS2_PLACEMENT_3D ( 'NONE', #6651, #3284, #11512 ) ;
#11176=PLANE ( 'NONE',  #2854 ) ;
#11177=FACE_OUTER_BOUND ( 'NONE', #4856, .T. ) ;
#11178=CARTESIAN_POINT ( 'NONE',  ( -86.77438362643999881, 65.17411849586700612, -150.4984795835770228 ) ) ;
#11179=AXIS2_PLACEMENT_3D ( 'NONE', #3840, #425, #14605 ) ;
#11180=ORIENTED_EDGE ( 'NONE', *, *, #5370, .F. ) ;
#11183=TOROIDAL_SURFACE ( 'NONE', #6492, 2.700000000000000178, 0.2000000000000000111 ) ;
#11184=VERTEX_POINT ( 'NONE', #11110 ) ;
#11187=CARTESIAN_POINT ( 'NONE',  ( -69.77438362644001302, 82.17411849586700612, -44.99847958359270450 ) ) ;
#11190=DIRECTION ( 'NONE',  ( 0.5000000000000003331, 0.8660254037844384856, 0.000000000000000000 ) ) ;
#11191=CARTESIAN_POINT ( 'NONE',  ( -56.85838362644099675, 99.17411849586700612, -147.9984795835769944 ) ) ;
#11192=DIRECTION ( 'NONE',  ( 0.000000000000000000, 0.000000000000000000, -1.000000000000000000 ) ) ;
#11193=PLANE ( 'NONE',  #1188 ) ;
#11196=ADVANCED_FACE ( 'NONE', ( #2657, #4053 ), #12050, .T. ) ;
#11201=CIRCLE ( 'NONE', #14895, 4.500000000000003553 ) ;
#11203=DIRECTION ( 'NONE',  ( -0.7071067811865474617, 8.659560562354921765E-17, 0.7071067811865474617 ) ) ;
#11205=ORIENTED_EDGE ( 'NONE', *, *, #6437, .T. ) ;
#11206=AXIS2_PLACEMENT_3D ( 'NONE', #2184, #11731, #7 ) ;
#11207=DIRECTION ( 'NONE',  ( 1.000000000000000000, 0.000000000000000000, 0.000000000000000000 ) ) ;
#11210=CARTESIAN_POINT ( 'NONE',  ( -57.02438362644099357, 99.17411849586700612, -149.9984795835770228 ) ) ;
#11211=ADVANCED_FACE ( 'NONE', ( #9778 ), #7477, .F. ) ;
#11212=EDGE_CURVE ( 'NONE', #12871, #12429, #5549, .T. ) ;
#11213=CARTESIAN_POINT ( 'NONE',  ( -77.52077156573416516, 0.000000000000000000, -152.4984795835769944 ) ) ;
#11214=LINE ( 'NONE', #14619, #8255 ) ;
#11215=FACE_OUTER_BOUND ( 'NONE', #4669, .T. ) ;
#11216=CARTESIAN_POINT ( 'NONE',  ( -69.19455825983806108, 98.16615590796850199, -94.68115879786580535 ) ) ;
#11218=ADVANCED_FACE ( 'NONE', ( #8779 ), #3546, .F. ) ;
#11221=ORIENTED_EDGE ( 'NONE', *, *, #7472, .F. ) ;
#11222=CONICAL_SURFACE ( 'NONE', #1806, 2.042000000000002036, 1.047197551196596965 ) ;
#11226=EDGE_CURVE ( 'NONE', #14843, #1405, #1718, .T. ) ;
#11227=EDGE_CURVE ( 'NONE', #8717, #6563, #3583, .T. ) ;
#11228=AXIS2_PLACEMENT_3D ( 'NONE', #6725, #11442, #3068 ) ;
#11229=DIRECTION ( 'NONE',  ( 0.000000000000000000, 0.000000000000000000, -1.000000000000000000 ) ) ;
#11230=VECTOR ( 'NONE', #10465, 1000.000000000000000 ) ;
#11232=ADVANCED_FACE ( 'NONE', ( #173 ), #14362, .F. ) ;
#11233=CARTESIAN_POINT ( 'NONE',  ( -69.77438362644001302, 82.17411849586700612, -183.7533135795160320 ) ) ;
#11235=DIRECTION ( 'NONE',  ( 0.000000000000000000, 0.000000000000000000, 1.000000000000000000 ) ) ;
#11237=PLANE ( 'NONE',  #7099 ) ;
#11239=DIRECTION ( 'NONE',  ( 0.8660254037844383745, -0.5000000000000003331, 0.000000000000000000 ) ) ;
#11241=ORIENTED_EDGE ( 'NONE', *, *, #5170, .T. ) ;
#11246=ORIENTED_EDGE ( 'NONE', *, *, #249, .F. ) ;
#11247=ORIENTED_EDGE ( 'NONE', *, *, #2512, .F. ) ;
#11248=ORIENTED_EDGE ( 'NONE', *, *, #10822, .T. ) ;
#11250=CARTESIAN_POINT ( 'NONE',  ( -86.77438362643999881, 65.17411849586700612, -182.2484795835770228 ) ) ;
#11253=CIRCLE ( 'NONE', #12000, 4.249999999999996447 ) ;
#11255=AXIS2_PLACEMENT_3D ( 'NONE', #13717, #6739, #4248 ) ;
#11260=LINE ( 'NONE', #10083, #8553 ) ;
#11262=DIRECTION ( 'NONE',  ( -0.8660254037844381525, 0.000000000000000000, -0.5000000000000007772 ) ) ;
#11265=CARTESIAN_POINT ( 'NONE',  ( -86.77438362643999881, 62.81621999649657084, -150.4984795835770228 ) ) ;
#11267=ORIENTED_EDGE ( 'NONE', *, *, #6023, .T. ) ;
#11268=ORIENTED_EDGE ( 'NONE', *, *, #15097, .F. ) ;
#11269=CIRCLE ( 'NONE', #1598, 1.250000000000001110 ) ;
#11270=CIRCLE ( 'NONE', #4571, 4.500000000000003553 ) ;
#11274=DIRECTION ( 'NONE',  ( 1.000000000000000000, 0.000000000000000000, 0.000000000000000000 ) ) ;
#11276=CARTESIAN_POINT ( 'NONE',  ( -50.73238362643999722, 65.17411849586700612, -147.9984795835769944 ) ) ;
#11277=FACE_OUTER_BOUND ( 'NONE', #133, .T. ) ;
#11278=CARTESIAN_POINT ( 'NONE',  ( -38.27438362644000591, 114.1741184958670061, -67.49847958357700861 ) ) ;
#11281=VERTEX_POINT ( 'NONE', #3115 ) ;
#11282=DIRECTION ( 'NONE',  ( 0.8660254037844383745, -0.5000000000000003331, 0.000000000000000000 ) ) ;
#11283=EDGE_LOOP ( 'NONE', ( #7782, #9646, #5945, #7759 ) ) ;
#11284=VERTEX_POINT ( 'NONE', #4431 ) ;
#11288=STYLED_ITEM ( 'NONE', ( #12185 ), #5480 ) ;
#11291=DIRECTION ( 'NONE',  ( -1.000000000000000000, 0.000000000000000000, 0.000000000000000000 ) ) ;
#11292=LINE ( 'NONE', #1820, #12710 ) ;
#11294=CARTESIAN_POINT ( 'NONE',  ( -49.02438362643999881, 65.17411849586700612, -150.4984795835770228 ) ) ;
#11299=ORIENTED_EDGE ( 'NONE', *, *, #1746, .F. ) ;
#11300=DIRECTION ( 'NONE',  ( 1.000000000000000000, 0.000000000000000000, 0.000000000000000000 ) ) ;
#11303=EDGE_CURVE ( 'NONE', #9479, #8420, #10315, .T. ) ;
#11304=CARTESIAN_POINT ( 'NONE',  ( -69.77438362644001302, 71.97411849586700328, -80.14847958357698587 ) ) ;
#11307=CIRCLE ( 'NONE', #13309, 4.500000000000003553 ) ;
#11308=CARTESIAN_POINT ( 'NONE',  ( -53.27438362644000591, 82.17411849586700612, -152.4984795835769944 ) ) ;
#11309=DIRECTION ( 'NONE',  ( 0.000000000000000000, 0.000000000000000000, 1.000000000000000000 ) ) ;
#11312=LINE ( 'NONE', #6521, #6504 ) ;
#11314=CARTESIAN_POINT ( 'NONE',  ( -52.77438362643999881, 65.17411849586700612, -147.9984795835769944 ) ) ;
#11316=VERTEX_POINT ( 'NONE', #2015 ) ;
#11317=VECTOR ( 'NONE', #12624, 1000.000000000000000 ) ;
#11318=VERTEX_POINT ( 'NONE', #8928 ) ;
#11321=EDGE_CURVE ( 'NONE', #10418, #9704, #3559, .T. ) ;
#11325=EDGE_CURVE ( 'NONE', #2361, #9205, #8265, .T. ) ;
#11327=CARTESIAN_POINT ( 'NONE',  ( -104.2743836264399988, 111.1741184958670061, -67.49847958357700861 ) ) ;
#11329=CARTESIAN_POINT ( 'NONE',  ( -66.62325245518700001, 97.86074886511960358, -93.49847958357699440 ) ) ;
#11330=DIRECTION ( 'NONE',  ( 0.000000000000000000, 0.000000000000000000, -1.000000000000000000 ) ) ;
#11334=DIRECTION ( 'NONE',  ( 0.000000000000000000, 1.000000000000000000, 0.000000000000000000 ) ) ;
#11336=CARTESIAN_POINT ( 'NONE',  ( -52.77438362644000591, 99.17411849586700612, -79.59847958357700293 ) ) ;
#11344=EDGE_CURVE ( 'NONE', #9860, #12733, #11488, .T. ) ;
#11346=CARTESIAN_POINT ( 'NONE',  ( -52.77438362644000591, 99.17411849586700612, -152.4984795835769944 ) ) ;
#11348=EDGE_CURVE ( 'NONE', #13148, #2388, #9485, .T. ) ;
#11349=EDGE_CURVE ( 'NONE', #15330, #9916, #10221, .T. ) ;
#11351=CARTESIAN_POINT ( 'NONE',  ( -65.90140028023573393, 75.17411849586525818, -44.99847958359791278 ) ) ;
#11352=DIRECTION ( 'NONE',  ( 0.000000000000000000, 0.000000000000000000, 1.000000000000000000 ) ) ;
#11353=FACE_OUTER_BOUND ( 'NONE', #4940, .T. ) ;
#11355=CARTESIAN_POINT ( 'NONE',  ( -86.77438362644100778, 99.17411849586700612, -146.8195303338917768 ) ) ;
#11356=DIRECTION ( 'NONE',  ( 0.000000000000000000, 0.000000000000000000, -1.000000000000000000 ) ) ;
#11357=EDGE_LOOP ( 'NONE', ( #10337, #11779, #2081 ) ) ;
#11358=CARTESIAN_POINT ( 'NONE',  ( -73.64736697264743270, 75.17411849586699191, -58.99847958357700151 ) ) ;
#11360=VERTEX_POINT ( 'NONE', #8856 ) ;
#11366=LINE ( 'NONE', #7664, #15126 ) ;
#11367=DIRECTION ( 'NONE',  ( 0.000000000000000000, 0.000000000000000000, 1.000000000000000000 ) ) ;
#11368=DIRECTION ( 'NONE',  ( 1.000000000000000000, 0.000000000000000000, 0.000000000000000000 ) ) ;
#11369=DIRECTION ( 'NONE',  ( 0.000000000000000000, 0.000000000000000000, -1.000000000000000000 ) ) ;
#11370=DIRECTION ( 'NONE',  ( 0.4999999999999998890, -0.8660254037844387076, 0.000000000000000000 ) ) ;
#11371=CARTESIAN_POINT ( 'NONE',  ( -50.07438362643999596, 65.17411849586700612, -145.4984795835769944 ) ) ;
#11372=CARTESIAN_POINT ( 'NONE',  ( -52.77438362644100067, 99.17411849586700612, -145.2984795835770058 ) ) ;
#11373=ORIENTED_EDGE ( 'NONE', *, *, #1398, .F. ) ;
#11382=EDGE_CURVE ( 'NONE', #3615, #1459, #5800, .T. ) ;
#11383=DIRECTION ( 'NONE',  ( 0.000000000000000000, 0.000000000000000000, -1.000000000000000000 ) ) ;
#11384=EDGE_LOOP ( 'NONE', ( #10576, #10747 ) ) ;
#11396=DIRECTION ( 'NONE',  ( 1.000000000000000000, 0.000000000000000000, 0.000000000000000000 ) ) ;
#11398=CARTESIAN_POINT ( 'NONE',  ( -57.27438362644000591, 65.17411849586700612, -152.4984795835769944 ) ) ;
#11405=ORIENTED_EDGE ( 'NONE', *, *, #2411, .T. ) ;
#11406=CARTESIAN_POINT ( 'NONE',  ( -59.27438362644000591, 82.17411849586700612, -80.14847958357698587 ) ) ;
#11407=EDGE_CURVE ( 'NONE', #4297, #7989, #14198, .T. ) ;
#11408=EDGE_LOOP ( 'NONE', ( #14537, #6679 ) ) ;
#11410=ORIENTED_EDGE ( 'NONE', *, *, #8692, .T. ) ;
#11415=EDGE_CURVE ( 'NONE', #11629, #13427, #1083, .T. ) ;
#11416=FACE_BOUND ( 'NONE', #12852, .T. ) ;
#11417=EDGE_CURVE ( 'NONE', #10624, #2361, #2245, .T. ) ;
#11419=CARTESIAN_POINT ( 'NONE',  ( -86.77438362644001302, 99.17411849586700612, -152.4984795835769944 ) ) ;
#11421=DIRECTION ( 'NONE',  ( -1.000000000000000000, 0.000000000000000000, 0.000000000000000000 ) ) ;
#11422=DIRECTION ( 'NONE',  ( 1.000000000000000000, 0.000000000000000000, 0.000000000000000000 ) ) ;
#11425=CIRCLE ( 'NONE', #7482, 2.699999999999993960 ) ;
#11428=CARTESIAN_POINT ( 'NONE',  ( -88.81638362644000040, 65.17411849586700612, -147.9984795835769944 ) ) ;
#11430=ORIENTED_EDGE ( 'NONE', *, *, #7169, .F. ) ;
#11432=CARTESIAN_POINT ( 'NONE',  ( -69.77438362644001302, 82.17411849586700612, -81.84847958357698872 ) ) ;
#11433=ORIENTED_EDGE ( 'NONE', *, *, #5666, .F. ) ;
#11436=ORIENTED_EDGE ( 'NONE', *, *, #12964, .F. ) ;
#11438=CIRCLE ( 'NONE', #9686, 2.042000000000002036 ) ;
#11440=CIRCLE ( 'NONE', #13433, 17.00000000000000000 ) ;
#11442=DIRECTION ( 'NONE',  ( 0.000000000000000000, 0.000000000000000000, -1.000000000000000000 ) ) ;
#11443=ADVANCED_FACE ( 'NONE', ( #1003 ), #15112, .F. ) ;
#11444=VECTOR ( 'NONE', #10475, 1000.000000000000000 ) ;
#11446=DIRECTION ( 'NONE',  ( 0.000000000000000000, 1.000000000000000000, 0.000000000000000000 ) ) ;
#11447=CARTESIAN_POINT ( 'NONE',  ( -69.77438362644001302, 81.46011849586699327, -83.44847958357698303 ) ) ;
#11448=DIRECTION ( 'NONE',  ( 1.000000000000000000, 0.000000000000000000, 0.000000000000000000 ) ) ;
#11451=VERTEX_POINT ( 'NONE', #4500 ) ;
#11452=DIRECTION ( 'NONE',  ( -1.000000000000000000, 0.000000000000000000, 0.000000000000000000 ) ) ;
#11455=CIRCLE ( 'NONE', #10200, 2.500000000000002220 ) ;
#11457=DIRECTION ( 'NONE',  ( 1.000000000000000000, 0.000000000000000000, 0.000000000000000000 ) ) ;
#11458=CYLINDRICAL_SURFACE ( 'NONE', #5145, 4.250000000000003553 ) ;
#11459=CIRCLE ( 'NONE', #14678, 10.50000000000000178 ) ;
#11461=CARTESIAN_POINT ( 'NONE',  ( -69.77438362644001302, 82.17411849586700612, -93.49847958357699440 ) ) ;
#11465=CIRCLE ( 'NONE', #4536, 8.000000000000007105 ) ;
#11467=CARTESIAN_POINT ( 'NONE',  ( -52.77438362644000591, 99.17411849586700612, -86.49847958357699440 ) ) ;
#11468=ORIENTED_EDGE ( 'NONE', *, *, #8922, .T. ) ;
#11469=ORIENTED_EDGE ( 'NONE', *, *, #8935, .F. ) ;
#11470=EDGE_LOOP ( 'NONE', ( #12497, #6789, #568 ) ) ;
#11471=ORIENTED_EDGE ( 'NONE', *, *, #14659, .F. ) ;
#11472=CIRCLE ( 'NONE', #8744, 4.499999999999997335 ) ;
#11473=AXIS2_PLACEMENT_3D ( 'NONE', #15114, #12968, #8227 ) ;
#11474=ORIENTED_EDGE ( 'NONE', *, *, #8292, .T. ) ;
#11479=CARTESIAN_POINT ( 'NONE',  ( -69.77438362644001302, 82.17411849586700612, -93.49847958357699440 ) ) ;
#11480=EDGE_CURVE ( 'NONE', #10868, #7835, #3650, .T. ) ;
#11481=DIRECTION ( 'NONE',  ( 0.000000000000000000, 0.000000000000000000, 1.000000000000000000 ) ) ;
#11486=FACE_OUTER_BOUND ( 'NONE', #10211, .T. ) ;
#11487=AXIS2_PLACEMENT_3D ( 'NONE', #8510, #13255, #5978 ) ;
#11488=LINE ( 'NONE', #853, #6309 ) ;
#11489=ORIENTED_EDGE ( 'NONE', *, *, #7459, .F. ) ;
#11490=DIRECTION ( 'NONE',  ( 0.000000000000000000, 0.000000000000000000, -1.000000000000000000 ) ) ;
#11492=ORIENTED_EDGE ( 'NONE', *, *, #11026, .F. ) ;
#11493=ORIENTED_EDGE ( 'NONE', *, *, #7519, .F. ) ;
#11494=DIRECTION ( 'NONE',  ( -1.000000000000000000, 0.000000000000000000, 0.000000000000000000 ) ) ;
#11498=VECTOR ( 'NONE', #1541, 1000.000000000000000 ) ;
#11499=DIRECTION ( 'NONE',  ( 0.000000000000000000, 0.000000000000000000, -1.000000000000000000 ) ) ;
#11501=LINE ( 'NONE', #13978, #926 ) ;
#11504=ORIENTED_EDGE ( 'NONE', *, *, #12952, .F. ) ;
#11508=AXIS2_PLACEMENT_3D ( 'NONE', #10563, #84, #14209 ) ;
#11510=EDGE_CURVE ( 'NONE', #1497, #13889, #14118, .T. ) ;
#11511=VERTEX_POINT ( 'NONE', #9222 ) ;
#11512=DIRECTION ( 'NONE',  ( 0.000000000000000000, 1.000000000000000000, 0.000000000000000000 ) ) ;
#11513=ORIENTED_EDGE ( 'NONE', *, *, #11480, .F. ) ;
#11515=ORIENTED_EDGE ( 'NONE', *, *, #7749, .T. ) ;
#11516=ADVANCED_FACE ( 'NONE', ( #12965 ), #13963, .F. ) ;
#11519=EDGE_CURVE ( 'NONE', #2023, #11281, #3300, .T. ) ;
#11521=EDGE_CURVE ( 'NONE', #14726, #8931, #2812, .T. ) ;
#11522=VECTOR ( 'NONE', #8853, 1000.000000000000000 ) ;
#11524=CARTESIAN_POINT ( 'NONE',  ( -71.19907181086536241, 98.11283521318516421, -94.49649318951415466 ) ) ;
#11525=PLANE ( 'NONE',  #14670 ) ;
#11529=AXIS2_PLACEMENT_3D ( 'NONE', #8993, #8919, #11396 ) ;
#11530=DIRECTION ( 'NONE',  ( -1.000000000000000000, 0.000000000000000000, 0.000000000000000000 ) ) ;
#11532=EDGE_LOOP ( 'NONE', ( #4686, #88, #1808, #9553, #7060, #1 ) ) ;
#11534=ADVANCED_FACE ( 'NONE', ( #930 ), #11983, .T. ) ;
#11536=FACE_OUTER_BOUND ( 'NONE', #12751, .T. ) ;
#11537=DIRECTION ( 'NONE',  ( 1.000000000000000000, 0.000000000000000000, 0.000000000000000000 ) ) ;
#11538=VECTOR ( 'NONE', #3590, 1000.000000000000000 ) ;
#11539=CARTESIAN_POINT ( 'NONE',  ( -54.81638362644100226, 97.99516924618178848, -150.4984795835770228 ) ) ;
#11540=LINE ( 'NONE', #3163, #10614 ) ;
#11541=CARTESIAN_POINT ( 'NONE',  ( -52.77438362644100067, 99.17411849586700612, -146.8195303338917768 ) ) ;
#11543=DIRECTION ( 'NONE',  ( 0.000000000000000000, 1.000000000000000000, 0.000000000000000000 ) ) ;
#11546=CARTESIAN_POINT ( 'NONE',  ( -53.79538362643999960, 66.94254237039483257, -147.9984795835769944 ) ) ;
#11547=ORIENTED_EDGE ( 'NONE', *, *, #10924, .T. ) ;
#11548=ORIENTED_EDGE ( 'NONE', *, *, #149, .F. ) ;
#11550=ORIENTED_EDGE ( 'NONE', *, *, #2677, .T. ) ;
#11552=EDGE_LOOP ( 'NONE', ( #12400, #4456, #13907, #10811, #11909 ) ) ;
#11553=ORIENTED_EDGE ( 'NONE', *, *, #7430, .F. ) ;
#11554=AXIS2_PLACEMENT_3D ( 'NONE', #6930, #15285, #4747 ) ;
#11560=CARTESIAN_POINT ( 'NONE',  ( -75.19401665569927218, 66.06115545897768015, -81.84847958357697451 ) ) ;
#11562=PLANE ( 'NONE',  #693 ) ;
#11565=DIRECTION ( 'NONE',  ( -0.000000000000000000, -0.000000000000000000, 1.000000000000000000 ) ) ;
#11566=CARTESIAN_POINT ( 'NONE',  ( -88.81638362644100937, 97.99516924618178848, -147.9984795835769944 ) ) ;
#11568=VERTEX_POINT ( 'NONE', #6224 ) ;
#11570=VERTEX_POINT ( 'NONE', #10932 ) ;
#11571=EDGE_LOOP ( 'NONE', ( #10373, #6941, #690 ) ) ;
#11574=DIRECTION ( 'NONE',  ( 0.000000000000000000, 0.000000000000000000, 1.000000000000000000 ) ) ;
#11576=FACE_OUTER_BOUND ( 'NONE', #1721, .T. ) ;
#11577=CARTESIAN_POINT ( 'NONE',  ( -69.43626855224094641, 75.17411849586699191, -43.99847958365483436 ) ) ;
#11578=LINE ( 'NONE', #8161, #6754 ) ;
#11579=CARTESIAN_POINT ( 'NONE',  ( -52.77438362644100067, 99.17411849586700612, -150.4984795835770228 ) ) ;
#11580=DIRECTION ( 'NONE',  ( -1.000000000000000000, 0.000000000000000000, 0.000000000000000000 ) ) ;
#11586=VERTEX_POINT ( 'NONE', #13421 ) ;
#11587=AXIS2_PLACEMENT_3D ( 'NONE', #12664, #4520, #11421 ) ;
#11588=ORIENTED_EDGE ( 'NONE', *, *, #13036, .T. ) ;
#11590=ORIENTED_EDGE ( 'NONE', *, *, #197, .F. ) ;
#11593=ORIENTED_EDGE ( 'NONE', *, *, #8602, .F. ) ;
#11597=AXIS2_PLACEMENT_3D ( 'NONE', #12270, #1642, #11106 ) ;
#11600=CARTESIAN_POINT ( 'NONE',  ( -52.77438362643999881, 67.53201699523744139, -147.9984795835769944 ) ) ;
#11601=EDGE_CURVE ( 'NONE', #4413, #10872, #7384, .T. ) ;
#11604=ORIENTED_EDGE ( 'NONE', *, *, #5728, .T. ) ;
#11605=EDGE_CURVE ( 'NONE', #5950, #9201, #11945, .T. ) ;
#11616=CIRCLE ( 'NONE', #12372, 10.20000000000000107 ) ;
#11619=DIRECTION ( 'NONE',  ( -1.000000000000000000, 0.000000000000000000, 0.000000000000000000 ) ) ;
#11622=ORIENTED_EDGE ( 'NONE', *, *, #13334, .F. ) ;
#11623=LINE ( 'NONE', #751, #8017 ) ;
#11625=EDGE_CURVE ( 'NONE', #2640, #3597, #11270, .T. ) ;
#11627=ADVANCED_FACE ( 'NONE', ( #2474 ), #1544, .F. ) ;
#11629=VERTEX_POINT ( 'NONE', #10787 ) ;
#11630=ORIENTED_EDGE ( 'NONE', *, *, #667, .T. ) ;
#11636=DIRECTION ( 'NONE',  ( 0.000000000000000000, -0.000000000000000000, 1.000000000000000000 ) ) ;
#11638=CARTESIAN_POINT ( 'NONE',  ( 0.000000000000000000, 0.000000000000000000, -79.59847958357700293 ) ) ;
#11641=ORIENTED_EDGE ( 'NONE', *, *, #13896, .T. ) ;
#11644=DIRECTION ( 'NONE',  ( 0.000000000000000000, 0.000000000000000000, 1.000000000000000000 ) ) ;
#11650=CARTESIAN_POINT ( 'NONE',  ( -91.27438362643999881, 65.17411849586700612, -145.4984795835769660 ) ) ;
#11653=CARTESIAN_POINT ( 'NONE',  ( -65.73898050152220662, 64.78624853950366003, -83.44847958357698303 ) ) ;
#11654=VERTEX_POINT ( 'NONE', #14341 ) ;
#11655=CARTESIAN_POINT ( 'NONE',  ( -73.01311196519618818, 67.29799558322736175, -81.84847958357697451 ) ) ;
#11656=ORIENTED_EDGE ( 'NONE', *, *, #3349, .T. ) ;
#11658=DIRECTION ( 'NONE',  ( 0.000000000000000000, 0.000000000000000000, 1.000000000000000000 ) ) ;
#11659=ORIENTED_EDGE ( 'NONE', *, *, #2992, .T. ) ;
#11661=ORIENTED_EDGE ( 'NONE', *, *, #4708, .F. ) ;
#11665=CARTESIAN_POINT ( 'NONE',  ( -69.77438362644001302, 90.17411849586700612, -58.99847958357700151 ) ) ;
#11667=CARTESIAN_POINT ( 'NONE',  ( -50.27438362643999881, 65.17411849586700612, -182.2484795835770228 ) ) ;
#11673=DIRECTION ( 'NONE',  ( 0.000000000000000000, 0.000000000000000000, -1.000000000000000000 ) ) ;
#11674=EDGE_LOOP ( 'NONE', ( #1596, #208 ) ) ;
#11675=CIRCLE ( 'NONE', #1526, 5.500000000000005329 ) ;
#11679=EDGE_CURVE ( 'NONE', #11586, #13082, #8528, .T. ) ;
#11681=CARTESIAN_POINT ( 'NONE',  ( -69.77438362644100778, 82.17411849586699191, -79.49847958357700861 ) ) ;
#11682=EDGE_CURVE ( 'NONE', #14025, #3986, #10767, .T. ) ;
#11683=AXIS2_PLACEMENT_3D ( 'NONE', #7023, #11749, #7878 ) ;
#11685=DIRECTION ( 'NONE',  ( 1.287488025362404182E-15, 1.000000000000000000, 0.000000000000000000 ) ) ;
#11692=ORIENTED_EDGE ( 'NONE', *, *, #5660, .T. ) ;
#11696=ADVANCED_FACE ( 'NONE', ( #8678 ), #3953, .T. ) ;
#11697=ORIENTED_EDGE ( 'NONE', *, *, #5951, .T. ) ;
#11701=ORIENTED_EDGE ( 'NONE', *, *, #13815, .T. ) ;
#11703=VECTOR ( 'NONE', #3664, 1000.000000000000000 ) ;
#11705=ADVANCED_FACE ( 'NONE', ( #13500, #13578 ), #533, .T. ) ;
#11707=CARTESIAN_POINT ( 'NONE',  ( -101.2743836264399988, 111.1741184958670061, -79.49847958357700861 ) ) ;
#11708=CYLINDRICAL_SURFACE ( 'NONE', #12074, 9.999999999999994671 ) ;
#11711=ADVANCED_FACE ( 'NONE', ( #9057 ), #12486, .F. ) ;
#11712=CARTESIAN_POINT ( 'NONE',  ( -56.85838362644099675, 99.17411849586700612, -147.9984795835769944 ) ) ;
#11714=DIRECTION ( 'NONE',  ( 0.000000000000000000, -1.000000000000000000, 0.000000000000000000 ) ) ;
#11718=EDGE_LOOP ( 'NONE', ( #11436, #2493, #3209, #2696 ) ) ;
#11719=DIRECTION ( 'NONE',  ( 0.000000000000000000, 0.000000000000000000, 1.000000000000000000 ) ) ;
#11720=AXIS2_PLACEMENT_3D ( 'NONE', #3407, #14036, #14183 ) ;
#11723=ORIENTED_EDGE ( 'NONE', *, *, #8917, .F. ) ;
#11729=CARTESIAN_POINT ( 'NONE',  ( -54.81638362644000040, 63.99516924618178848, -150.4984795835770228 ) ) ;
#11731=DIRECTION ( 'NONE',  ( 0.000000000000000000, 0.000000000000000000, -1.000000000000000000 ) ) ;
#11732=CONICAL_SURFACE ( 'NONE', #13468, 2.042000000000002036, 1.047197551196596965 ) ;
#11733=CARTESIAN_POINT ( 'NONE',  ( -69.77438362643999881, 89.17411849586052597, -43.99847958364157563 ) ) ;
#11734=FACE_OUTER_BOUND ( 'NONE', #870, .T. ) ;
#11737=FACE_BOUND ( 'NONE', #3596, .T. ) ;
#11738=AXIS2_PLACEMENT_3D ( 'NONE', #8068, #8383, #13124 ) ;
#11739=ORIENTED_EDGE ( 'NONE', *, *, #10634, .F. ) ;
#11740=DIRECTION ( 'NONE',  ( 0.000000000000000000, -1.000000000000000000, 0.000000000000000000 ) ) ;
#11743=CIRCLE ( 'NONE', #4815, 3.000000000000002665 ) ;
#11746=CARTESIAN_POINT ( 'NONE',  ( -69.77438362644001302, 82.17411849586700612, -81.84847958357698872 ) ) ;
#11749=DIRECTION ( 'NONE',  ( 0.000000000000000000, 0.000000000000000000, -1.000000000000000000 ) ) ;
#11750=DIRECTION ( 'NONE',  ( -1.000000000000000000, 0.000000000000000000, 0.000000000000000000 ) ) ;
#11752=AXIS2_PLACEMENT_3D ( 'NONE', #12416, #9765, #14422 ) ;
#11756=DIRECTION ( 'NONE',  ( 0.000000000000000000, 0.000000000000000000, -1.000000000000000000 ) ) ;
#11757=CARTESIAN_POINT ( 'NONE',  ( -54.81638362644000040, 63.99516924618178848, -147.9984795835769944 ) ) ;
#11758=VERTEX_POINT ( 'NONE', #6675 ) ;
#11761=VERTEX_POINT ( 'NONE', #2943 ) ;
#11762=ADVANCED_FACE ( 'NONE', ( #7684 ), #3165, .F. ) ;
#11768=FACE_OUTER_BOUND ( 'NONE', #11470, .T. ) ;
#11769=CARTESIAN_POINT ( 'NONE',  ( -66.62325245518700001, 94.57411849586699759, -93.49847958357699440 ) ) ;
#11770=CARTESIAN_POINT ( 'NONE',  ( -88.81638362644000040, 63.99516924618178848, -147.9984795835769944 ) ) ;
#11776=EDGE_LOOP ( 'NONE', ( #1008, #11471, #4795, #7076, #5587 ) ) ;
#11779=ORIENTED_EDGE ( 'NONE', *, *, #5470, .F. ) ;
#11783=AXIS2_PLACEMENT_3D ( 'NONE', #10640, #9470, #9547 ) ;
#11789=DIRECTION ( 'NONE',  ( -0.000000000000000000, -0.000000000000000000, 1.000000000000000000 ) ) ;
#11791=DIRECTION ( 'NONE',  ( 0.5000000000000003331, 0.8660254037844384856, 0.000000000000000000 ) ) ;
#11792=CARTESIAN_POINT ( 'NONE',  ( -52.77438362644000591, 99.17411849586700612, -86.49847958357699440 ) ) ;
#11793=DIRECTION ( 'NONE',  ( 1.000000000000000000, 0.000000000000000000, 0.000000000000000000 ) ) ;
#11795=DIRECTION ( 'NONE',  ( 0.000000000000000000, 0.000000000000000000, -1.000000000000000000 ) ) ;
#11796=ORIENTED_EDGE ( 'NONE', *, *, #7538, .T. ) ;
#11797=FACE_OUTER_BOUND ( 'NONE', #7765, .T. ) ;
#11798=AXIS2_PLACEMENT_3D ( 'NONE', #5608, #4499, #12804 ) ;
#11799=EDGE_CURVE ( 'NONE', #15133, #2626, #11312, .T. ) ;
#11804=AXIS2_PLACEMENT_3D ( 'NONE', #14551, #13402, #360 ) ;
#11805=EDGE_CURVE ( 'NONE', #5361, #3573, #1780, .T. ) ;
#11807=LINE ( 'NONE', #11729, #1650 ) ;
#11809=LINE ( 'NONE', #1175, #10963 ) ;
#11810=CARTESIAN_POINT ( 'NONE',  ( -69.77438362644001302, 81.46011849586699327, -81.84847958357697451 ) ) ;
#11812=EDGE_CURVE ( 'NONE', #13217, #12323, #681, .T. ) ;
#11813=CARTESIAN_POINT ( 'NONE',  ( -53.77438362644000591, 82.17411849586700612, -112.9984795835769944 ) ) ;
#11815=CARTESIAN_POINT ( 'NONE',  ( -69.77438362644001302, 82.17411849586700612, -150.4984795835769944 ) ) ;
#11816=DIRECTION ( 'NONE',  ( 0.000000000000000000, 0.000000000000000000, 1.000000000000000000 ) ) ;
#11817=VERTEX_POINT ( 'NONE', #4252 ) ;
#11818=DIRECTION ( 'NONE',  ( 0.8660254037844387076, 0.4999999999999998890, 0.000000000000000000 ) ) ;
#11820=ORIENTED_EDGE ( 'NONE', *, *, #8012, .F. ) ;
#11821=EDGE_LOOP ( 'NONE', ( #7173, #8516, #8662, #12947 ) ) ;
#11823=ADVANCED_FACE ( 'NONE', ( #5507 ), #12563, .F. ) ;
#11832=AXIS2_PLACEMENT_3D ( 'NONE', #13682, #6560, #8941 ) ;
#11833=DIRECTION ( 'NONE',  ( 0.000000000000000000, 0.000000000000000000, -1.000000000000000000 ) ) ;
#11835=LINE ( 'NONE', #11600, #4143 ) ;
#11836=CARTESIAN_POINT ( 'NONE',  ( -96.77438362643999881, 59.67411849586700612, -15.85886927678779834 ) ) ;
#11838=VERTEX_POINT ( 'NONE', #11770 ) ;
#11839=( LENGTH_UNIT ( ) NAMED_UNIT ( * ) SI_UNIT ( .MILLI., .METRE. ) );
#11841=ORIENTED_EDGE ( 'NONE', *, *, #331, .F. ) ;
#11842=VECTOR ( 'NONE', #14358, 1000.000000000000000 ) ;
#11843=PLANE ( 'NONE',  #13666 ) ;
#11845=FACE_OUTER_BOUND ( 'NONE', #8610, .T. ) ;
#11846=LINE ( 'NONE', #2219, #9757 ) ;
#11847=CARTESIAN_POINT ( 'NONE',  ( -88.81638362644100937, 97.99516924618178848, -147.9984795835769944 ) ) ;
#11849=DIRECTION ( 'NONE',  ( 0.000000000000000000, 1.000000000000000000, 0.000000000000000000 ) ) ;
#11850=CARTESIAN_POINT ( 'NONE',  ( -62.02799568714584666, 0.000000000000000000, -79.59847958357700293 ) ) ;
#11851=CIRCLE ( 'NONE', #5175, 2.042000000000002036 ) ;
#11853=DIRECTION ( 'NONE',  ( 1.000000000000000000, 0.000000000000000000, 0.000000000000000000 ) ) ;
#11855=ORIENTED_EDGE ( 'NONE', *, *, #5654, .T. ) ;
#11856=FACE_BOUND ( 'NONE', #11384, .T. ) ;
#11858=ORIENTED_EDGE ( 'NONE', *, *, #3952, .F. ) ;
#11860=VERTEX_POINT ( 'NONE', #3232 ) ;
#11862=DIRECTION ( 'NONE',  ( 0.000000000000000000, 0.000000000000000000, -1.000000000000000000 ) ) ;
#11863=CIRCLE ( 'NONE', #5429, 8.124999999999992895 ) ;
#11865=DIRECTION ( 'NONE',  ( 0.000000000000000000, 0.000000000000000000, -1.000000000000000000 ) ) ;
#11867=DIRECTION ( 'NONE',  ( 0.000000000000000000, 0.000000000000000000, -1.000000000000000000 ) ) ;
#11868=LINE ( 'NONE', #65, #1938 ) ;
#11870=FACE_BOUND ( 'NONE', #9594, .T. ) ;
#11871=EDGE_CURVE ( 'NONE', #9154, #13931, #981, .T. ) ;
#11875=DIRECTION ( 'NONE',  ( 0.000000000000000000, 0.000000000000000000, -1.000000000000000000 ) ) ;
#11877=ORIENTED_EDGE ( 'NONE', *, *, #5559, .T. ) ;
#11878=ORIENTED_EDGE ( 'NONE', *, *, #526, .T. ) ;
#11879=CARTESIAN_POINT ( 'NONE',  ( -86.77438362644100778, 99.17411849586700612, -149.9984795835770228 ) ) ;
#11882=ADVANCED_FACE ( 'NONE', ( #5668 ), #5976, .F. ) ;
#11883=CARTESIAN_POINT ( 'NONE',  ( -80.52077156573417938, 60.67411849586702743, -152.4984795835769944 ) ) ;
#11885=CARTESIAN_POINT ( 'NONE',  ( -86.77438362644001302, 99.17411849586700612, -86.49847958357699440 ) ) ;
#11888=DIRECTION ( 'NONE',  ( -0.000000000000000000, -0.000000000000000000, -1.000000000000000000 ) ) ;
#11890=CARTESIAN_POINT ( 'NONE',  ( -52.77438362643999881, 67.53201699523744139, -150.4984795835770228 ) ) ;
#11891=ORIENTED_EDGE ( 'NONE', *, *, #4046, .T. ) ;
#11893=ORIENTED_EDGE ( 'NONE', *, *, #7660, .T. ) ;
#11894=ORIENTED_EDGE ( 'NONE', *, *, #8652, .F. ) ;
#11895=VERTEX_POINT ( 'NONE', #12784 ) ;
#11898=DIRECTION ( 'NONE',  ( 0.000000000000000000, 0.000000000000000000, 1.000000000000000000 ) ) ;
#11903=EDGE_CURVE ( 'NONE', #8783, #3610, #10365, .T. ) ;
#11905=LINE ( 'NONE', #11667, #15175 ) ;
#11908=ADVANCED_FACE ( 'NONE', ( #9197 ), #12701, .F. ) ;
#11909=ORIENTED_EDGE ( 'NONE', *, *, #2499, .T. ) ;
#11911=LINE ( 'NONE', #15310, #10825 ) ;
#11914=DIRECTION ( 'NONE',  ( -0.000000000000000000, -0.000000000000000000, 1.000000000000000000 ) ) ;
#11915=EDGE_CURVE ( 'NONE', #3573, #1497, #287, .T. ) ;
#11917=ORIENTED_EDGE ( 'NONE', *, *, #2223, .F. ) ;
#11918=VECTOR ( 'NONE', #4636, 1000.000000000000000 ) ;
#11921=DIRECTION ( 'NONE',  ( 0.000000000000000000, 0.000000000000000000, 1.000000000000000000 ) ) ;
#11924=DIRECTION ( 'NONE',  ( 0.000000000000000000, 0.000000000000000000, -1.000000000000000000 ) ) ;
#11925=DIRECTION ( 'NONE',  ( 0.000000000000000000, 0.000000000000000000, -1.000000000000000000 ) ) ;
#11926=PLANE ( 'NONE',  #14019 ) ;
#11929=CARTESIAN_POINT ( 'NONE',  ( -87.79538362644099436, 97.40569462133919387, -147.9984795835769944 ) ) ;
#11930=VERTEX_POINT ( 'NONE', #7131 ) ;
#11931=DIRECTION ( 'NONE',  ( 0.000000000000000000, -1.000000000000000000, 0.000000000000000000 ) ) ;
#11933=ORIENTED_EDGE ( 'NONE', *, *, #8119, .T. ) ;
#11934=ORIENTED_EDGE ( 'NONE', *, *, #10099, .F. ) ;
#11937=DIRECTION ( 'NONE',  ( 1.287488025362404182E-15, 1.000000000000000000, 0.000000000000000000 ) ) ;
#11941=DIRECTION ( 'NONE',  ( 0.000000000000000000, 0.000000000000000000, 1.000000000000000000 ) ) ;
#11942=CARTESIAN_POINT ( 'NONE',  ( -54.81638362644000040, 65.17411849586700612, -147.9984795835769944 ) ) ;
#11943=CARTESIAN_POINT ( 'NONE',  ( -65.78565528768382364, 67.29799558322736175, -83.44847958357698303 ) ) ;
#11945=LINE ( 'NONE', #5201, #6549 ) ;
#11946=CIRCLE ( 'NONE', #13440, 5.499999999999998224 ) ;
#11948=FACE_OUTER_BOUND ( 'NONE', #13584, .T. ) ;
#11949=ORIENTED_EDGE ( 'NONE', *, *, #4156, .F. ) ;
#11951=ORIENTED_EDGE ( 'NONE', *, *, #322, .F. ) ;
#11952=ORIENTED_EDGE ( 'NONE', *, *, #5456, .T. ) ;
#11959=DIRECTION ( 'NONE',  ( 1.000000000000000000, 0.000000000000000000, 0.000000000000000000 ) ) ;
#11960=DIRECTION ( 'NONE',  ( 0.000000000000000000, 0.7071067811865510144, 0.7071067811865441310 ) ) ;
#11962=CARTESIAN_POINT ( 'NONE',  ( -53.79538362643999960, 63.40569462133918677, -147.9984795835769944 ) ) ;
#11964=AXIS2_PLACEMENT_3D ( 'NONE', #11479, #847, #9374 ) ;
#11967=ORIENTED_EDGE ( 'NONE', *, *, #14653, .F. ) ;
#11970=VECTOR ( 'NONE', #13, 1000.000000000000114 ) ;
#11976=ORIENTED_EDGE ( 'NONE', *, *, #15220, .F. ) ;
#11977=VECTOR ( 'NONE', #885, 1000.000000000000000 ) ;
#11979=EDGE_CURVE ( 'NONE', #10427, #12362, #1056, .T. ) ;
#11980=VECTOR ( 'NONE', #11875, 1000.000000000000000 ) ;
#11982=CARTESIAN_POINT ( 'NONE',  ( -84.07438362643999596, 65.17411849586700612, -145.2984795835770058 ) ) ;
#11983=CONICAL_SURFACE ( 'NONE', #5304, 10.49999999999999467, 0.7853981633974497223 ) ;
#11985=DIRECTION ( 'NONE',  ( 0.000000000000000000, 0.000000000000000000, 1.000000000000000000 ) ) ;
#11989=LINE ( 'NONE', #13091, #2776 ) ;
#11990=ADVANCED_FACE ( 'NONE', ( #15248 ), #4643, .T. ) ;
#11991=ORIENTED_EDGE ( 'NONE', *, *, #3722, .F. ) ;
#11996=EDGE_CURVE ( 'NONE', #8449, #1774, #12181, .T. ) ;
#12000=AXIS2_PLACEMENT_3D ( 'NONE', #61, #1154, #2395 ) ;
#12002=DIRECTION ( 'NONE',  ( 0.000000000000000000, 0.000000000000000000, 1.000000000000000000 ) ) ;
#12010=LINE ( 'NONE', #10846, #12980 ) ;
#12014=VERTEX_POINT ( 'NONE', #2762 ) ;
#12015=PLANE ( 'NONE',  #10021 ) ;
#12018=EDGE_LOOP ( 'NONE', ( #9084, #9764 ) ) ;
#12019=EDGE_CURVE ( 'NONE', #7621, #12917, #1035, .T. ) ;
#12020=ORIENTED_EDGE ( 'NONE', *, *, #3273, .T. ) ;
#12022=ADVANCED_FACE ( 'NONE', ( #10993 ), #362, .T. ) ;
#12024=CYLINDRICAL_SURFACE ( 'NONE', #901, 8.124999999999992895 ) ;
#12025=DIRECTION ( 'NONE',  ( 0.000000000000000000, 0.000000000000000000, 1.000000000000000000 ) ) ;
#12028=AXIS2_PLACEMENT_3D ( 'NONE', #6627, #5451, #14962 ) ;
#12029=CARTESIAN_POINT ( 'NONE',  ( -90.85838362644000199, 65.17411849586700612, -147.9984795835769944 ) ) ;
#12031=CARTESIAN_POINT ( 'NONE',  ( -80.52077156573417938, 0.000000000000000000, -73.34256232478206528 ) ) ;
#12033=DIRECTION ( 'NONE',  ( -1.000000000000000000, 0.000000000000000000, 0.000000000000000000 ) ) ;
#12034=EDGE_LOOP ( 'NONE', ( #5439, #5207, #6381, #1997, #13215 ) ) ;
#12036=ORIENTED_EDGE ( 'NONE', *, *, #2209, .F. ) ;
#12037=ORIENTED_EDGE ( 'NONE', *, *, #12571, .T. ) ;
#12039=CIRCLE ( 'NONE', #12536, 2.500000000000002220 ) ;
#12042=DIRECTION ( 'NONE',  ( -1.000000000000000000, 0.000000000000000000, 0.000000000000000000 ) ) ;
#12043=FACE_OUTER_BOUND ( 'NONE', #7814, .T. ) ;
#12046=CARTESIAN_POINT ( 'NONE',  ( -54.81638362644100226, 97.99516924618178848, -147.9984795835769944 ) ) ;
#12049=CARTESIAN_POINT ( 'NONE',  ( -90.85838362644000199, 65.17411849586700612, -147.9984795835769944 ) ) ;
#12050=PLANE ( 'NONE',  #12715 ) ;
#12051=AXIS2_PLACEMENT_3D ( 'NONE', #10027, #1730, #5313 ) ;
#12055=VERTEX_POINT ( 'NONE', #6502 ) ;
#12061=B_SPLINE_CURVE_WITH_KNOTS ( 'NONE', 3,
 ( #8322, #3430, #12895, #13068, #6092, #13138, #12191, #3967 ),
 .UNSPECIFIED., .F., .F.,
 ( 4, 2, 2, 4 ),
 ( 0.04315383327195209534, 0.04413750674003968227, 0.04512118020812726227, 0.04708852714430240144 ),
 .UNSPECIFIED. ) ;
#12062=CIRCLE ( 'NONE', #12305, 8.124999999999992895 ) ;
#12063=FACE_OUTER_BOUND ( 'NONE', #9843, .T. ) ;
#12065=CARTESIAN_POINT ( 'NONE',  ( -35.27438362644000591, 60.67411849586700612, -79.49847958357700861 ) ) ;
#12067=DIRECTION ( 'NONE',  ( 0.000000000000000000, 0.000000000000000000, -1.000000000000000000 ) ) ;
#12068=EDGE_CURVE ( 'NONE', #1225, #10774, #7740, .T. ) ;
#12070=ORIENTED_EDGE ( 'NONE', *, *, #11871, .F. ) ;
#12073=EDGE_CURVE ( 'NONE', #8497, #2784, #7495, .T. ) ;
#12074=AXIS2_PLACEMENT_3D ( 'NONE', #14112, #11867, #4730 ) ;
#12082=AXIS2_PLACEMENT_3D ( 'NONE', #4018, #6445, #7378 ) ;
#12083=EDGE_CURVE ( 'NONE', #8800, #1856, #2766, .T. ) ;
#12084=DIRECTION ( 'NONE',  ( -1.000000000000000000, 0.000000000000000000, 0.000000000000000000 ) ) ;
#12086=DIRECTION ( 'NONE',  ( 0.000000000000000000, 0.000000000000000000, 1.000000000000000000 ) ) ;
#12087=CARTESIAN_POINT ( 'NONE',  ( -52.77438362643999881, 65.17411849586700612, -147.9984795835769944 ) ) ;
#12088=DIRECTION ( 'NONE',  ( 1.000000000000000000, 0.000000000000000000, 0.000000000000000000 ) ) ;
#12089=EDGE_CURVE ( 'NONE', #5361, #3573, #11440, .T. ) ;
#12091=DIRECTION ( 'NONE',  ( 0.000000000000000000, 1.000000000000000000, 0.000000000000000000 ) ) ;
#12095=ORIENTED_EDGE ( 'NONE', *, *, #8006, .F. ) ;
#12096=VERTEX_POINT ( 'NONE', #8966 ) ;
#12097=ORIENTED_EDGE ( 'NONE', *, *, #5246, .T. ) ;
#12099=DIRECTION ( 'NONE',  ( -0.000000000000000000, 0.000000000000000000, -1.000000000000000000 ) ) ;
#12101=EDGE_CURVE ( 'NONE', #12468, #11318, #2846, .T. ) ;
#12102=DIRECTION ( 'NONE',  ( 1.000000000000000000, 0.000000000000000000, 0.000000000000000000 ) ) ;
#12104=DIRECTION ( 'NONE',  ( -1.000000000000000000, 0.000000000000000000, -0.000000000000000000 ) ) ;
#12107=DIRECTION ( 'NONE',  ( 1.000000000000000000, 0.000000000000000000, 0.000000000000000000 ) ) ;
#12110=DIRECTION ( 'NONE',  ( -1.287488025362404182E-15, -1.000000000000000000, 0.000000000000000000 ) ) ;
#12112=ORIENTED_EDGE ( 'NONE', *, *, #5728, .F. ) ;
#12122=DIRECTION ( 'NONE',  ( 0.000000000000000000, 0.000000000000000000, 1.000000000000000000 ) ) ;
#12123=CARTESIAN_POINT ( 'NONE',  ( -59.02799568714584666, 60.67411849586701322, -79.59847958357700293 ) ) ;
#12125=LINE ( 'NONE', #1182, #11538 ) ;
#12129=LINE ( 'NONE', #1498, #1670 ) ;
#12130=ORIENTED_EDGE ( 'NONE', *, *, #2320, .T. ) ;
#12133=LINE ( 'NONE', #14825, #3506 ) ;
#12136=FACE_OUTER_BOUND ( 'NONE', #3686, .T. ) ;
#12137=CARTESIAN_POINT ( 'NONE',  ( -54.81638362644000040, 66.35306774555222376, -147.9984795835769944 ) ) ;
#12138=LINE ( 'NONE', #6261, #3906 ) ;
#12139=DIRECTION ( 'NONE',  ( 0.000000000000000000, -1.000000000000000000, 0.000000000000000000 ) ) ;
#12141=EDGE_LOOP ( 'NONE', ( #12850, #13054, #8548, #4335, #9994 ) ) ;
#12142=CARTESIAN_POINT ( 'NONE',  ( -69.77438362644100778, 92.17411849586700612, -79.49847958357700861 ) ) ;
#12145=VERTEX_POINT ( 'NONE', #9971 ) ;
#12149=CARTESIAN_POINT ( 'NONE',  ( -75.01311196519617397, 67.29799558322736175, -81.84847958357697451 ) ) ;
#12155=ORIENTED_EDGE ( 'NONE', *, *, #1529, .F. ) ;
#12156=ORIENTED_EDGE ( 'NONE', *, *, #2432, .T. ) ;
#12167=VECTOR ( 'NONE', #9248, 1000.000000000000000 ) ;
#12169=FACE_BOUND ( 'NONE', #13586, .T. ) ;
#12172=EDGE_CURVE ( 'NONE', #389, #191, #5014, .T. ) ;
#12177=VERTEX_POINT ( 'NONE', #14928 ) ;
#12178=ADVANCED_FACE ( 'NONE', ( #3000 ), #14623, .T. ) ;
#12179=AXIS2_PLACEMENT_3D ( 'NONE', #11432, #5554, #2120 ) ;
#12181=CIRCLE ( 'NONE', #4262, 4.499999999999997335 ) ;
#12185=PRESENTATION_STYLE_ASSIGNMENT (( #2648 ) ) ;
#12191=CARTESIAN_POINT ( 'NONE',  ( -73.03793661008894844, 89.17411849586700612, -44.70344037800717274 ) ) ;
#12193=DIRECTION ( 'NONE',  ( 0.000000000000000000, 0.000000000000000000, 1.000000000000000000 ) ) ;
#12195=EDGE_CURVE ( 'NONE', #9170, #10367, #13927, .T. ) ;
#12197=CARTESIAN_POINT ( 'NONE',  ( -62.02799568714584666, 164.3482369917340122, -73.34256232478206528 ) ) ;
#12198=VECTOR ( 'NONE', #6966, 1000.000000000000000 ) ;
#12199=ORIENTED_EDGE ( 'NONE', *, *, #11056, .F. ) ;
#12202=CARTESIAN_POINT ( 'NONE',  ( -52.77438362644000591, 99.17411849586700612, -145.4984795835769660 ) ) ;
#12203=ADVANCED_FACE ( 'NONE', ( #8263 ), #1124, .F. ) ;
#12207=DIRECTION ( 'NONE',  ( 0.000000000000000000, 0.000000000000000000, -1.000000000000000000 ) ) ;
#12208=CARTESIAN_POINT ( 'NONE',  ( -86.77438362643999881, 62.81621999649657084, -150.4984795835770228 ) ) ;
#12210=DIRECTION ( 'NONE',  ( 0.000000000000000000, 1.000000000000000000, 0.000000000000000000 ) ) ;
#12211=CARTESIAN_POINT ( 'NONE',  ( -69.77438362644001302, 82.17411849586700612, -152.4984795835769944 ) ) ;
#12212=CARTESIAN_POINT ( 'NONE',  ( -52.77438362644100067, 99.17411849586700612, -145.4984795835769944 ) ) ;
#12213=CARTESIAN_POINT ( 'NONE',  ( 0.000000000000000000, 0.000000000000000000, -79.59847958357700293 ) ) ;
#12214=EDGE_LOOP ( 'NONE', ( #14137, #10259 ) ) ;
#12217=ORIENTED_EDGE ( 'NONE', *, *, #8743, .F. ) ;
#12218=AXIS2_PLACEMENT_3D ( 'NONE', #5045, #7305, #12033 ) ;
#12221=ORIENTED_EDGE ( 'NONE', *, *, #8558, .T. ) ;
#12223=FACE_OUTER_BOUND ( 'NONE', #14721, .T. ) ;
#12224=CARTESIAN_POINT ( 'NONE',  ( -49.02438362644100067, 99.17411849586700612, -150.4984795835770228 ) ) ;
#12225=FACE_OUTER_BOUND ( 'NONE', #158, .T. ) ;
#12228=AXIS2_PLACEMENT_3D ( 'NONE', #1294, #6138, #6055 ) ;
#12229=DIRECTION ( 'NONE',  ( -1.000000000000000000, 0.000000000000000000, 0.000000000000000000 ) ) ;
#12230=DIRECTION ( 'NONE',  ( 0.000000000000000000, 0.000000000000000000, -1.000000000000000000 ) ) ;
#12231=CARTESIAN_POINT ( 'NONE',  ( -86.77438362644100778, 99.17411849586700612, -147.9984795835769944 ) ) ;
#12232=FACE_OUTER_BOUND ( 'NONE', #9862, .T. ) ;
#12235=CONICAL_SURFACE ( 'NONE', #7546, 2.042000000000002036, 1.047197551196596965 ) ;
#12239=ORIENTED_EDGE ( 'NONE', *, *, #13615, .F. ) ;
#12242=ORIENTED_EDGE ( 'NONE', *, *, #15318, .T. ) ;
#12243=VECTOR ( 'NONE', #789, 1000.000000000000000 ) ;
#12244=AXIS2_PLACEMENT_3D ( 'NONE', #8604, #6221, #1617 ) ;
#12245=FACE_OUTER_BOUND ( 'NONE', #12450, .T. ) ;
#12247=DIRECTION ( 'NONE',  ( 0.8660254037844383745, -0.5000000000000003331, 0.000000000000000000 ) ) ;
#12255=CARTESIAN_POINT ( 'NONE',  ( -86.77438362644001302, 65.17411849586700612, -86.49847958357699440 ) ) ;
#12256=EDGE_LOOP ( 'NONE', ( #11622, #14295 ) ) ;
#12260=ORIENTED_EDGE ( 'NONE', *, *, #14799, .F. ) ;
#12262=VERTEX_POINT ( 'NONE', #11757 ) ;
#12264=CYLINDRICAL_SURFACE ( 'NONE', #8525, 2.500000000000002220 ) ;
#12268=CARTESIAN_POINT ( 'NONE',  ( -38.27438362644000591, 111.1741184958670061, -79.49847958357700861 ) ) ;
#12270=CARTESIAN_POINT ( 'NONE',  ( -69.77438362644001302, 81.46011849586699327, -83.44847958357698303 ) ) ;
#12271=LINE ( 'NONE', #1643, #7293 ) ;
#12272=LINE ( 'NONE', #8778, #5342 ) ;
#12273=EDGE_CURVE ( 'NONE', #6920, #12145, #8242, .T. ) ;
#12274=DIRECTION ( 'NONE',  ( 0.000000000000000000, -1.000000000000000000, 0.000000000000000000 ) ) ;
#12276=ORIENTED_EDGE ( 'NONE', *, *, #6285, .T. ) ;
#12278=COLOUR_RGB ( '', 0.31764706, 0.68627451, 0.89019608) ;
#12279=EDGE_CURVE ( 'NONE', #3159, #4603, #14913, .T. ) ;
#12280=ORIENTED_EDGE ( 'NONE', *, *, #14260, .T. ) ;
#12282=ORIENTED_EDGE ( 'NONE', *, *, #6136, .T. ) ;
#12283=ORIENTED_EDGE ( 'NONE', *, *, #5293, .F. ) ;
#12284=VECTOR ( 'NONE', #3543, 1000.000000000000000 ) ;
#12289=DIRECTION ( 'NONE',  ( -1.000000000000000000, 0.000000000000000000, 0.000000000000000000 ) ) ;
#12290=AXIS2_PLACEMENT_3D ( 'NONE', #2888, #13744, #1645 ) ;
#12291=LINE ( 'NONE', #8160, #5261 ) ;
#12293=VECTOR ( 'NONE', #7945, 1000.000000000000000 ) ;
#12294=DIRECTION ( 'NONE',  ( 1.000000000000000000, 0.000000000000000000, 0.000000000000000000 ) ) ;
#12301=ADVANCED_FACE ( 'NONE', ( #10420 ), #8112, .F. ) ;
#12303=AXIS2_PLACEMENT_3D ( 'NONE', #3969, #1790, #7557 ) ;
#12305=AXIS2_PLACEMENT_3D ( 'NONE', #8002, #12662, #15125 ) ;
#12306=LINE ( 'NONE', #11062, #7822 ) ;
#12308=EDGE_LOOP ( 'NONE', ( #9115, #4736, #6251, #9131, #3804, #8451, #2497, #1982, #3143, #13372, #8665, #8402, #2771, #4772, #2207, #4299, #1994, #13504, #5359, #10975, #2410, #2331, #15155, #3394 ) ) ;
#12313=DIRECTION ( 'NONE',  ( 0.000000000000000000, -1.000000000000000000, 0.000000000000000000 ) ) ;
#12314=VECTOR ( 'NONE', #9490, 1000.000000000000000 ) ;
#12315=DIRECTION ( 'NONE',  ( 0.000000000000000000, 0.000000000000000000, -1.000000000000000000 ) ) ;
#12317=DIRECTION ( 'NONE',  ( -0.000000000000000000, -0.000000000000000000, -1.000000000000000000 ) ) ;
#12318=DIRECTION ( 'NONE',  ( 1.000000000000000000, 0.000000000000000000, 0.000000000000000000 ) ) ;
#12320=CARTESIAN_POINT ( 'NONE',  ( -86.77438362644001302, 59.67411849586700612, -15.85886927678779834 ) ) ;
#12321=DIRECTION ( 'NONE',  ( -1.000000000000000000, 0.000000000000000000, 0.000000000000000000 ) ) ;
#12323=VERTEX_POINT ( 'NONE', #2210 ) ;
#12326=ORIENTED_EDGE ( 'NONE', *, *, #11048, .F. ) ;
#12328=CIRCLE ( 'NONE', #5647, 2.700000000000001066 ) ;
#12330=CYLINDRICAL_SURFACE ( 'NONE', #6315, 16.00000000000000000 ) ;
#12335=AXIS2_PLACEMENT_3D ( 'NONE', #1585, #1887, #6642 ) ;
#12336=ORIENTED_EDGE ( 'NONE', *, *, #7354, .F. ) ;
#12338=ORIENTED_EDGE ( 'NONE', *, *, #14520, .F. ) ;
#12339=ORIENTED_EDGE ( 'NONE', *, *, #13598, .T. ) ;
#12341=ORIENTED_EDGE ( 'NONE', *, *, #10629, .T. ) ;
#12344=EDGE_CURVE ( 'NONE', #1952, #11360, #6029, .T. ) ;
#12350=ADVANCED_FACE ( 'NONE', ( #9113 ), #11525, .F. ) ;
#12352=CARTESIAN_POINT ( 'NONE',  ( -38.27438362644000591, 57.67411849586700612, -79.49847958357700861 ) ) ;
#12355=DIRECTION ( 'NONE',  ( 0.000000000000000000, 1.000000000000000000, 0.000000000000000000 ) ) ;
#12356=CARTESIAN_POINT ( 'NONE',  ( -68.09912303623625007, 89.17411849586702033, -44.18949531478481418 ) ) ;
#12358=ORIENTED_EDGE ( 'NONE', *, *, #5293, .T. ) ;
#12360=ORIENTED_EDGE ( 'NONE', *, *, #4140, .F. ) ;
#12362=VERTEX_POINT ( 'NONE', #3528 ) ;
#12365=CARTESIAN_POINT ( 'NONE',  ( -86.77438362643999881, 65.17411849586700612, -147.9984795835769944 ) ) ;
#12370=CARTESIAN_POINT ( 'NONE',  ( -86.77438362644001302, 59.67411849586700612, -15.85886927678779834 ) ) ;
#12372=AXIS2_PLACEMENT_3D ( 'NONE', #11075, #14618, #10910 ) ;
#12373=DIRECTION ( 'NONE',  ( -0.8660254037844387076, -0.4999999999999998890, 0.000000000000000000 ) ) ;
#12376=ORIENTED_EDGE ( 'NONE', *, *, #13434, .T. ) ;
#12378=EDGE_CURVE ( 'NONE', #5260, #13566, #15232, .T. ) ;
#12379=EDGE_CURVE ( 'NONE', #8742, #1201, #4858, .T. ) ;
#12384=EDGE_CURVE ( 'NONE', #7524, #4480, #11989, .T. ) ;
#12387=CARTESIAN_POINT ( 'NONE',  ( -37.27438362644100778, 101.6741184958670061, -79.59847958357700293 ) ) ;
#12389=CARTESIAN_POINT ( 'NONE',  ( -79.11147769456633227, 68.38713492810558137, -83.44847958357698303 ) ) ;
#12390=PLANE ( 'NONE',  #10887 ) ;
#12394=DIRECTION ( 'NONE',  ( -1.000000000000000000, 0.000000000000000000, 0.000000000000000000 ) ) ;
#12395=ADVANCED_FACE ( 'NONE', ( #10745 ), #7752, .F. ) ;
#12400=ORIENTED_EDGE ( 'NONE', *, *, #11303, .F. ) ;
#12402=CARTESIAN_POINT ( 'NONE',  ( -48.27438362644000591, 65.17411849586700612, -152.4984795835769944 ) ) ;
#12404=CARTESIAN_POINT ( 'NONE',  ( -84.07438362644101915, 99.17411849586700612, -145.4984795835769944 ) ) ;
#12405=CARTESIAN_POINT ( 'NONE',  ( -85.75338362644100698, 97.40569462133917966, -147.9984795835769944 ) ) ;
#12408=CARTESIAN_POINT ( 'NONE',  ( -52.77438362644000591, 65.17411849586700612, -86.49847958357699440 ) ) ;
#12411=EDGE_LOOP ( 'NONE', ( #540, #1932 ) ) ;
#12412=VERTEX_POINT ( 'NONE', #7263 ) ;
#12413=ORIENTED_EDGE ( 'NONE', *, *, #13781, .F. ) ;
#12414=ORIENTED_EDGE ( 'NONE', *, *, #10001, .T. ) ;
#12416=CARTESIAN_POINT ( 'NONE',  ( -75.01311196519617397, 67.29799558322736175, -81.84847958357697451 ) ) ;
#12418=DIRECTION ( 'NONE',  ( 0.000000000000000000, 1.000000000000000000, 0.000000000000000000 ) ) ;
#12420=CYLINDRICAL_SURFACE ( 'NONE', #3537, 2.750000000000002665 ) ;
#12424=CARTESIAN_POINT ( 'NONE',  ( -86.77438362644001302, 65.17411849586700612, -145.4984795835769660 ) ) ;
#12427=ORIENTED_EDGE ( 'NONE', *, *, #3757, .F. ) ;
#12429=VERTEX_POINT ( 'NONE', #9316 ) ;
#12430=AXIS2_PLACEMENT_3D ( 'NONE', #6940, #11658, #3210 ) ;
#12432=EDGE_LOOP ( 'NONE', ( #13488, #12130 ) ) ;
#12433=PRODUCT_DEFINITION_CONTEXT ( 'detailed design', #2768, 'design' ) ;
#12434=EDGE_CURVE ( 'NONE', #191, #2764, #10633, .T. ) ;
#12438=CARTESIAN_POINT ( 'NONE',  ( -69.77438362644100778, 82.17411849586700612, -67.49847958357700861 ) ) ;
#12440=FACE_OUTER_BOUND ( 'NONE', #1317, .T. ) ;
#12441=CARTESIAN_POINT ( 'NONE',  ( -37.27438362644000591, 65.17411849586700612, -152.4984795835769944 ) ) ;
#12442=DIRECTION ( 'NONE',  ( -1.287488025362404182E-15, -1.000000000000000000, 0.000000000000000000 ) ) ;
#12445=ORIENTED_EDGE ( 'NONE', *, *, #13327, .T. ) ;
#12446=DIRECTION ( 'NONE',  ( 0.000000000000000000, 0.000000000000000000, 1.000000000000000000 ) ) ;
#12450=EDGE_LOOP ( 'NONE', ( #12413, #9588, #10064 ) ) ;
#12451=EDGE_CURVE ( 'NONE', #12703, #14576, #13450, .T. ) ;
#12454=ORIENTED_EDGE ( 'NONE', *, *, #14608, .T. ) ;
#12458=CARTESIAN_POINT ( 'NONE',  ( -90.85838362644000199, 65.17411849586700612, -147.9984795835769944 ) ) ;
#12461=DIRECTION ( 'NONE',  ( 0.000000000000000000, 0.000000000000000000, -1.000000000000000000 ) ) ;
#12464=CARTESIAN_POINT ( 'NONE',  ( -59.02799568714584666, 59.67411849586700612, -79.59847958357700293 ) ) ;
#12467=DIRECTION ( 'NONE',  ( 1.000000000000000000, 0.000000000000000000, 0.000000000000000000 ) ) ;
#12468=VERTEX_POINT ( 'NONE', #5852 ) ;
#12470=EDGE_CURVE ( 'NONE', #5594, #11761, #11578, .T. ) ;
#12471=CARTESIAN_POINT ( 'NONE',  ( -101.2743836264399988, 114.1741184958670061, -67.49847958357700861 ) ) ;
#12475=CIRCLE ( 'NONE', #14445, 9.999999999999994671 ) ;
#12476=DIRECTION ( 'NONE',  ( -1.000000000000000000, 0.000000000000000000, 0.000000000000000000 ) ) ;
#12477=AXIS2_PLACEMENT_3D ( 'NONE', #318, #5068, #9780 ) ;
#12478=ADVANCED_FACE ( 'NONE', ( #4746 ), #15283, .F. ) ;
#12479=DIRECTION ( 'NONE',  ( 0.000000000000000000, 1.000000000000000000, 0.000000000000000000 ) ) ;
#12480=CARTESIAN_POINT ( 'NONE',  ( -69.77438362644001302, 82.17411849586700612, -80.14847958357698587 ) ) ;
#12481=AXIS2_PLACEMENT_3D ( 'NONE', #3738, #7321, #10153 ) ;
#12484=DIRECTION ( 'NONE',  ( 0.000000000000000000, 0.000000000000000000, -1.000000000000000000 ) ) ;
#12485=EDGE_CURVE ( 'NONE', #10868, #14784, #8082, .T. ) ;
#12486=CYLINDRICAL_SURFACE ( 'NONE', #602, 4.499999999999997335 ) ;
#12487=ORIENTED_EDGE ( 'NONE', *, *, #421, .T. ) ;
#12489=CIRCLE ( 'NONE', #4804, 8.000000000000007105 ) ;
#12490=VECTOR ( 'NONE', #9658, 1000.000000000000000 ) ;
#12492=ADVANCED_FACE ( 'NONE', ( #4593 ), #5933, .T. ) ;
#12497=ORIENTED_EDGE ( 'NONE', *, *, #15318, .F. ) ;
#12501=FACE_OUTER_BOUND ( 'NONE', #1258, .T. ) ;
#12503=AXIS2_PLACEMENT_3D ( 'NONE', #8433, #6212, #7368 ) ;
#12504=VECTOR ( 'NONE', #5209, 1000.000000000000000 ) ;
#12509=CARTESIAN_POINT ( 'NONE',  ( -50.73238362643999722, 66.35306774555222376, -147.9984795835769944 ) ) ;
#12515=ORIENTED_EDGE ( 'NONE', *, *, #7169, .T. ) ;
#12517=VECTOR ( 'NONE', #12315, 1000.000000000000000 ) ;
#12518=CARTESIAN_POINT ( 'NONE',  ( -54.81638362644100226, 97.99516924618178848, -147.9984795835769944 ) ) ;
#12521=CARTESIAN_POINT ( 'NONE',  ( -42.77438362644000591, 65.17411849586700612, -152.4984795835769944 ) ) ;
#12522=LINE ( 'NONE', #14831, #6859 ) ;
#12523=DIRECTION ( 'NONE',  ( 1.000000000000000000, 0.000000000000000000, 0.000000000000000000 ) ) ;
#12525=AXIS2_PLACEMENT_3D ( 'NONE', #12149, #13626, #7507 ) ;
#12528=VECTOR ( 'NONE', #3034, 1000.000000000000114 ) ;
#12529=FACE_OUTER_BOUND ( 'NONE', #2158, .T. ) ;
#12533=ORIENTED_EDGE ( 'NONE', *, *, #11407, .F. ) ;
#12535=AXIS2_PLACEMENT_3D ( 'NONE', #7276, #12002, #11070 ) ;
#12536=AXIS2_PLACEMENT_3D ( 'NONE', #3878, #13496, #1543 ) ;
#12537=LINE ( 'NONE', #13624, #8951 ) ;
#12539=CARTESIAN_POINT ( 'NONE',  ( -69.77438362644001302, 82.17411849586700612, -138.4984795835769944 ) ) ;
#12542=DIRECTION ( 'NONE',  ( 0.000000000000000000, 0.000000000000000000, 1.000000000000000000 ) ) ;
#12548=CIRCLE ( 'NONE', #3119, 4.500000000000003553 ) ;
#12550=VERTEX_POINT ( 'NONE', #14127 ) ;
#12553=ORIENTED_EDGE ( 'NONE', *, *, #149, .T. ) ;
#12555=DIRECTION ( 'NONE',  ( -1.000000000000000000, 0.000000000000000000, 0.000000000000000000 ) ) ;
#12556=EDGE_CURVE ( 'NONE', #4383, #2303, #1794, .T. ) ;
#12557=AXIS2_PLACEMENT_3D ( 'NONE', #4444, #3050, #13833 ) ;
#12558=FACE_OUTER_BOUND ( 'NONE', #6144, .T. ) ;
#12559=FACE_OUTER_BOUND ( 'NONE', #13548, .T. ) ;
#12563=CYLINDRICAL_SURFACE ( 'NONE', #8968, 4.499999999999997335 ) ;
#12564=ORIENTED_EDGE ( 'NONE', *, *, #3001, .T. ) ;
#12565=CARTESIAN_POINT ( 'NONE',  ( -80.52077156573417938, 103.6741184958669777, -73.34256232478206528 ) ) ;
#12566=AXIS2_PLACEMENT_3D ( 'NONE', #9569, #11058, #428 ) ;
#12567=ORIENTED_EDGE ( 'NONE', *, *, #12766, .F. ) ;
#12569=ORIENTED_EDGE ( 'NONE', *, *, #2314, .T. ) ;
#12571=EDGE_CURVE ( 'NONE', #7989, #4297, #9958, .T. ) ;
#12576=ADVANCED_FACE ( 'NONE', ( #2799 ), #8541, .F. ) ;
#12577=CARTESIAN_POINT ( 'NONE',  ( -73.13733409597239188, 66.60412428008086749, -83.44847958357698303 ) ) ;
#12581=ADVANCED_FACE ( 'NONE', ( #3813 ), #3277, .T. ) ;
#12584=DIRECTION ( 'NONE',  ( 0.000000000000000000, 0.000000000000000000, -1.000000000000000000 ) ) ;
#12592=ORIENTED_EDGE ( 'NONE', *, *, #7647, .F. ) ;
#12593=VECTOR ( 'NONE', #643, 1000.000000000000000 ) ;
#12594=CARTESIAN_POINT ( 'NONE',  ( -73.13733409597239188, 66.60412428008086749, -83.44847958357698303 ) ) ;
#12596=DIRECTION ( 'NONE',  ( 0.000000000000000000, 0.000000000000000000, 1.000000000000000000 ) ) ;
#12597=CARTESIAN_POINT ( 'NONE',  ( -69.77438362644001302, 92.37411849586700896, -80.14847958357698587 ) ) ;
#12599=CARTESIAN_POINT ( 'NONE',  ( -67.09329877327485292, 74.51466092244987749, -58.65793715699411592 ) ) ;
#12604=CARTESIAN_POINT ( 'NONE',  ( -37.27438362642642034, 65.17411849586919459, -79.59847958357700293 ) ) ;
#12605=ORIENTED_EDGE ( 'NONE', *, *, #14984, .F. ) ;
#12606=DIRECTION ( 'NONE',  ( 0.000000000000000000, 0.000000000000000000, -1.000000000000000000 ) ) ;
#12609=EDGE_LOOP ( 'NONE', ( #2944, #225, #5781, #6633 ) ) ;
#12612=PLANE ( 'NONE',  #5247 ) ;
#12622=ORIENTED_EDGE ( 'NONE', *, *, #1230, .T. ) ;
#12624=DIRECTION ( 'NONE',  ( 0.000000000000000000, -1.000000000000000000, 0.000000000000000000 ) ) ;
#12629=EDGE_LOOP ( 'NONE', ( #3555, #5591 ) ) ;
#12630=FACE_OUTER_BOUND ( 'NONE', #12609, .T. ) ;
#12631=EDGE_CURVE ( 'NONE', #14726, #1497, #9621, .T. ) ;
#12637=ORIENTED_EDGE ( 'NONE', *, *, #6851, .F. ) ;
#12643=DIRECTION ( 'NONE',  ( 0.000000000000000000, 0.000000000000000000, 1.000000000000000000 ) ) ;
#12644=EDGE_CURVE ( 'NONE', #4454, #3610, #8618, .T. ) ;
#12647=LINE ( 'NONE', #12509, #379 ) ;
#12650=ORIENTED_EDGE ( 'NONE', *, *, #4124, .T. ) ;
#12651=CYLINDRICAL_SURFACE ( 'NONE', #1566, 17.00000000000000000 ) ;
#12652=ADVANCED_FACE ( 'NONE', ( #12043 ), #14354, .T. ) ;
#12653=ORIENTED_EDGE ( 'NONE', *, *, #862, .F. ) ;
#12655=ORIENTED_EDGE ( 'NONE', *, *, #9297, .T. ) ;
#12660=FACE_OUTER_BOUND ( 'NONE', #8032, .T. ) ;
#12662=DIRECTION ( 'NONE',  ( 0.000000000000000000, 0.000000000000000000, -1.000000000000000000 ) ) ;
#12664=CARTESIAN_POINT ( 'NONE',  ( -52.77438362643999881, 65.17411849586700612, -147.9984795835769944 ) ) ;
#12665=CARTESIAN_POINT ( 'NONE',  ( -51.75338362644099277, 97.40569462133917966, -147.9984795835769944 ) ) ;
#12666=CARTESIAN_POINT ( 'NONE',  ( -52.77438362643999881, 67.53201699523744139, -147.9984795835769944 ) ) ;
#12667=VECTOR ( 'NONE', #5195, 1000.000000000000000 ) ;
#12669=FACE_OUTER_BOUND ( 'NONE', #5282, .T. ) ;
#12672=CARTESIAN_POINT ( 'NONE',  ( -88.81638362644100937, 99.17411849586700612, -147.9984795835769944 ) ) ;
#12673=ORIENTED_EDGE ( 'NONE', *, *, #14151, .T. ) ;
#12674=VECTOR ( 'NONE', #14994, 1000.000000000000000 ) ;
#12676=ORIENTED_EDGE ( 'NONE', *, *, #7793, .F. ) ;
#12678=AXIS2_PLACEMENT_3D ( 'NONE', #3343, #5695, #11494 ) ;
#12681=CARTESIAN_POINT ( 'NONE',  ( -65.90140028023257912, 89.17411849586700612, -57.99847958357699440 ) ) ;
#12684=DIRECTION ( 'NONE',  ( -1.000000000000000000, 1.287488025362404182E-15, 0.000000000000000000 ) ) ;
#12687=AXIS2_PLACEMENT_3D ( 'NONE', #13287, #166, #13135 ) ;
#12689=ORIENTED_EDGE ( 'NONE', *, *, #6151, .F. ) ;
#12692=EDGE_LOOP ( 'NONE', ( #3592, #6079, #11858, #6901, #14255 ) ) ;
#12695=DIRECTION ( 'NONE',  ( 0.000000000000000000, 1.000000000000000000, 0.000000000000000000 ) ) ;
#12699=FACE_OUTER_BOUND ( 'NONE', #8704, .T. ) ;
#12700=EDGE_CURVE ( 'NONE', #13871, #506, #1941, .T. ) ;
#12701=PLANE ( 'NONE',  #9196 ) ;
#12703=VERTEX_POINT ( 'NONE', #5374 ) ;
#12704=CARTESIAN_POINT ( 'NONE',  ( -59.02799568714584666, 110.1741184958670061, -79.59847958357700293 ) ) ;
#12705=ORIENTED_EDGE ( 'NONE', *, *, #5717, .T. ) ;
#12706=ORIENTED_EDGE ( 'NONE', *, *, #45, .F. ) ;
#12708=ORIENTED_EDGE ( 'NONE', *, *, #2499, .F. ) ;
#12709=ORIENTED_EDGE ( 'NONE', *, *, #13695, .F. ) ;
#12710=VECTOR ( 'NONE', #14846, 1000.000000000000000 ) ;
#12711=AXIS2_PLACEMENT_3D ( 'NONE', #2096, #855, #11719 ) ;
#12715=AXIS2_PLACEMENT_3D ( 'NONE', #10955, #7403, #6468 ) ;
#12719=DIRECTION ( 'NONE',  ( 0.000000000000000000, 0.000000000000000000, 1.000000000000000000 ) ) ;
#12721=CARTESIAN_POINT ( 'NONE',  ( -84.73238362643999722, 66.35306774555222376, -147.9984795835769944 ) ) ;
#12723=AXIS2_PLACEMENT_3D ( 'NONE', #13312, #7416, #14375 ) ;
#12725=EDGE_CURVE ( 'NONE', #5515, #2624, #3109, .T. ) ;
#12726=CIRCLE ( 'NONE', #5556, 2.750000000000002665 ) ;
#12731=VECTOR ( 'NONE', #2280, 1000.000000000000000 ) ;
#12733=VERTEX_POINT ( 'NONE', #14810 ) ;
#12734=CYLINDRICAL_SURFACE ( 'NONE', #7501, 2.750000000000002665 ) ;
#12735=CLOSED_SHELL ( 'NONE', ( #6795, #10056, #4219, #10554, #15284, #4459, #9208, #10294, #7654, #33, #12301, #11696, #898, #14815, #10757, #1491, #7039, #12816, #1199, #8462, #14524, #15027, #14080, #2687, #6889, #9414, #15297, #11990, #3836, #1084, #6984, #684, #809, #9635, #11516, #103, #4590, #9049, #3855, #6050, #11823, #9803, #9813, #5101, #14920, #108, #10088, #1186, #14542, #9867, #6759, #2808, #9233, #7277, #6668, #212, #5188, #12914, #7841, #12581, #7369, #963, #8446, #6891, #3704, #2958, #5934, #1066, #3464, #2212, #6148, #4873, #5364, #8390, #9882, #5231, #5007, #11118, #8395, #4310, #5390, #785, #565, #4039, #9063, #10763, #9433, #7471, #1578, #3621, #13620, #3927, #12022, #7846, #3934, #8669, #7525, #7694, #12576, #3057, #6990, #2984, #4915, #6948, #4561, #9983, #8124, #5847, #12203, #951, #9135, #4407, #501, #14464, #6605, #3161, #5543, #3075, #13877, #7799, #3671, #2319, #9145, #10935, #8819, #7235, #7732, #11443, #13399, #1547, #11705, #9106, #10462, #2434, #13543, #9111, #4989, #10880, #2243, #11711, #9617, #15262, #5157, #9519, #14727, #11147, #1367, #2868, #233, #9254, #10772, #9507, #6340, #1391, #7908, #4696, #12395, #6766, #5522, #7383, #3330, #11130, #12350, #15121, #313, #8408, #1383, #3364, #7573, #9794, #5969, #9230, #7324, #11218, #3043, #90, #11196, #13516, #3179, #11627, #14172, #11534, #12178, #1181, #1737, #5343, #14745, #13146, #11054, #11211, #2217, #11882, #7061, #9341, #1957, #11762, #7077, #9723, #6392, #7150, #3150, #4231, #7177, #4577, #2218, #1840, #13395, #12478, #3471, #9528, #5818 ) ) ;
#12737=DIRECTION ( 'NONE',  ( -1.287488025362404182E-15, -1.000000000000000000, 0.000000000000000000 ) ) ;
#12741=CARTESIAN_POINT ( 'NONE',  ( -53.77438362644000591, 82.17411849586700612, -183.7533135795160320 ) ) ;
#12742=CARTESIAN_POINT ( 'NONE',  ( -63.06767964790545022, 68.65632084656354550, -83.44847958357698303 ) ) ;
#12743=LINE ( 'NONE', #7009, #2067 ) ;
#12744=CARTESIAN_POINT ( 'NONE',  ( -86.77438362644100778, 99.17411849586700612, -147.9984795835769944 ) ) ;
#12746=ORIENTED_EDGE ( 'NONE', *, *, #14933, .F. ) ;
#12747=FACE_OUTER_BOUND ( 'NONE', #6750, .T. ) ;
#12748=VECTOR ( 'NONE', #4799, 1000.000000000000000 ) ;
#12751=EDGE_LOOP ( 'NONE', ( #12283, #3547, #1872, #4160 ) ) ;
#12752=DIRECTION ( 'NONE',  ( -1.000000000000000000, 0.000000000000000000, 0.000000000000000000 ) ) ;
#12759=DIRECTION ( 'NONE',  ( 1.000000000000000000, 0.000000000000000000, 0.000000000000000000 ) ) ;
#12764=EDGE_CURVE ( 'NONE', #9228, #12323, #1864, .T. ) ;
#12766=EDGE_CURVE ( 'NONE', #4260, #5306, #2050, .T. ) ;
#12767=DIRECTION ( 'NONE',  ( 0.000000000000000000, 0.000000000000000000, -1.000000000000000000 ) ) ;
#12770=AXIS2_PLACEMENT_3D ( 'NONE', #1365, #8058, #1285 ) ;
#12774=AXIS2_PLACEMENT_3D ( 'NONE', #4406, #12484, #10131 ) ;
#12776=DIRECTION ( 'NONE',  ( 0.8660254037844387076, 0.4999999999999998890, 0.000000000000000000 ) ) ;
#12779=DIRECTION ( 'NONE',  ( 1.000000000000000000, 1.541976423090494894E-16, 0.000000000000000000 ) ) ;
#12783=AXIS2_PLACEMENT_3D ( 'NONE', #12231, #3700, #13172 ) ;
#12784=CARTESIAN_POINT ( 'NONE',  ( -50.73238362644099197, 99.17411849586700612, -147.9984795835769944 ) ) ;
#12785=ORIENTED_EDGE ( 'NONE', *, *, #12631, .T. ) ;
#12787=ORIENTED_EDGE ( 'NONE', *, *, #5065, .T. ) ;
#12791=VERTEX_POINT ( 'NONE', #11329 ) ;
#12792=ORIENTED_EDGE ( 'NONE', *, *, #3653, .F. ) ;
#12793=AXIS2_PLACEMENT_3D ( 'NONE', #9926, #7398, #5060 ) ;
#12795=AXIS2_PLACEMENT_3D ( 'NONE', #4830, #15281, #10474 ) ;
#12801=CARTESIAN_POINT ( 'NONE',  ( -52.77438362644000591, 65.17411849586700612, -152.4984795835769944 ) ) ;
#12803=DIRECTION ( 'NONE',  ( -1.000000000000000000, 0.000000000000000000, 0.000000000000000000 ) ) ;
#12804=DIRECTION ( 'NONE',  ( -1.000000000000000000, 0.000000000000000000, 0.000000000000000000 ) ) ;
#12806=AXIS2_PLACEMENT_3D ( 'NONE', #8995, #12719, #10309 ) ;
#12807=EDGE_LOOP ( 'NONE', ( #11893, #1090 ) ) ;
#12808=CARTESIAN_POINT ( 'NONE',  ( 0.000000000000000000, 0.000000000000000000, -79.59847958357700293 ) ) ;
#12810=VERTEX_POINT ( 'NONE', #11398 ) ;
#12811=ORIENTED_EDGE ( 'NONE', *, *, #3832, .F. ) ;
#12814=VECTOR ( 'NONE', #6248, 1000.000000000000000 ) ;
#12816=ADVANCED_FACE ( 'NONE', ( #10224 ), #12420, .F. ) ;
#12817=AXIS2_PLACEMENT_3D ( 'NONE', #902, #15013, #4402 ) ;
#12821=CARTESIAN_POINT ( 'NONE',  ( -51.75338362643999801, 66.94254237039483257, -147.9984795835769944 ) ) ;
#12822=CARTESIAN_POINT ( 'NONE',  ( -65.90140028023417074, 75.17411849586613926, -57.99847958357779021 ) ) ;
#12823=CARTESIAN_POINT ( 'NONE',  ( -55.52438362644000591, 99.17411849586700612, -145.4984795835769660 ) ) ;
#12824=CARTESIAN_POINT ( 'NONE',  ( -73.13733409597239188, 66.60412428008086749, -83.44847958357698303 ) ) ;
#12825=DIRECTION ( 'NONE',  ( 0.000000000000000000, -1.000000000000000000, 0.000000000000000000 ) ) ;
#12826=VERTEX_POINT ( 'NONE', #6391 ) ;
#12828=ORIENTED_EDGE ( 'NONE', *, *, #1247, .F. ) ;
#12830=EDGE_LOOP ( 'NONE', ( #756, #10410, #8034, #6957 ) ) ;
#12831=CYLINDRICAL_SURFACE ( 'NONE', #3258, 1.250000000000001110 ) ;
#12834=EDGE_CURVE ( 'NONE', #11758, #4603, #5034, .T. ) ;
#12839=LINE ( 'NONE', #13995, #12674 ) ;
#12840=CARTESIAN_POINT ( 'NONE',  ( -69.77438362644001302, 82.17411849586700612, -67.69567958357700377 ) ) ;
#12841=CIRCLE ( 'NONE', #11597, 16.06499999999999773 ) ;
#12842=CARTESIAN_POINT ( 'NONE',  ( -52.77438362644000591, 65.17411849586700612, -86.49847958357699440 ) ) ;
#12843=EDGE_CURVE ( 'NONE', #5278, #2560, #15184, .T. ) ;
#12844=CARTESIAN_POINT ( 'NONE',  ( -104.2743836264399988, 60.67411849586700612, -79.49847958357700861 ) ) ;
#12845=ORIENTED_EDGE ( 'NONE', *, *, #14163, .T. ) ;
#12847=PLANE ( 'NONE',  #9330 ) ;
#12850=ORIENTED_EDGE ( 'NONE', *, *, #3312, .T. ) ;
#12852=EDGE_LOOP ( 'NONE', ( #14324, #1270 ) ) ;
#12858=DIRECTION ( 'NONE',  ( -1.287488025362404182E-15, -1.000000000000000000, 0.000000000000000000 ) ) ;
#12859=CIRCLE ( 'NONE', #4694, 4.499999999999997335 ) ;
#12869=VERTEX_POINT ( 'NONE', #9215 ) ;
#12871=VERTEX_POINT ( 'NONE', #11560 ) ;
#12872=VERTEX_POINT ( 'NONE', #5685 ) ;
#12876=DIRECTION ( 'NONE',  ( -1.000000000000000000, 0.000000000000000000, 0.000000000000000000 ) ) ;
#12877=LINE ( 'NONE', #8439, #8097 ) ;
#12878=CARTESIAN_POINT ( 'NONE',  ( -88.81638362644100937, 100.3530677455522238, -147.9984795835769944 ) ) ;
#12879=CARTESIAN_POINT ( 'NONE',  ( -56.85838362644099675, 99.17411849586700612, -147.9984795835769944 ) ) ;
#12880=CARTESIAN_POINT ( 'NONE',  ( -69.77438362644001302, 90.17411849586700612, -29.37106258560738681 ) ) ;
#12881=FACE_OUTER_BOUND ( 'NONE', #3724, .T. ) ;
#12885=DIRECTION ( 'NONE',  ( 0.000000000000000000, 0.000000000000000000, -1.000000000000000000 ) ) ;
#12887=DIRECTION ( 'NONE',  ( -1.000000000000000000, 0.000000000000000000, 0.000000000000000000 ) ) ;
#12888=ORIENTED_EDGE ( 'NONE', *, *, #14316, .F. ) ;
#12889=EDGE_LOOP ( 'NONE', ( #1703, #6064, #835, #1631 ) ) ;
#12890=FACE_OUTER_BOUND ( 'NONE', #1257, .T. ) ;
#12891=CARTESIAN_POINT ( 'NONE',  ( -91.02438362643999881, 65.17411849586700612, -182.2484795835770228 ) ) ;
#12893=DIRECTION ( 'NONE',  ( 0.000000000000000000, 0.000000000000000000, -1.000000000000000000 ) ) ;
#12895=CARTESIAN_POINT ( 'NONE',  ( -70.45539183192644828, 89.17411849586699191, -44.02377680093030676 ) ) ;
#12897=CARTESIAN_POINT ( 'NONE',  ( -63.28565528768381654, 67.29799558322736175, -83.44847958357698303 ) ) ;
#12898=ORIENTED_EDGE ( 'NONE', *, *, #12485, .T. ) ;
#12899=CARTESIAN_POINT ( 'NONE',  ( -53.27438362644000591, 82.17411849586700612, -150.4984795835769944 ) ) ;
#12900=EDGE_CURVE ( 'NONE', #14841, #14332, #802, .T. ) ;
#12901=ORIENTED_EDGE ( 'NONE', *, *, #2989, .T. ) ;
#12908=AXIS2_PLACEMENT_3D ( 'NONE', #4080, #6354, #14844 ) ;
#12910=DIRECTION ( 'NONE',  ( 0.000000000000000000, 0.000000000000000000, 1.000000000000000000 ) ) ;
#12914=ADVANCED_FACE ( 'NONE', ( #13880 ), #6983, .T. ) ;
#12916=DIRECTION ( 'NONE',  ( -1.000000000000000000, 0.000000000000000000, 0.000000000000000000 ) ) ;
#12917=VERTEX_POINT ( 'NONE', #924 ) ;
#12923=ORIENTED_EDGE ( 'NONE', *, *, #8677, .F. ) ;
#12924=AXIS2_PLACEMENT_3D ( 'NONE', #11746, #5870, #1113 ) ;
#12929=DIRECTION ( 'NONE',  ( 0.000000000000000000, 0.000000000000000000, 1.000000000000000000 ) ) ;
#12930=CIRCLE ( 'NONE', #6265, 2.750000000000002665 ) ;
#12932=EDGE_CURVE ( 'NONE', #2624, #6663, #6531, .T. ) ;
#12933=LINE ( 'NONE', #2295, #13001 ) ;
#12934=AXIS2_PLACEMENT_3D ( 'NONE', #4743, #1320, #4672 ) ;
#12942=DIRECTION ( 'NONE',  ( -1.000000000000000000, 0.000000000000000000, 0.000000000000000000 ) ) ;
#12947=ORIENTED_EDGE ( 'NONE', *, *, #12172, .F. ) ;
#12949=ORIENTED_EDGE ( 'NONE', *, *, #3736, .F. ) ;
#12952=EDGE_CURVE ( 'NONE', #10071, #11036, #8493, .T. ) ;
#12954=DIRECTION ( 'NONE',  ( -1.000000000000000000, 0.000000000000000000, 0.000000000000000000 ) ) ;
#12955=DIRECTION ( 'NONE',  ( 0.000000000000000000, 0.000000000000000000, 1.000000000000000000 ) ) ;
#12957=EDGE_CURVE ( 'NONE', #11895, #13217, #14111, .T. ) ;
#12958=FACE_OUTER_BOUND ( 'NONE', #7440, .T. ) ;
#12960=CARTESIAN_POINT ( 'NONE',  ( -62.27438362644000591, 75.17411849586699191, -57.99847958357699440 ) ) ;
#12961=DIRECTION ( 'NONE',  ( 0.000000000000000000, 0.000000000000000000, 1.000000000000000000 ) ) ;
#12962=DIRECTION ( 'NONE',  ( -1.000000000000000000, 0.000000000000000000, 0.000000000000000000 ) ) ;
#12964=EDGE_CURVE ( 'NONE', #3958, #3363, #5988, .T. ) ;
#12965=FACE_OUTER_BOUND ( 'NONE', #7176, .T. ) ;
#12966=ADVANCED_FACE ( 'NONE', ( #12225 ), #3856, .F. ) ;
#12968=DIRECTION ( 'NONE',  ( 0.000000000000000000, 0.000000000000000000, -1.000000000000000000 ) ) ;
#12970=VERTEX_POINT ( 'NONE', #2755 ) ;
#12972=ORIENTED_EDGE ( 'NONE', *, *, #4317, .F. ) ;
#12973=AXIS2_PLACEMENT_3D ( 'NONE', #86, #4838, #7241 ) ;
#12974=( NAMED_UNIT ( * ) PLANE_ANGLE_UNIT ( ) SI_UNIT ( $, .RADIAN. ) );
#12980=VECTOR ( 'NONE', #4719, 1000.000000000000000 ) ;
#12985=LINE ( 'NONE', #11653, #13463 ) ;
#12986=AXIS2_PLACEMENT_3D ( 'NONE', #14513, #8468, #5219 ) ;
#12988=CARTESIAN_POINT ( 'NONE',  ( -69.77438362644100778, 82.17411849586700612, -79.49847958357700861 ) ) ;
#12989=EDGE_LOOP ( 'NONE', ( #9345, #3314, #2073, #10940 ) ) ;
#12990=ORIENTED_EDGE ( 'NONE', *, *, #10949, .T. ) ;
#12993=CONICAL_SURFACE ( 'NONE', #14710, 8.349999999999996092, 0.7853981633974476129 ) ;
#12998=DIRECTION ( 'NONE',  ( 0.000000000000000000, 0.000000000000000000, 1.000000000000000000 ) ) ;
#12999=CARTESIAN_POINT ( 'NONE',  ( -69.77438362644001302, 82.17411849586700612, -152.4984795835769944 ) ) ;
#13000=VECTOR ( 'NONE', #11937, 1000.000000000000000 ) ;
#13001=VECTOR ( 'NONE', #7046, 1000.000000000000000 ) ;
#13002=DIRECTION ( 'NONE',  ( 0.000000000000000000, -0.000000000000000000, 1.000000000000000000 ) ) ;
#13003=ORIENTED_EDGE ( 'NONE', *, *, #886, .T. ) ;
#13007=DIRECTION ( 'NONE',  ( 1.049727191138615614E-16, 0.8571673007021106683, 0.5150380749100569311 ) ) ;
#13010=EDGE_CURVE ( 'NONE', #6866, #4383, #8581, .T. ) ;
#13013=DIRECTION ( 'NONE',  ( 0.000000000000000000, 0.000000000000000000, -1.000000000000000000 ) ) ;
#13016=DIRECTION ( 'NONE',  ( 0.000000000000000000, 0.000000000000000000, -1.000000000000000000 ) ) ;
#13019=LINE ( 'NONE', #10841, #3044 ) ;
#13021=DIRECTION ( 'NONE',  ( 1.000000000000000000, 0.000000000000000000, 0.000000000000000000 ) ) ;
#13022=AXIS2_PLACEMENT_3D ( 'NONE', #5600, #1861, #12418 ) ;
#13023=EDGE_LOOP ( 'NONE', ( #10341, #12828, #15332, #15197, #991 ) ) ;
#13027=CARTESIAN_POINT ( 'NONE',  ( -52.77438362644000591, 99.17411849586700612, -145.4984795835769660 ) ) ;
#13032=ORIENTED_EDGE ( 'NONE', *, *, #7928, .F. ) ;
#13036=EDGE_CURVE ( 'NONE', #14943, #8436, #10720, .T. ) ;
#13037=AXIS2_PLACEMENT_3D ( 'NONE', #11982, #9484, #9640 ) ;
#13041=LINE ( 'NONE', #4495, #7617 ) ;
#13048=EDGE_CURVE ( 'NONE', #4095, #11284, #11459, .T. ) ;
#13051=EDGE_LOOP ( 'NONE', ( #3321, #7366, #15136, #2350 ) ) ;
#13054=ORIENTED_EDGE ( 'NONE', *, *, #11903, .F. ) ;
#13055=AXIS2_PLACEMENT_3D ( 'NONE', #9638, #10967, #13225 ) ;
#13056=EDGE_CURVE ( 'NONE', #13261, #8742, #14546, .T. ) ;
#13057=CARTESIAN_POINT ( 'NONE',  ( -37.27438362644000591, 99.17411849586700612, -15.85886927678779834 ) ) ;
#13062=CARTESIAN_POINT ( 'NONE',  ( -42.77438362644000591, 110.1741184958670061, -15.85886927678779834 ) ) ;
#13063=VECTOR ( 'NONE', #11282, 1000.000000000000114 ) ;
#13068=CARTESIAN_POINT ( 'NONE',  ( -71.12250604111588359, 89.17411849586699191, -44.11946707556861469 ) ) ;
#13069=LINE ( 'NONE', #1251, #2103 ) ;
#13071=CARTESIAN_POINT ( 'NONE',  ( -72.92551479769302603, 97.86074886511958937, -93.49847958357699440 ) ) ;
#13073=ORIENTED_EDGE ( 'NONE', *, *, #10178, .F. ) ;
#13074=DIRECTION ( 'NONE',  ( 0.000000000000000000, 0.000000000000000000, -1.000000000000000000 ) ) ;
#13077=ORIENTED_EDGE ( 'NONE', *, *, #9146, .F. ) ;
#13078=DIRECTION ( 'NONE',  ( -1.000000000000000000, 0.000000000000000000, 0.000000000000000000 ) ) ;
#13079=AXIS2_PLACEMENT_3D ( 'NONE', #9097, #14838, #6485 ) ;
#13082=VERTEX_POINT ( 'NONE', #11210 ) ;
#13085=CARTESIAN_POINT ( 'NONE',  ( -65.90140028023417074, 75.17411849586613926, -57.99847958357779021 ) ) ;
#13088=CARTESIAN_POINT ( 'NONE',  ( -86.77438362644001302, 82.17411849586700612, -79.59847958357700293 ) ) ;
#13091=CARTESIAN_POINT ( 'NONE',  ( -35.27438362644000591, 72.17411849586700612, -67.49847958357700861 ) ) ;
#13096=EDGE_LOOP ( 'NONE', ( #8454, #12845, #4975, #817 ) ) ;
#13103=FACE_OUTER_BOUND ( 'NONE', #983, .T. ) ;
#13104=CYLINDRICAL_SURFACE ( 'NONE', #6353, 4.499999999999997335 ) ;
#13106=ORIENTED_EDGE ( 'NONE', *, *, #5470, .T. ) ;
#13109=EDGE_CURVE ( 'NONE', #858, #10812, #1801, .T. ) ;
#13110=ORIENTED_EDGE ( 'NONE', *, *, #698, .T. ) ;
#13111=DIRECTION ( 'NONE',  ( 0.000000000000000000, 0.000000000000000000, 1.000000000000000000 ) ) ;
#13113=ORIENTED_EDGE ( 'NONE', *, *, #7828, .F. ) ;
#13114=ORIENTED_EDGE ( 'NONE', *, *, #2314, .F. ) ;
#13115=ORIENTED_EDGE ( 'NONE', *, *, #9402, .T. ) ;
#13117=DIRECTION ( 'NONE',  ( -1.000000000000000000, 0.000000000000000000, 0.000000000000000000 ) ) ;
#13118=CARTESIAN_POINT ( 'NONE',  ( -51.75338362643999801, 63.40569462133917256, -147.9984795835769944 ) ) ;
#13120=CARTESIAN_POINT ( 'NONE',  ( -50.73238362643999722, 63.99516924618178848, -150.4984795835770228 ) ) ;
#13121=FACE_BOUND ( 'NONE', #8532, .T. ) ;
#13122=EDGE_CURVE ( 'NONE', #6604, #6326, #5795, .T. ) ;
#13124=DIRECTION ( 'NONE',  ( -1.000000000000000000, 0.000000000000000000, 0.000000000000000000 ) ) ;
#13126=DIRECTION ( 'NONE',  ( -0.000000000000000000, -0.000000000000000000, 1.000000000000000000 ) ) ;
#13127=ORIENTED_EDGE ( 'NONE', *, *, #12344, .F. ) ;
#13135=DIRECTION ( 'NONE',  ( 0.000000000000000000, 1.000000000000000000, 0.000000000000000000 ) ) ;
#13138=CARTESIAN_POINT ( 'NONE',  ( -72.41519636940742544, 89.17411849586704875, -44.45439862457369884 ) ) ;
#13140=EDGE_CURVE ( 'NONE', #7562, #11318, #7278, .T. ) ;
#13143=ORIENTED_EDGE ( 'NONE', *, *, #4941, .F. ) ;
#13145=ORIENTED_EDGE ( 'NONE', *, *, #11226, .T. ) ;
#13146=ADVANCED_FACE ( 'NONE', ( #6275 ), #5486, .F. ) ;
#13147=EDGE_LOOP ( 'NONE', ( #15152, #1462, #499, #4190, #4949 ) ) ;
#13148=VERTEX_POINT ( 'NONE', #2995 ) ;
#13150=ORIENTED_EDGE ( 'NONE', *, *, #4762, .T. ) ;
#13153=CARTESIAN_POINT ( 'NONE',  ( -104.2743836264399988, 60.67411849586700612, -67.49847958357700861 ) ) ;
#13155=DIRECTION ( 'NONE',  ( 0.000000000000000000, 0.000000000000000000, -1.000000000000000000 ) ) ;
#13156=EDGE_CURVE ( 'NONE', #4417, #4564, #13773, .T. ) ;
#13162=SHAPE_DEFINITION_REPRESENTATION ( #503, #5010 ) ;
#13167=DIRECTION ( 'NONE',  ( 1.000000000000000000, 0.000000000000000000, 0.000000000000000000 ) ) ;
#13168=LINE ( 'NONE', #4944, #1601 ) ;
#13169=AXIS2_PLACEMENT_3D ( 'NONE', #1445, #6201, #10665 ) ;
#13172=DIRECTION ( 'NONE',  ( -1.000000000000000000, 0.000000000000000000, 0.000000000000000000 ) ) ;
#13174=CIRCLE ( 'NONE', #12678, 2.042000000000002036 ) ;
#13176=FACE_OUTER_BOUND ( 'NONE', #11283, .T. ) ;
#13177=ORIENTED_EDGE ( 'NONE', *, *, #8878, .F. ) ;
#13178=CYLINDRICAL_SURFACE ( 'NONE', #12503, 1.250000000000001110 ) ;
#13180=ORIENTED_EDGE ( 'NONE', *, *, #14622, .F. ) ;
#13181=ORIENTED_EDGE ( 'NONE', *, *, #5767, .F. ) ;
#13182=ORIENTED_EDGE ( 'NONE', *, *, #14163, .F. ) ;
#13187=AXIS2_PLACEMENT_3D ( 'NONE', #1911, #13634, #10120 ) ;
#13191=DIRECTION ( 'NONE',  ( 0.000000000000000000, 0.000000000000000000, -1.000000000000000000 ) ) ;
#13197=ORIENTED_EDGE ( 'NONE', *, *, #8308, .F. ) ;
#13199=ORIENTED_EDGE ( 'NONE', *, *, #5559, .F. ) ;
#13200=ORIENTED_EDGE ( 'NONE', *, *, #7668, .F. ) ;
#13202=EDGE_CURVE ( 'NONE', #7541, #10234, #734, .T. ) ;
#13209=LINE ( 'NONE', #1328, #4398 ) ;
#13210=CARTESIAN_POINT ( 'NONE',  ( -65.73898050152220662, 64.78624853950366003, -81.84847958357697451 ) ) ;
#13211=FACE_OUTER_BOUND ( 'NONE', #554, .T. ) ;
#13213=DIRECTION ( 'NONE',  ( 0.000000000000000000, 0.000000000000000000, 1.000000000000000000 ) ) ;
#13214=DIRECTION ( 'NONE',  ( 0.000000000000000000, 0.000000000000000000, 1.000000000000000000 ) ) ;
#13215=ORIENTED_EDGE ( 'NONE', *, *, #12019, .T. ) ;
#13217=VERTEX_POINT ( 'NONE', #3148 ) ;
#13218=TOROIDAL_SURFACE ( 'NONE', #6535, 2.700000000000000178, 0.2000000000000000111 ) ;
#13219=ORIENTED_EDGE ( 'NONE', *, *, #2584, .T. ) ;
#13220=LINE ( 'NONE', #9329, #8955 ) ;
#13221=CARTESIAN_POINT ( 'NONE',  ( -53.77438362644000591, 82.17411849586700612, -117.9984795835769944 ) ) ;
#13222=EDGE_CURVE ( 'NONE', #6563, #8835, #1579, .T. ) ;
#13224=CIRCLE ( 'NONE', #3297, 1.500000000000001332 ) ;
#13225=DIRECTION ( 'NONE',  ( 0.000000000000000000, 1.000000000000000000, 0.000000000000000000 ) ) ;
#13226=CYLINDRICAL_SURFACE ( 'NONE', #6496, 16.50000000000000000 ) ;
#13229=VECTOR ( 'NONE', #464, 1000.000000000000000 ) ;
#13231=DIRECTION ( 'NONE',  ( 1.000000000000000000, 0.000000000000000000, 0.000000000000000000 ) ) ;
#13232=VERTEX_POINT ( 'NONE', #1976 ) ;
#13233=CARTESIAN_POINT ( 'NONE',  ( -55.52438362644000591, 65.17411849586700612, -86.49847958357699440 ) ) ;
#13238=VERTEX_POINT ( 'NONE', #9110 ) ;
#13241=ORIENTED_EDGE ( 'NONE', *, *, #3186, .T. ) ;
#13244=CIRCLE ( 'NONE', #7564, 8.000000000000007105 ) ;
#13248=EDGE_CURVE ( 'NONE', #14841, #1774, #11292, .T. ) ;
#13250=DIRECTION ( 'NONE',  ( 0.000000000000000000, 0.000000000000000000, 1.000000000000000000 ) ) ;
#13252=DIRECTION ( 'NONE',  ( -1.000000000000000000, 0.000000000000000000, 0.000000000000000000 ) ) ;
#13253=PLANE ( 'NONE',  #2373 ) ;
#13254=EDGE_LOOP ( 'NONE', ( #8755, #3512, #10444, #8804, #917, #4760 ) ) ;
#13255=DIRECTION ( 'NONE',  ( 0.000000000000000000, 0.000000000000000000, -1.000000000000000000 ) ) ;
#13258=AXIS2_PLACEMENT_3D ( 'NONE', #12666, #10401, #10331 ) ;
#13259=EDGE_LOOP ( 'NONE', ( #7662, #4839, #12341, #12706 ) ) ;
#13261=VERTEX_POINT ( 'NONE', #4165 ) ;
#13263=VERTEX_POINT ( 'NONE', #6577 ) ;
#13264=CARTESIAN_POINT ( 'NONE',  ( -77.94906324475290660, 70.01464610989972925, -81.84847958357697451 ) ) ;
#13268=DIRECTION ( 'NONE',  ( 0.000000000000000000, 0.000000000000000000, -1.000000000000000000 ) ) ;
#13276=DIRECTION ( 'NONE',  ( 0.000000000000000000, 0.000000000000000000, -1.000000000000000000 ) ) ;
#13283=FACE_OUTER_BOUND ( 'NONE', #7062, .T. ) ;
#13287=CARTESIAN_POINT ( 'NONE',  ( -90.85838362644101096, 99.17411849586700612, -147.9984795835769944 ) ) ;
#13289=CARTESIAN_POINT ( 'NONE',  ( -88.81638362644100937, 97.99516924618178848, -150.4984795835770228 ) ) ;
#13294=CARTESIAN_POINT ( 'NONE',  ( -52.77438362644100067, 99.17411849586700612, -145.2984795835770058 ) ) ;
#13296=EDGE_LOOP ( 'NONE', ( #1063, #1023, #5694, #9884 ) ) ;
#13297=CIRCLE ( 'NONE', #645, 2.750000000000002665 ) ;
#13298=CARTESIAN_POINT ( 'NONE',  ( -57.27438362643999881, 65.17411849586700612, -79.59847958357700293 ) ) ;
#13300=ORIENTED_EDGE ( 'NONE', *, *, #13613, .F. ) ;
#13301=ORIENTED_EDGE ( 'NONE', *, *, #11812, .T. ) ;
#13305=AXIS2_PLACEMENT_3D ( 'NONE', #8508, #3933, #10913 ) ;
#13308=PLANE ( 'NONE',  #5877 ) ;
#13309=AXIS2_PLACEMENT_3D ( 'NONE', #14582, #1411, #9769 ) ;
#13312=CARTESIAN_POINT ( 'NONE',  ( -52.77438362643999881, 65.17411849586700612, -182.2484795835770228 ) ) ;
#13323=VECTOR ( 'NONE', #8799, 1000.000000000000000 ) ;
#13326=AXIS2_PLACEMENT_3D ( 'NONE', #4712, #337, #4638 ) ;
#13327=EDGE_CURVE ( 'NONE', #3176, #2123, #2555, .T. ) ;
#13329=CARTESIAN_POINT ( 'NONE',  ( -86.77438362644100778, 99.17411849586700612, -79.59847958357700293 ) ) ;
#13334=EDGE_CURVE ( 'NONE', #9205, #2361, #11472, .T. ) ;
#13335=ORIENTED_EDGE ( 'NONE', *, *, #10492, .T. ) ;
#13338=EDGE_CURVE ( 'NONE', #9368, #4210, #11905, .T. ) ;
#13345=LINE ( 'NONE', #2629, #6482 ) ;
#13346=ADVANCED_FACE ( 'NONE', ( #9340 ), #1198, .T. ) ;
#13348=LINE ( 'NONE', #2777, #9025 ) ;
#13349=AXIS2_PLACEMENT_3D ( 'NONE', #9774, #6395, #14508 ) ;
#13350=DIRECTION ( 'NONE',  ( 1.000000000000000000, 0.000000000000000000, 0.000000000000000000 ) ) ;
#13352=CARTESIAN_POINT ( 'NONE',  ( -61.42438362644001160, 82.17411849586700612, -80.14847958357698587 ) ) ;
#13356=CARTESIAN_POINT ( 'NONE',  ( -52.77438362643999881, 65.17411849586700612, -182.2484795835770228 ) ) ;
#13357=ORIENTED_EDGE ( 'NONE', *, *, #2908, .F. ) ;
#13361=CIRCLE ( 'NONE', #10112, 2.750000000000002665 ) ;
#13365=DIRECTION ( 'NONE',  ( 0.3469356515732584523, -0.9378889346118967074, 0.000000000000000000 ) ) ;
#13366=CARTESIAN_POINT ( 'NONE',  ( -101.2743836264399988, 114.1741184958669777, -79.49847958357700861 ) ) ;
#13367=CARTESIAN_POINT ( 'NONE',  ( -86.77438362644001302, 99.17411849586700612, -86.49847958357699440 ) ) ;
#13368=DIRECTION ( 'NONE',  ( -1.000000000000000000, 0.000000000000000000, 0.000000000000000000 ) ) ;
#13369=DIRECTION ( 'NONE',  ( 0.8660254037844383745, -0.5000000000000003331, 0.000000000000000000 ) ) ;
#13371=DIRECTION ( 'NONE',  ( -0.8660254037844387076, -0.4999999999999998890, 0.000000000000000000 ) ) ;
#13372=ORIENTED_EDGE ( 'NONE', *, *, #4620, .T. ) ;
#13373=DIRECTION ( 'NONE',  ( 0.000000000000000000, -0.000000000000000000, -1.000000000000000000 ) ) ;
#13374=ORIENTED_EDGE ( 'NONE', *, *, #14092, .F. ) ;
#13375=VERTEX_POINT ( 'NONE', #10581 ) ;
#13379=DIRECTION ( 'NONE',  ( 0.000000000000000000, 0.000000000000000000, 1.000000000000000000 ) ) ;
#13381=CARTESIAN_POINT ( 'NONE',  ( -86.77438362644001302, 99.17411849586700612, -145.4984795835769660 ) ) ;
#13382=CARTESIAN_POINT ( 'NONE',  ( -89.52438362644001302, 65.17411849586700612, -152.4984795835769944 ) ) ;
#13383=CARTESIAN_POINT ( 'NONE',  ( -80.27438362643999881, 82.17411849586700612, -80.44847958357698303 ) ) ;
#13384=FACE_OUTER_BOUND ( 'NONE', #6199, .T. ) ;
#13385=PLANE ( 'NONE',  #1822 ) ;
#13388=EDGE_LOOP ( 'NONE', ( #11205, #11891 ) ) ;
#13389=LINE ( 'NONE', #9722, #7115 ) ;
#13392=ORIENTED_EDGE ( 'NONE', *, *, #9297, .F. ) ;
#13394=DIRECTION ( 'NONE',  ( 0.000000000000000000, 0.000000000000000000, -1.000000000000000000 ) ) ;
#13395=ADVANCED_FACE ( 'NONE', ( #8344 ), #7187, .F. ) ;
#13399=ADVANCED_FACE ( 'NONE', ( #3521 ), #8106, .F. ) ;
#13400=CARTESIAN_POINT ( 'NONE',  ( -86.77438362643999881, 65.17411849586700612, -147.9984795835769944 ) ) ;
#13401=DIRECTION ( 'NONE',  ( 0.000000000000000000, 1.000000000000000000, 0.000000000000000000 ) ) ;
#13402=DIRECTION ( 'NONE',  ( 0.000000000000000000, 0.000000000000000000, -1.000000000000000000 ) ) ;
#13406=EDGE_LOOP ( 'NONE', ( #10529, #6606, #13452, #9438, #1142 ) ) ;
#13407=EDGE_LOOP ( 'NONE', ( #13182, #3383 ) ) ;
#13410=ORIENTED_EDGE ( 'NONE', *, *, #1261, .F. ) ;
#13412=CARTESIAN_POINT ( 'NONE',  ( -69.77438362644001302, 82.17411849586700612, -79.49847958357700861 ) ) ;
#13413=EDGE_CURVE ( 'NONE', #11838, #1588, #10738, .T. ) ;
#13415=LINE ( 'NONE', #11087, #3830 ) ;
#13421=CARTESIAN_POINT ( 'NONE',  ( -57.02438362644099357, 99.17411849586700612, -145.4984795835769660 ) ) ;
#13422=ORIENTED_EDGE ( 'NONE', *, *, #12273, .T. ) ;
#13424=ORIENTED_EDGE ( 'NONE', *, *, #13860, .T. ) ;
#13427=VERTEX_POINT ( 'NONE', #4770 ) ;
#13431=AXIS2_PLACEMENT_3D ( 'NONE', #12594, #5537, #6775 ) ;
#13433=AXIS2_PLACEMENT_3D ( 'NONE', #3076, #8736, #6435 ) ;
#13434=EDGE_CURVE ( 'NONE', #3140, #1405, #12475, .T. ) ;
#13440=AXIS2_PLACEMENT_3D ( 'NONE', #12521, #1729, #9871 ) ;
#13441=EDGE_CURVE ( 'NONE', #11318, #704, #424, .T. ) ;
#13443=PLANE ( 'NONE',  #9990 ) ;
#13444=CARTESIAN_POINT ( 'NONE',  ( -52.77438362644100067, 101.5320169952374414, -147.9984795835769944 ) ) ;
#13445=CARTESIAN_POINT ( 'NONE',  ( -42.77438362644000591, 110.1741184958670061, -79.59847958357700293 ) ) ;
#13446=CARTESIAN_POINT ( 'NONE',  ( -65.90140028023257912, 89.17411849586700612, -44.99847958359791988 ) ) ;
#13448=ORIENTED_EDGE ( 'NONE', *, *, #13628, .T. ) ;
#13450=CIRCLE ( 'NONE', #11206, 8.050000000000000711 ) ;
#13451=EDGE_LOOP ( 'NONE', ( #13808, #4797, #1224, #5741, #5435, #3885, #9534, #8876 ) ) ;
#13452=ORIENTED_EDGE ( 'NONE', *, *, #607, .T. ) ;
#13453=EDGE_LOOP ( 'NONE', ( #11656, #10390, #8844, #11241, #7388, #8686, #13874, #407 ) ) ;
#13458=FACE_OUTER_BOUND ( 'NONE', #13709, .T. ) ;
#13460=CARTESIAN_POINT ( 'NONE',  ( -69.77438362644100778, 82.17411849586699191, -67.49847958357700861 ) ) ;
#13461=CARTESIAN_POINT ( 'NONE',  ( -53.79538362644100147, 100.9425423703948326, -147.9984795835769944 ) ) ;
#13463=VECTOR ( 'NONE', #2345, 1000.000000000000000 ) ;
#13464=FACE_OUTER_BOUND ( 'NONE', #17, .T. ) ;
#13465=ORIENTED_EDGE ( 'NONE', *, *, #277, .T. ) ;
#13467=ORIENTED_EDGE ( 'NONE', *, *, #11139, .F. ) ;
#13468=AXIS2_PLACEMENT_3D ( 'NONE', #4903, #4821, #1546 ) ;
#13473=DIRECTION ( 'NONE',  ( -1.287488025362404182E-15, -1.000000000000000000, 0.000000000000000000 ) ) ;
#13477=DIRECTION ( 'NONE',  ( -0.000000000000000000, -0.000000000000000000, 1.000000000000000000 ) ) ;
#13479=CARTESIAN_POINT ( 'NONE',  ( -89.27438362644100778, 110.1741184958670061, -79.59847958357700293 ) ) ;
#13482=AXIS2_PLACEMENT_3D ( 'NONE', #14997, #12542, #11368 ) ;
#13485=ORIENTED_EDGE ( 'NONE', *, *, #27, .T. ) ;
#13488=ORIENTED_EDGE ( 'NONE', *, *, #6429, .T. ) ;
#13489=CIRCLE ( 'NONE', #11752, 1.250000000000001110 ) ;
#13491=VECTOR ( 'NONE', #12247, 1000.000000000000114 ) ;
#13492=DIRECTION ( 'NONE',  ( 0.000000000000000000, 1.000000000000000000, 0.000000000000000000 ) ) ;
#13496=DIRECTION ( 'NONE',  ( 0.000000000000000000, 0.000000000000000000, 1.000000000000000000 ) ) ;
#13500=FACE_BOUND ( 'NONE', #10683, .T. ) ;
#13501=ORIENTED_EDGE ( 'NONE', *, *, #7709, .F. ) ;
#13504=ORIENTED_EDGE ( 'NONE', *, *, #11321, .F. ) ;
#13506=VERTEX_POINT ( 'NONE', #9875 ) ;
#13507=ORIENTED_EDGE ( 'NONE', *, *, #5277, .T. ) ;
#13508=ORIENTED_EDGE ( 'NONE', *, *, #7820, .T. ) ;
#13516=ADVANCED_FACE ( 'NONE', ( #5230, #11126 ), #13385, .F. ) ;
#13517=LINE ( 'NONE', #5214, #6656 ) ;
#13521=PLANE ( 'NONE',  #12290 ) ;
#13522=DIRECTION ( 'NONE',  ( 0.000000000000000000, 0.000000000000000000, -1.000000000000000000 ) ) ;
#13523=EDGE_LOOP ( 'NONE', ( #14930, #11590, #3173 ) ) ;
#13527=ORIENTED_EDGE ( 'NONE', *, *, #12725, .F. ) ;
#13528=ORIENTED_EDGE ( 'NONE', *, *, #14404, .T. ) ;
#13529=ORIENTED_EDGE ( 'NONE', *, *, #2509, .T. ) ;
#13532=DIRECTION ( 'NONE',  ( 0.000000000000000000, -1.000000000000000000, 0.000000000000000000 ) ) ;
#13534=FACE_OUTER_BOUND ( 'NONE', #4255, .T. ) ;
#13538=CIRCLE ( 'NONE', #11783, 2.042000000000002036 ) ;
#13542=AXIS2_PLACEMENT_3D ( 'NONE', #12458, #4163, #8888 ) ;
#13543=ADVANCED_FACE ( 'NONE', ( #10821 ), #9642, .T. ) ;
#13548=EDGE_LOOP ( 'NONE', ( #6996, #5550, #12708 ) ) ;
#13553=EDGE_LOOP ( 'NONE', ( #10016, #8797, #15081, #9364, #2480 ) ) ;
#13554=CIRCLE ( 'NONE', #3627, 4.250000000000003553 ) ;
#13556=ORIENTED_EDGE ( 'NONE', *, *, #14283, .T. ) ;
#13558=DIRECTION ( 'NONE',  ( 0.000000000000000000, 0.000000000000000000, -1.000000000000000000 ) ) ;
#13561=CARTESIAN_POINT ( 'NONE',  ( -88.81638362644000040, 63.99516924618178848, -147.9984795835769944 ) ) ;
#13562=DIRECTION ( 'NONE',  ( 0.000000000000000000, 0.000000000000000000, -1.000000000000000000 ) ) ;
#13563=CARTESIAN_POINT ( 'NONE',  ( -84.73238362643999722, 66.35306774555222376, -150.4984795835770228 ) ) ;
#13564=CARTESIAN_POINT ( 'NONE',  ( -86.77438362644001302, 65.17411849586700612, -86.49847958357699440 ) ) ;
#13566=VERTEX_POINT ( 'NONE', #9797 ) ;
#13568=CARTESIAN_POINT ( 'NONE',  ( -72.45546847960635262, 74.51466092245016171, -58.65793715699378197 ) ) ;
#13572=CARTESIAN_POINT ( 'NONE',  ( -55.27438362644100067, 99.17411849586700612, -182.2484795835770228 ) ) ;
#13578=FACE_OUTER_BOUND ( 'NONE', #2390, .T. ) ;
#13579=CONICAL_SURFACE ( 'NONE', #6890, 2.042000000000002036, 1.047197551196596965 ) ;
#13582=VERTEX_POINT ( 'NONE', #7494 ) ;
#13584=EDGE_LOOP ( 'NONE', ( #3767, #7211, #1770, #2715, #2869 ) ) ;
#13586=EDGE_LOOP ( 'NONE', ( #5388, #7677 ) ) ;
#13587=LINE ( 'NONE', #542, #12504 ) ;
#13588=AXIS2_PLACEMENT_3D ( 'NONE', #3564, #2469, #7070 ) ;
#13592=EDGE_CURVE ( 'NONE', #5341, #1220, #14459, .T. ) ;
#13594=CARTESIAN_POINT ( 'NONE',  ( -86.77438362643999881, 67.53201699523744139, -150.4984795835770228 ) ) ;
#13596=CARTESIAN_POINT ( 'NONE',  ( -79.02077156573416516, 60.67411849586702743, -152.4984795835769944 ) ) ;
#13597=FACE_OUTER_BOUND ( 'NONE', #7206, .T. ) ;
#13598=EDGE_CURVE ( 'NONE', #2303, #8186, #1590, .T. ) ;
#13600=EDGE_LOOP ( 'NONE', ( #9411, #9633 ) ) ;
#13601=DIRECTION ( 'NONE',  ( 1.000000000000000000, 0.000000000000000000, 0.000000000000000000 ) ) ;
#13603=ORIENTED_EDGE ( 'NONE', *, *, #13592, .T. ) ;
#13604=ORIENTED_EDGE ( 'NONE', *, *, #1762, .F. ) ;
#13607=DIRECTION ( 'NONE',  ( 0.8660254037844387076, 0.4999999999999998890, 0.000000000000000000 ) ) ;
#13611=DIRECTION ( 'NONE',  ( -0.8660254037844381525, 0.000000000000000000, -0.5000000000000007772 ) ) ;
#13612=LINE ( 'NONE', #3205, #12243 ) ;
#13613=EDGE_CURVE ( 'NONE', #11082, #8835, #7616, .T. ) ;
#13615=EDGE_CURVE ( 'NONE', #9681, #4480, #11743, .T. ) ;
#13617=FACE_OUTER_BOUND ( 'NONE', #14887, .T. ) ;
#13618=ORIENTED_EDGE ( 'NONE', *, *, #6578, .F. ) ;
#13620=ADVANCED_FACE ( 'NONE', ( #644 ), #15057, .F. ) ;
#13624=CARTESIAN_POINT ( 'NONE',  ( -84.73238362643999722, 66.35306774555222376, -147.9984795835769944 ) ) ;
#13625=EDGE_CURVE ( 'NONE', #11570, #5237, #13612, .T. ) ;
#13626=DIRECTION ( 'NONE',  ( 0.000000000000000000, 0.000000000000000000, -1.000000000000000000 ) ) ;
#13628=EDGE_CURVE ( 'NONE', #4013, #5361, #1079, .T. ) ;
#13633=CARTESIAN_POINT ( 'NONE',  ( -70.06129951035623549, 98.17413497942138179, -94.70806078951538609 ) ) ;
#13634=DIRECTION ( 'NONE',  ( 0.000000000000000000, 0.000000000000000000, 1.000000000000000000 ) ) ;
#13638=LINE ( 'NONE', #12471, #2858 ) ;
#13646=PLANE ( 'NONE',  #10796 ) ;
#13647=DIRECTION ( 'NONE',  ( 0.000000000000000000, 0.000000000000000000, -1.000000000000000000 ) ) ;
#13650=ORIENTED_EDGE ( 'NONE', *, *, #1666, .F. ) ;
#13652=VERTEX_POINT ( 'NONE', #11278 ) ;
#13653=VERTEX_POINT ( 'NONE', #12665 ) ;
#13654=ORIENTED_EDGE ( 'NONE', *, *, #6046, .T. ) ;
#13664=LINE ( 'NONE', #9858, #7836 ) ;
#13665=DIRECTION ( 'NONE',  ( 0.000000000000000000, 0.000000000000000000, 1.000000000000000000 ) ) ;
#13666=AXIS2_PLACEMENT_3D ( 'NONE', #8579, #5968, #9577 ) ;
#13668=CARTESIAN_POINT ( 'NONE',  ( -57.02438362643999170, 65.17411849586700612, -145.4984795835769660 ) ) ;
#13669=ORIENTED_EDGE ( 'NONE', *, *, #3538, .T. ) ;
#13670=AXIS2_PLACEMENT_3D ( 'NONE', #5708, #10406, #13078 ) ;
#13672=EDGE_LOOP ( 'NONE', ( #15060, #11550 ) ) ;
#13674=ADVANCED_BREP_SHAPE_REPRESENTATION ( '', ( #5480, #357, #418, #285 ), #15141 ) ;
#13679=CARTESIAN_POINT ( 'NONE',  ( -54.81638362644000040, 66.35306774555222376, -147.9984795835769944 ) ) ;
#13680=LINE ( 'NONE', #5079, #1521 ) ;
#13682=CARTESIAN_POINT ( 'NONE',  ( -90.85838362644101096, 99.17411849586700612, -147.9984795835769944 ) ) ;
#13685=VERTEX_POINT ( 'NONE', #7167 ) ;
#13686=CARTESIAN_POINT ( 'NONE',  ( -86.77438362644100778, 101.5320169952374414, -150.4984795835770228 ) ) ;
#13687=ORIENTED_EDGE ( 'NONE', *, *, #7712, .F. ) ;
#13688=AXIS2_PLACEMENT_3D ( 'NONE', #5623, #14897, #4286 ) ;
#13690=ADVANCED_FACE ( 'NONE', ( #9241 ), #6932, .T. ) ;
#13695=EDGE_CURVE ( 'NONE', #13506, #5739, #12489, .T. ) ;
#13697=FACE_BOUND ( 'NONE', #4339, .T. ) ;
#13698=CARTESIAN_POINT ( 'NONE',  ( -64.53565528768383786, 67.29799558322736175, -83.44847958357698303 ) ) ;
#13699=EDGE_CURVE ( 'NONE', #8210, #5814, #9249, .T. ) ;
#13700=CARTESIAN_POINT ( 'NONE',  ( -88.81638362644000040, 63.99516924618178848, -147.9984795835769944 ) ) ;
#13704=LINE ( 'NONE', #1751, #2899 ) ;
#13705=AXIS2_PLACEMENT_3D ( 'NONE', #7587, #7509, #12313 ) ;
#13706=AXIS2_PLACEMENT_3D ( 'NONE', #12808, #5612, #10318 ) ;
#13709=EDGE_LOOP ( 'NONE', ( #7406, #15026, #14592, #320 ) ) ;
#13710=CIRCLE ( 'NONE', #2548, 4.249999999999996447 ) ;
#13711=CARTESIAN_POINT ( 'NONE',  ( -52.77438362643999881, 65.17411849586700612, -182.2484795835770228 ) ) ;
#13715=DIRECTION ( 'NONE',  ( 0.000000000000000000, 1.000000000000000000, 0.000000000000000000 ) ) ;
#13717=CARTESIAN_POINT ( 'NONE',  ( -56.85838362643999488, 65.17411849586700612, -147.9984795835769944 ) ) ;
#13724=DIRECTION ( 'NONE',  ( -1.000000000000000000, 0.000000000000000000, 0.000000000000000000 ) ) ;
#13726=AXIS2_PLACEMENT_3D ( 'NONE', #13356, #2714, #3799 ) ;
#13727=ADVANCED_FACE ( 'NONE', ( #9395 ), #9321, .T. ) ;
#13728=VERTEX_POINT ( 'NONE', #14291 ) ;
#13729=VERTEX_POINT ( 'NONE', #12823 ) ;
#13730=ORIENTED_EDGE ( 'NONE', *, *, #1755, .F. ) ;
#13731=ORIENTED_EDGE ( 'NONE', *, *, #9578, .T. ) ;
#13738=CARTESIAN_POINT ( 'NONE',  ( -50.73238362644099197, 100.3530677455522238, -150.4984795835770228 ) ) ;
#13740=DIRECTION ( 'NONE',  ( 1.000000000000000000, 0.000000000000000000, 0.000000000000000000 ) ) ;
#13744=DIRECTION ( 'NONE',  ( 1.000000000000000000, 0.000000000000000000, 0.000000000000000000 ) ) ;
#13746=ORIENTED_EDGE ( 'NONE', *, *, #6161, .F. ) ;
#13747=LINE ( 'NONE', #3117, #10478 ) ;
#13749=ORIENTED_EDGE ( 'NONE', *, *, #7568, .T. ) ;
#13750=ORIENTED_EDGE ( 'NONE', *, *, #14503, .F. ) ;
#13751=VECTOR ( 'NONE', #2188, 1000.000000000000000 ) ;
#13754=DIRECTION ( 'NONE',  ( 0.000000000000000000, 0.000000000000000000, 1.000000000000000000 ) ) ;
#13756=CARTESIAN_POINT ( 'NONE',  ( -69.77438362644001302, 82.17411849586700612, -150.4984795835769944 ) ) ;
#13757=CARTESIAN_POINT ( 'NONE',  ( -69.77438362644001302, 82.17411849586700612, -85.04847958357700577 ) ) ;
#13759=CARTESIAN_POINT ( 'NONE',  ( -69.77438362644001302, 74.17411849586699191, -58.99847958357700151 ) ) ;
#13765=VERTEX_POINT ( 'NONE', #8240 ) ;
#13767=EDGE_LOOP ( 'NONE', ( #2559, #13527, #909, #11246 ) ) ;
#13769=ORIENTED_EDGE ( 'NONE', *, *, #2677, .F. ) ;
#13771=FACE_OUTER_BOUND ( 'NONE', #3641, .T. ) ;
#13772=CARTESIAN_POINT ( 'NONE',  ( -52.77438362644000591, 99.17411849586700612, -145.4984795835769660 ) ) ;
#13773=LINE ( 'NONE', #14921, #2309 ) ;
#13775=EDGE_CURVE ( 'NONE', #14091, #12096, #6313, .T. ) ;
#13776=CYLINDRICAL_SURFACE ( 'NONE', #6196, 4.500000000000003553 ) ;
#13777=CARTESIAN_POINT ( 'NONE',  ( -69.77438362644001302, 82.17411849586700612, -85.04847958357699156 ) ) ;
#13780=DIRECTION ( 'NONE',  ( -1.000000000000000000, 0.000000000000000000, 0.000000000000000000 ) ) ;
#13781=EDGE_CURVE ( 'NONE', #13263, #2616, #14062, .T. ) ;
#13782=CARTESIAN_POINT ( 'NONE',  ( -86.77438362644100778, 99.17411849586700612, -147.9984795835769944 ) ) ;
#13784=AXIS2_PLACEMENT_3D ( 'NONE', #7645, #2585, #12289 ) ;
#13785=ORIENTED_EDGE ( 'NONE', *, *, #5456, .F. ) ;
#13786=CARTESIAN_POINT ( 'NONE',  ( -52.77438362644100067, 96.81621999649657084, -147.9984795835769944 ) ) ;
#13792=DIRECTION ( 'NONE',  ( 0.8660254037844381525, 1.060575238724905436E-16, -0.5000000000000007772 ) ) ;
#13793=EDGE_CURVE ( 'NONE', #6998, #957, #12743, .T. ) ;
#13794=DIRECTION ( 'NONE',  ( 0.000000000000000000, 0.000000000000000000, -1.000000000000000000 ) ) ;
#13800=ORIENTED_EDGE ( 'NONE', *, *, #6044, .T. ) ;
#13801=CARTESIAN_POINT ( 'NONE',  ( -91.27438362643999881, 65.17411849586700612, -86.49847958357699440 ) ) ;
#13802=AXIS2_PLACEMENT_3D ( 'NONE', #12197, #9861, #13373 ) ;
#13804=AXIS2_PLACEMENT_3D ( 'NONE', #5500, #5581, #10282 ) ;
#13806=ORIENTED_EDGE ( 'NONE', *, *, #14503, .T. ) ;
#13808=ORIENTED_EDGE ( 'NONE', *, *, #4236, .T. ) ;
#13812=FACE_OUTER_BOUND ( 'NONE', #2986, .T. ) ;
#13815=EDGE_CURVE ( 'NONE', #6563, #13238, #12061, .T. ) ;
#13816=DIRECTION ( 'NONE',  ( 1.000000000000000000, 0.000000000000000000, 0.000000000000000000 ) ) ;
#13818=CARTESIAN_POINT ( 'NONE',  ( -86.77438362644001302, 65.17411849586700612, -145.4984795835769660 ) ) ;
#13820=DIRECTION ( 'NONE',  ( -1.000000000000000000, 0.000000000000000000, 0.000000000000000000 ) ) ;
#13823=ORIENTED_EDGE ( 'NONE', *, *, #4762, .F. ) ;
#13824=DIRECTION ( 'NONE',  ( 1.000000000000000000, 0.000000000000000000, 0.000000000000000000 ) ) ;
#13825=ORIENTED_EDGE ( 'NONE', *, *, #12101, .F. ) ;
#13826=VERTEX_POINT ( 'NONE', #12123 ) ;
#13827=ORIENTED_EDGE ( 'NONE', *, *, #12957, .T. ) ;
#13828=VECTOR ( 'NONE', #10950, 1000.000000000000000 ) ;
#13832=LINE ( 'NONE', #1959, #14661 ) ;
#13833=DIRECTION ( 'NONE',  ( 1.000000000000000000, 0.000000000000000000, 0.000000000000000000 ) ) ;
#13834=CARTESIAN_POINT ( 'NONE',  ( -69.77438362644001302, 74.17411849586699191, -58.99847958357700151 ) ) ;
#13835=DIRECTION ( 'NONE',  ( 1.000000000000000000, 0.000000000000000000, 0.000000000000000000 ) ) ;
#13837=CIRCLE ( 'NONE', #9863, 4.500000000000003553 ) ;
#13838=VERTEX_POINT ( 'NONE', #1493 ) ;
#13840=VERTEX_POINT ( 'NONE', #11962 ) ;
#13841=LINE ( 'NONE', #10488, #2496 ) ;
#13847=LINE ( 'NONE', #15070, #6992 ) ;
#13848=EDGE_CURVE ( 'NONE', #2616, #6604, #8517, .T. ) ;
#13851=CARTESIAN_POINT ( 'NONE',  ( -80.52077156573417938, 103.6741184958669777, -152.4984795835769944 ) ) ;
#13860=EDGE_CURVE ( 'NONE', #9916, #12014, #5215, .T. ) ;
#13862=CARTESIAN_POINT ( 'NONE',  ( -82.27438362643999881, 65.17411849586700612, -145.4984795835769660 ) ) ;
#13867=VERTEX_POINT ( 'NONE', #2802 ) ;
#13871=VERTEX_POINT ( 'NONE', #310 ) ;
#13872=ORIENTED_EDGE ( 'NONE', *, *, #14151, .F. ) ;
#13873=EDGE_CURVE ( 'NONE', #8986, #9154, #7041, .T. ) ;
#13874=ORIENTED_EDGE ( 'NONE', *, *, #6993, .T. ) ;
#13877=ADVANCED_FACE ( 'NONE', ( #9856 ), #13443, .F. ) ;
#13878=LINE ( 'NONE', #14318, #1876 ) ;
#13880=FACE_OUTER_BOUND ( 'NONE', #3167, .T. ) ;
#13881=CYLINDRICAL_SURFACE ( 'NONE', #9819, 2.500000000000002220 ) ;
#13882=DIRECTION ( 'NONE',  ( -1.000000000000000000, 0.000000000000000000, 0.000000000000000000 ) ) ;
#13883=CARTESIAN_POINT ( 'NONE',  ( -86.77438362643999881, 65.17411849586700612, -147.9984795835769944 ) ) ;
#13886=EDGE_CURVE ( 'NONE', #12703, #12970, #12271, .T. ) ;
#13887=ORIENTED_EDGE ( 'NONE', *, *, #14608, .F. ) ;
#13888=DIRECTION ( 'NONE',  ( 0.000000000000000000, 0.000000000000000000, 1.000000000000000000 ) ) ;
#13889=VERTEX_POINT ( 'NONE', #13210 ) ;
#13893=VECTOR ( 'NONE', #5895, 1000.000000000000000 ) ;
#13896=EDGE_CURVE ( 'NONE', #13826, #1753, #10951, .T. ) ;
#13901=FACE_OUTER_BOUND ( 'NONE', #1760, .T. ) ;
#13902=VECTOR ( 'NONE', #13558, 1000.000000000000000 ) ;
#13905=CARTESIAN_POINT ( 'NONE',  ( -50.73238362643999722, 66.35306774555222376, -150.4984795835770228 ) ) ;
#13906=VECTOR ( 'NONE', #9478, 1000.000000000000114 ) ;
#13907=ORIENTED_EDGE ( 'NONE', *, *, #4809, .T. ) ;
#13910=VERTEX_POINT ( 'NONE', #14663 ) ;
#13915=ORIENTED_EDGE ( 'NONE', *, *, #13122, .T. ) ;
#13919=AXIS2_PLACEMENT_3D ( 'NONE', #4476, #7965, #14021 ) ;
#13920=LINE ( 'NONE', #2204, #12293 ) ;
#13922=VECTOR ( 'NONE', #11499, 1000.000000000000000 ) ;
#13924=LINE ( 'NONE', #9346, #5392 ) ;
#13926=AXIS2_PLACEMENT_3D ( 'NONE', #13057, #9460, #14281 ) ;
#13927=CIRCLE ( 'NONE', #7504, 2.500000000000002220 ) ;
#13931=VERTEX_POINT ( 'NONE', #7238 ) ;
#13934=DIRECTION ( 'NONE',  ( 0.000000000000000000, 0.000000000000000000, -1.000000000000000000 ) ) ;
#13942=ADVANCED_FACE ( 'NONE', ( #170 ), #3896, .T. ) ;
#13943=VERTEX_POINT ( 'NONE', #4917 ) ;
#13947=ORIENTED_EDGE ( 'NONE', *, *, #7272, .F. ) ;
#13948=CIRCLE ( 'NONE', #571, 2.500000000000002220 ) ;
#13949=ORIENTED_EDGE ( 'NONE', *, *, #706, .T. ) ;
#13952=VECTOR ( 'NONE', #10386, 1000.000000000000000 ) ;
#13956=DIRECTION ( 'NONE',  ( 1.000000000000000000, 0.000000000000000000, 0.000000000000000000 ) ) ;
#13957=CARTESIAN_POINT ( 'NONE',  ( -56.52438362643999170, 65.17411849586700612, -150.4984795835770228 ) ) ;
#13958=CARTESIAN_POINT ( 'NONE',  ( -37.27438362644000591, 104.6741184958670061, -152.4984795835769944 ) ) ;
#13959=EDGE_CURVE ( 'NONE', #2626, #11629, #2725, .T. ) ;
#13962=CIRCLE ( 'NONE', #2310, 2.042000000000002036 ) ;
#13963=CYLINDRICAL_SURFACE ( 'NONE', #14691, 4.500000000000003553 ) ;
#13964=ORIENTED_EDGE ( 'NONE', *, *, #5675, .F. ) ;
#13965=CARTESIAN_POINT ( 'NONE',  ( -88.81638362644000040, 63.99516924618178848, -150.4984795835770228 ) ) ;
#13966=ORIENTED_EDGE ( 'NONE', *, *, #13434, .F. ) ;
#13972=EDGE_CURVE ( 'NONE', #8717, #4666, #13244, .T. ) ;
#13976=DIRECTION ( 'NONE',  ( 0.000000000000000000, -0.000000000000000000, 1.000000000000000000 ) ) ;
#13977=CARTESIAN_POINT ( 'NONE',  ( -86.27438362644001302, 82.17411849586700612, -150.4984795835769944 ) ) ;
#13978=CARTESIAN_POINT ( 'NONE',  ( -69.77438362644001302, 110.1741184958670061, -152.4984795835769944 ) ) ;
#13979=DIRECTION ( 'NONE',  ( 0.000000000000000000, 1.000000000000000000, 0.000000000000000000 ) ) ;
#13982=ORIENTED_EDGE ( 'NONE', *, *, #5958, .T. ) ;
#13983=DIRECTION ( 'NONE',  ( 0.000000000000000000, 0.000000000000000000, 1.000000000000000000 ) ) ;
#13985=EDGE_CURVE ( 'NONE', #12733, #4114, #1554, .T. ) ;
#13986=VERTEX_POINT ( 'NONE', #11100 ) ;
#13987=EDGE_CURVE ( 'NONE', #10037, #12810, #8535, .T. ) ;
#13988=ORIENTED_EDGE ( 'NONE', *, *, #6040, .F. ) ;
#13992=ORIENTED_EDGE ( 'NONE', *, *, #7665, .T. ) ;
#13994=EDGE_CURVE ( 'NONE', #11184, #3974, #3888, .T. ) ;
#13995=CARTESIAN_POINT ( 'NONE',  ( -52.77438362643999881, 62.81621999649657084, -147.9984795835769944 ) ) ;
#13997=AXIS2_PLACEMENT_3D ( 'NONE', #12438, #10160, #4365 ) ;
#13999=AXIS2_PLACEMENT_3D ( 'NONE', #7776, #7851, #13820 ) ;
#14000=EDGE_CURVE ( 'NONE', #1058, #14010, #13587, .T. ) ;
#14001=CARTESIAN_POINT ( 'NONE',  ( -65.90140028023257912, 89.17411849586700612, -57.99847958357699440 ) ) ;
#14002=ORIENTED_EDGE ( 'NONE', *, *, #6881, .F. ) ;
#14007=AXIS2_PLACEMENT_3D ( 'NONE', #14240, #11921, #4943 ) ;
#14010=VERTEX_POINT ( 'NONE', #2876 ) ;
#14011=VECTOR ( 'NONE', #1160, 1000.000000000000000 ) ;
#14016=CIRCLE ( 'NONE', #4862, 2.500000000000002220 ) ;
#14019=AXIS2_PLACEMENT_3D ( 'NONE', #7130, #1291, #11849 ) ;
#14020=DIRECTION ( 'NONE',  ( 0.000000000000000000, 0.000000000000000000, -1.000000000000000000 ) ) ;
#14021=DIRECTION ( 'NONE',  ( -1.000000000000000000, 0.000000000000000000, 0.000000000000000000 ) ) ;
#14024=ORIENTED_EDGE ( 'NONE', *, *, #521, .T. ) ;
#14025=VERTEX_POINT ( 'NONE', #6310 ) ;
#14027=EDGE_LOOP ( 'NONE', ( #9665, #4117, #4059 ) ) ;
#14028=CIRCLE ( 'NONE', #12303, 1.000000000000000888 ) ;
#14031=AXIS2_PLACEMENT_3D ( 'NONE', #10559, #10479, #4680 ) ;
#14033=VECTOR ( 'NONE', #8937, 1000.000000000000000 ) ;
#14036=DIRECTION ( 'NONE',  ( 1.224646799147351975E-16, 1.000000000000000000, 0.000000000000000000 ) ) ;
#14039=DIRECTION ( 'NONE',  ( 0.000000000000000000, 1.000000000000000000, 0.000000000000000000 ) ) ;
#14040=CARTESIAN_POINT ( 'NONE',  ( -69.77438362644001302, 74.17411849586699191, -79.59847958357700293 ) ) ;
#14043=LINE ( 'NONE', #9149, #889 ) ;
#14045=AXIS2_PLACEMENT_3D ( 'NONE', #7912, #11481, #8850 ) ;
#14047=DIRECTION ( 'NONE',  ( 0.000000000000000000, 0.000000000000000000, -1.000000000000000000 ) ) ;
#14049=VERTEX_POINT ( 'NONE', #5138 ) ;
#14050=VERTEX_POINT ( 'NONE', #14652 ) ;
#14056=LINE ( 'NONE', #15122, #14280 ) ;
#14058=DIRECTION ( 'NONE',  ( 1.000000000000000000, 0.000000000000000000, 0.000000000000000000 ) ) ;
#14061=CARTESIAN_POINT ( 'NONE',  ( -91.02438362643999881, 65.17411849586700612, -145.4984795835769660 ) ) ;
#14062=LINE ( 'NONE', #2421, #78 ) ;
#14063=LINE ( 'NONE', #11, #1363 ) ;
#14064=PLANE ( 'NONE',  #12973 ) ;
#14067=ORIENTED_EDGE ( 'NONE', *, *, #11382, .F. ) ;
#14068=CIRCLE ( 'NONE', #3661, 5.500000000000005329 ) ;
#14069=ORIENTED_EDGE ( 'NONE', *, *, #1746, .T. ) ;
#14070=DIRECTION ( 'NONE',  ( 1.000000000000000000, 0.000000000000000000, 0.000000000000000000 ) ) ;
#14074=EDGE_CURVE ( 'NONE', #13685, #8016, #10004, .T. ) ;
#14079=AXIS2_PLACEMENT_3D ( 'NONE', #13367, #1561, #6317 ) ;
#14080=ADVANCED_FACE ( 'NONE', ( #13283 ), #12264, .T. ) ;
#14081=DIRECTION ( 'NONE',  ( 0.000000000000000000, 0.000000000000000000, -1.000000000000000000 ) ) ;
#14083=ORIENTED_EDGE ( 'NONE', *, *, #40, .T. ) ;
#14084=LINE ( 'NONE', #7116, #12314 ) ;
#14087=ORIENTED_EDGE ( 'NONE', *, *, #14369, .T. ) ;
#14091=VERTEX_POINT ( 'NONE', #4119 ) ;
#14092=EDGE_CURVE ( 'NONE', #10812, #12871, #13489, .T. ) ;
#14098=PLANE ( 'NONE',  #5682 ) ;
#14099=CARTESIAN_POINT ( 'NONE',  ( -80.52077156573417938, 0.000000000000000000, -152.4984795835769944 ) ) ;
#14101=VERTEX_POINT ( 'NONE', #8990 ) ;
#14102=DIRECTION ( 'NONE',  ( 0.000000000000000000, 0.000000000000000000, -1.000000000000000000 ) ) ;
#14103=VERTEX_POINT ( 'NONE', #6615 ) ;
#14105=EDGE_LOOP ( 'NONE', ( #3493, #11548, #3040, #11697 ) ) ;
#14106=ORIENTED_EDGE ( 'NONE', *, *, #15269, .F. ) ;
#14110=PLANE ( 'NONE',  #2914 ) ;
#14111=LINE ( 'NONE', #3481, #3788 ) ;
#14112=CARTESIAN_POINT ( 'NONE',  ( -69.77438362644100778, 82.17411849586699191, -67.49847958357700861 ) ) ;
#14113=LINE ( 'NONE', #12960, #460 ) ;
#14114=DIRECTION ( 'NONE',  ( 0.000000000000000000, 0.000000000000000000, -1.000000000000000000 ) ) ;
#14118=LINE ( 'NONE', #14190, #2561 ) ;
#14121=ORIENTED_EDGE ( 'NONE', *, *, #14733, .T. ) ;
#14125=DIRECTION ( 'NONE',  ( -1.000000000000000000, 0.000000000000000000, 0.000000000000000000 ) ) ;
#14127=CARTESIAN_POINT ( 'NONE',  ( -77.52077156573416516, 103.6741184958669777, -79.59847958357700293 ) ) ;
#14129=FACE_OUTER_BOUND ( 'NONE', #13553, .T. ) ;
#14130=CARTESIAN_POINT ( 'NONE',  ( -62.27438362644000591, 90.17411849586700612, -58.99847958357700151 ) ) ;
#14131=DIRECTION ( 'NONE',  ( 0.000000000000000000, 0.000000000000000000, -1.000000000000000000 ) ) ;
#14132=LINE ( 'NONE', #7011, #5289 ) ;
#14133=EDGE_LOOP ( 'NONE', ( #13603, #774 ) ) ;
#14134=CARTESIAN_POINT ( 'NONE',  ( -59.02799568714584666, 60.67411849586701322, -152.4984795835769944 ) ) ;
#14137=ORIENTED_EDGE ( 'NONE', *, *, #6044, .F. ) ;
#14144=DIRECTION ( 'NONE',  ( -0.4999999999999998890, 0.8660254037844387076, 0.000000000000000000 ) ) ;
#14145=DIRECTION ( 'NONE',  ( -0.8660254037844381525, 0.000000000000000000, -0.5000000000000007772 ) ) ;
#14149=EDGE_LOOP ( 'NONE', ( #15230, #3745, #7308, #9903, #13374, #7182 ) ) ;
#14151=EDGE_CURVE ( 'NONE', #2748, #682, #5680, .T. ) ;
#14152=CARTESIAN_POINT ( 'NONE',  ( -75.01311196519617397, 67.29799558322736175, -83.44847958357698303 ) ) ;
#14161=AXIS2_PLACEMENT_3D ( 'NONE', #12370, #14527, #6336 ) ;
#14163=EDGE_CURVE ( 'NONE', #1856, #8800, #5817, .T. ) ;
#14165=FACE_BOUND ( 'NONE', #13672, .T. ) ;
#14171=ORIENTED_EDGE ( 'NONE', *, *, #10146, .T. ) ;
#14172=ADVANCED_FACE ( 'NONE', ( #1304 ), #8141, .T. ) ;
#14177=ORIENTED_EDGE ( 'NONE', *, *, #13048, .T. ) ;
#14181=DIRECTION ( 'NONE',  ( 1.000000000000000000, 1.727704675731647582E-15, 0.000000000000000000 ) ) ;
#14182=CYLINDRICAL_SURFACE ( 'NONE', #6380, 8.124999999999992895 ) ;
#14183=DIRECTION ( 'NONE',  ( -1.000000000000000000, 0.000000000000000000, 0.000000000000000000 ) ) ;
#14184=CARTESIAN_POINT ( 'NONE',  ( -86.77438362644001302, 65.17411849586700612, -152.4984795835769944 ) ) ;
#14185=AXIS2_PLACEMENT_3D ( 'NONE', #14243, #12086, #3776 ) ;
#14188=EDGE_CURVE ( 'NONE', #14573, #10111, #1341, .T. ) ;
#14190=CARTESIAN_POINT ( 'NONE',  ( -66.41143315690761995, 66.60412428008086749, -81.84847958357698872 ) ) ;
#14191=ORIENTED_EDGE ( 'NONE', *, *, #8027, .T. ) ;
#14192=CARTESIAN_POINT ( 'NONE',  ( -86.77438362643999881, 65.17411849586700612, -79.59847958357700293 ) ) ;
#14193=VECTOR ( 'NONE', #6621, 1000.000000000000000 ) ;
#14194=CIRCLE ( 'NONE', #7527, 2.500000000000002220 ) ;
#14195=ORIENTED_EDGE ( 'NONE', *, *, #6128, .F. ) ;
#14197=ORIENTED_EDGE ( 'NONE', *, *, #1570, .F. ) ;
#14198=CIRCLE ( 'NONE', #7530, 1.250000000000001110 ) ;
#14201=DIRECTION ( 'NONE',  ( -0.4999999999999998890, 0.8660254037844387076, 0.000000000000000000 ) ) ;
#14202=FACE_OUTER_BOUND ( 'NONE', #6423, .T. ) ;
#14204=DIRECTION ( 'NONE',  ( 0.000000000000000000, -0.000000000000000000, -1.000000000000000000 ) ) ;
#14205=CIRCLE ( 'NONE', #2069, 10.50000000000000178 ) ;
#14207=DIRECTION ( 'NONE',  ( -1.000000000000000000, 0.000000000000000000, 0.000000000000000000 ) ) ;
#14209=DIRECTION ( 'NONE',  ( -1.000000000000000000, 0.000000000000000000, 0.000000000000000000 ) ) ;
#14211=LINE ( 'NONE', #9548, #566 ) ;
#14212=AXIS2_PLACEMENT_3D ( 'NONE', #28, #3524, #8345 ) ;
#14213=ORIENTED_EDGE ( 'NONE', *, *, #11682, .T. ) ;
#14215=EDGE_LOOP ( 'NONE', ( #1549, #11299, #2786, #9137 ) ) ;
#14216=EDGE_LOOP ( 'NONE', ( #8384, #260, #11723, #8228 ) ) ;
#14218=AXIS2_PLACEMENT_3D ( 'NONE', #12212, #1586, #6339 ) ;
#14219=VECTOR ( 'NONE', #3876, 1000.000000000000000 ) ;
#14220=EDGE_LOOP ( 'NONE', ( #5438, #9198, #12036, #12972 ) ) ;
#14222=DIRECTION ( 'NONE',  ( 0.000000000000000000, 0.000000000000000000, -1.000000000000000000 ) ) ;
#14226=EDGE_CURVE ( 'NONE', #11654, #557, #9520, .T. ) ;
#14227=AXIS2_PLACEMENT_3D ( 'NONE', #1288, #8426, #12084 ) ;
#14228=FACE_OUTER_BOUND ( 'NONE', #7291, .T. ) ;
#14229=ORIENTED_EDGE ( 'NONE', *, *, #10080, .F. ) ;
#14231=DIRECTION ( 'NONE',  ( 1.000000000000000000, 0.000000000000000000, 0.000000000000000000 ) ) ;
#14235=EDGE_LOOP ( 'NONE', ( #3061, #14889, #8720 ) ) ;
#14240=CARTESIAN_POINT ( 'NONE',  ( -69.77438362644001302, 82.17411849586700612, -85.04847958357699156 ) ) ;
#14243=CARTESIAN_POINT ( 'NONE',  ( -86.77438362644001302, 99.17411849586700612, -86.49847958357699440 ) ) ;
#14246=CIRCLE ( 'NONE', #7584, 8.349999999999996092 ) ;
#14247=ORIENTED_EDGE ( 'NONE', *, *, #7568, .F. ) ;
#14248=AXIS2_PLACEMENT_3D ( 'NONE', #5833, #8148, #12803 ) ;
#14252=EDGE_CURVE ( 'NONE', #5814, #8210, #14469, .T. ) ;
#14255=ORIENTED_EDGE ( 'NONE', *, *, #1398, .T. ) ;
#14257=ORIENTED_EDGE ( 'NONE', *, *, #8677, .T. ) ;
#14258=CIRCLE ( 'NONE', #5362, 1.500000000000001332 ) ;
#14260=EDGE_CURVE ( 'NONE', #6866, #2365, #5319, .T. ) ;
#14261=CIRCLE ( 'NONE', #1886, 16.50000000000000000 ) ;
#14264=FACE_OUTER_BOUND ( 'NONE', #7871, .T. ) ;
#14265=EDGE_CURVE ( 'NONE', #13838, #9398, #6149, .T. ) ;
#14267=CARTESIAN_POINT ( 'NONE',  ( -86.77438362644001302, 65.17411849586700612, -86.49847958357699440 ) ) ;
#14268=PLANE ( 'NONE',  #9963 ) ;
#14269=FACE_OUTER_BOUND ( 'NONE', #12308, .T. ) ;
#14273=DIRECTION ( 'NONE',  ( 0.000000000000000000, 0.000000000000000000, 1.000000000000000000 ) ) ;
#14276=CIRCLE ( 'NONE', #3129, 2.500000000000002220 ) ;
#14278=ORIENTED_EDGE ( 'NONE', *, *, #6526, .F. ) ;
#14279=VERTEX_POINT ( 'NONE', #10532 ) ;
#14280=VECTOR ( 'NONE', #10555, 1000.000000000000000 ) ;
#14281=DIRECTION ( 'NONE',  ( 0.000000000000000000, 0.000000000000000000, 1.000000000000000000 ) ) ;
#14283=EDGE_CURVE ( 'NONE', #8154, #2658, #11253, .T. ) ;
#14285=AXIS2_PLACEMENT_3D ( 'NONE', #4296, #6564, #9021 ) ;
#14286=CARTESIAN_POINT ( 'NONE',  ( -88.81638362644000040, 63.99516924618178848, -147.9984795835769944 ) ) ;
#14291=CARTESIAN_POINT ( 'NONE',  ( -80.52077156573417938, 59.67411849586701322, -152.4984795835769944 ) ) ;
#14292=DIRECTION ( 'NONE',  ( 0.000000000000000000, -1.000000000000000000, 0.000000000000000000 ) ) ;
#14294=DIRECTION ( 'NONE',  ( 0.000000000000000000, 0.000000000000000000, 1.000000000000000000 ) ) ;
#14295=ORIENTED_EDGE ( 'NONE', *, *, #11325, .F. ) ;
#14296=PLANE ( 'NONE',  #1315 ) ;
#14298=EDGE_LOOP ( 'NONE', ( #15195, #13508, #772, #6646 ) ) ;
#14300=AXIS2_PLACEMENT_3D ( 'NONE', #1920, #8902, #11537 ) ;
#14304=CARTESIAN_POINT ( 'NONE',  ( -69.77438362644001302, 82.17411849586700612, -150.4984795835769944 ) ) ;
#14305=CARTESIAN_POINT ( 'NONE',  ( -52.77438362643999881, 65.17411849586700612, -150.4984795835770228 ) ) ;
#14307=CIRCLE ( 'NONE', #6169, 10.50000000000000178 ) ;
#14308=PLANE ( 'NONE',  #10748 ) ;
#14309=EDGE_LOOP ( 'NONE', ( #6844, #11661, #3826, #8661 ) ) ;
#14312=ORIENTED_EDGE ( 'NONE', *, *, #2044, .T. ) ;
#14315=ORIENTED_EDGE ( 'NONE', *, *, #4419, .T. ) ;
#14316=EDGE_CURVE ( 'NONE', #11145, #3516, #7054, .T. ) ;
#14318=CARTESIAN_POINT ( 'NONE',  ( -35.27438362644000591, 59.67411849586700612, -79.49847958357700861 ) ) ;
#14320=CARTESIAN_POINT ( 'NONE',  ( -37.27438362644000591, 65.17411849586700612, -15.85886927678779834 ) ) ;
#14321=DIRECTION ( 'NONE',  ( 0.000000000000000000, 0.000000000000000000, -1.000000000000000000 ) ) ;
#14322=CARTESIAN_POINT ( 'NONE',  ( -101.2743836264399988, 57.67411849586699901, -67.49847958357700861 ) ) ;
#14324=ORIENTED_EDGE ( 'NONE', *, *, #10470, .T. ) ;
#14325=CARTESIAN_POINT ( 'NONE',  ( -63.06767964790545022, 68.65632084656354550, -83.44847958357698303 ) ) ;
#14328=VERTEX_POINT ( 'NONE', #12402 ) ;
#14332=VERTEX_POINT ( 'NONE', #284 ) ;
#14333=EDGE_CURVE ( 'NONE', #7802, #632, #9023, .T. ) ;
#14334=ORIENTED_EDGE ( 'NONE', *, *, #6285, .F. ) ;
#14335=AXIS2_PLACEMENT_3D ( 'NONE', #358, #8731, #12229 ) ;
#14336=FACE_OUTER_BOUND ( 'NONE', #11718, .T. ) ;
#14338=FACE_OUTER_BOUND ( 'NONE', #2698, .T. ) ;
#14341=CARTESIAN_POINT ( 'NONE',  ( -54.81638362644000040, 63.99516924618178848, -150.4984795835770228 ) ) ;
#14343=DIRECTION ( 'NONE',  ( -0.8660254037844387076, -0.4999999999999998890, 0.000000000000000000 ) ) ;
#14344=EDGE_CURVE ( 'NONE', #2214, #8981, #1693, .T. ) ;
#14345=ORIENTED_EDGE ( 'NONE', *, *, #5394, .T. ) ;
#14346=ORIENTED_EDGE ( 'NONE', *, *, #14659, .T. ) ;
#14348=ORIENTED_EDGE ( 'NONE', *, *, #5854, .T. ) ;
#14349=EDGE_CURVE ( 'NONE', #389, #4822, #13345, .T. ) ;
#14353=DIRECTION ( 'NONE',  ( 0.000000000000000000, 0.000000000000000000, -1.000000000000000000 ) ) ;
#14354=CYLINDRICAL_SURFACE ( 'NONE', #6038, 3.000000000000002665 ) ;
#14358=DIRECTION ( 'NONE',  ( -1.000000000000000000, -1.541976423090494894E-16, 0.000000000000000000 ) ) ;
#14359=CARTESIAN_POINT ( 'NONE',  ( -101.2743836264399988, 111.1741184958670061, -15.85886927678779834 ) ) ;
#14360=DIRECTION ( 'NONE',  ( -0.000000000000000000, -0.000000000000000000, -1.000000000000000000 ) ) ;
#14361=DIRECTION ( 'NONE',  ( -1.000000000000000000, 0.000000000000000000, 0.000000000000000000 ) ) ;
#14362=PLANE ( 'NONE',  #12481 ) ;
#14363=ORIENTED_EDGE ( 'NONE', *, *, #11415, .F. ) ;
#14366=EDGE_LOOP ( 'NONE', ( #949, #11588, #3802, #1026 ) ) ;
#14367=EDGE_LOOP ( 'NONE', ( #7442, #10702, #2697, #5303 ) ) ;
#14369=EDGE_CURVE ( 'NONE', #913, #11018, #524, .T. ) ;
#14373=FACE_OUTER_BOUND ( 'NONE', #9151, .T. ) ;
#14374=CYLINDRICAL_SURFACE ( 'NONE', #2875, 4.499999999999997335 ) ;
#14375=DIRECTION ( 'NONE',  ( -1.000000000000000000, 0.000000000000000000, 0.000000000000000000 ) ) ;
#14376=DIRECTION ( 'NONE',  ( 0.000000000000000000, 0.000000000000000000, -1.000000000000000000 ) ) ;
#14377=ORIENTED_EDGE ( 'NONE', *, *, #5717, .F. ) ;
#14380=ORIENTED_EDGE ( 'NONE', *, *, #6040, .T. ) ;
#14387=FACE_OUTER_BOUND ( 'NONE', #11821, .T. ) ;
#14391=DIRECTION ( 'NONE',  ( 0.000000000000000000, 0.000000000000000000, -1.000000000000000000 ) ) ;
#14397=EDGE_LOOP ( 'NONE', ( #3436, #12376 ) ) ;
#14399=CIRCLE ( 'NONE', #7731, 2.500000000000002220 ) ;
#14400=CARTESIAN_POINT ( 'NONE',  ( -86.77438362644001302, 99.17411849586700612, -152.4984795835769944 ) ) ;
#14403=AXIS2_PLACEMENT_3D ( 'NONE', #5110, #9824, #3935 ) ;
#14404=EDGE_CURVE ( 'NONE', #587, #9170, #6512, .T. ) ;
#14405=CARTESIAN_POINT ( 'NONE',  ( -69.77438362644001302, 82.17411849586700612, -112.9984795835769944 ) ) ;
#14406=CARTESIAN_POINT ( 'NONE',  ( -88.81638362644100937, 97.99516924618178848, -147.9984795835769944 ) ) ;
#14407=FACE_BOUND ( 'NONE', #12256, .T. ) ;
#14409=EDGE_CURVE ( 'NONE', #486, #12362, #6250, .T. ) ;
#14412=AXIS2_PLACEMENT_3D ( 'NONE', #3484, #15265, #8147 ) ;
#14414=LINE ( 'NONE', #10867, #11980 ) ;
#14419=ORIENTED_EDGE ( 'NONE', *, *, #12834, .F. ) ;
#14421=AXIS2_PLACEMENT_3D ( 'NONE', #7469, #3964, #11959 ) ;
#14422=DIRECTION ( 'NONE',  ( 1.000000000000000000, 0.000000000000000000, 0.000000000000000000 ) ) ;
#14424=DIRECTION ( 'NONE',  ( 0.8660254037844387076, 0.4999999999999998890, 0.000000000000000000 ) ) ;
#14426=DIRECTION ( 'NONE',  ( -1.000000000000000000, 0.000000000000000000, -0.000000000000000000 ) ) ;
#14428=EDGE_CURVE ( 'NONE', #11930, #7225, #4991, .T. ) ;
#14429=FACE_OUTER_BOUND ( 'NONE', #9685, .T. ) ;
#14430=FACE_OUTER_BOUND ( 'NONE', #9988, .T. ) ;
#14432=CARTESIAN_POINT ( 'NONE',  ( -63.28565528768381654, 67.29799558322736175, -81.84847958357697451 ) ) ;
#14434=DIRECTION ( 'NONE',  ( 0.000000000000000000, -0.000000000000000000, 1.000000000000000000 ) ) ;
#14435=CARTESIAN_POINT ( 'NONE',  ( -86.77438362644100778, 101.5320169952374414, -147.9984795835769944 ) ) ;
#14436=ORIENTED_EDGE ( 'NONE', *, *, #7929, .T. ) ;
#14441=ORIENTED_EDGE ( 'NONE', *, *, #13985, .F. ) ;
#14443=EDGE_CURVE ( 'NONE', #8857, #6323, #8442, .T. ) ;
#14445=AXIS2_PLACEMENT_3D ( 'NONE', #1665, #14453, #12139 ) ;
#14450=EDGE_CURVE ( 'NONE', #10494, #4413, #372, .T. ) ;
#14451=DIRECTION ( 'NONE',  ( 0.000000000000000000, 0.000000000000000000, -1.000000000000000000 ) ) ;
#14453=DIRECTION ( 'NONE',  ( 0.000000000000000000, 0.000000000000000000, 1.000000000000000000 ) ) ;
#14454=EDGE_CURVE ( 'NONE', #3974, #4383, #25, .T. ) ;
#14455=CARTESIAN_POINT ( 'NONE',  ( -80.52077156573417938, 60.67411849586702743, -79.59847958357700293 ) ) ;
#14456=EDGE_CURVE ( 'NONE', #8210, #2658, #7526, .T. ) ;
#14459=CIRCLE ( 'NONE', #14218, 2.700000000000001066 ) ;
#14460=VECTOR ( 'NONE', #9989, 1000.000000000000000 ) ;
#14464=ADVANCED_FACE ( 'NONE', ( #12245 ), #1615, .F. ) ;
#14466=ORIENTED_EDGE ( 'NONE', *, *, #11625, .T. ) ;
#14469=CIRCLE ( 'NONE', #6073, 3.749999999999996447 ) ;
#14470=EDGE_CURVE ( 'NONE', #4691, #12791, #7957, .T. ) ;
#14472=DIRECTION ( 'NONE',  ( -1.000000000000000000, 0.000000000000000000, 0.000000000000000000 ) ) ;
#14475=DIRECTION ( 'NONE',  ( 0.000000000000000000, 0.000000000000000000, 1.000000000000000000 ) ) ;
#14480=ORIENTED_EDGE ( 'NONE', *, *, #11799, .F. ) ;
#14481=CARTESIAN_POINT ( 'NONE',  ( -69.77438362644100778, 82.17411849586699191, -67.49847958357700861 ) ) ;
#14484=EDGE_LOOP ( 'NONE', ( #7155, #3135 ) ) ;
#14485=CARTESIAN_POINT ( 'NONE',  ( -77.52077156573416516, 60.67411849586702743, -73.34256232478206528 ) ) ;
#14487=DIRECTION ( 'NONE',  ( 0.000000000000000000, 1.000000000000000000, 0.000000000000000000 ) ) ;
#14492=LINE ( 'NONE', #13352, #6599 ) ;
#14494=ORIENTED_EDGE ( 'NONE', *, *, #5140, .F. ) ;
#14495=CARTESIAN_POINT ( 'NONE',  ( -52.77438362643999881, 65.17411849586700612, -79.59847958357700293 ) ) ;
#14503=EDGE_CURVE ( 'NONE', #2640, #6920, #8039, .T. ) ;
#14508=DIRECTION ( 'NONE',  ( 1.000000000000000000, 0.000000000000000000, 0.000000000000000000 ) ) ;
#14509=DIRECTION ( 'NONE',  ( -1.000000000000000000, 0.000000000000000000, 0.000000000000000000 ) ) ;
#14512=PLANE ( 'NONE',  #1388 ) ;
#14513=CARTESIAN_POINT ( 'NONE',  ( -69.77438362644001302, 82.17411849586700612, -82.44847958357698303 ) ) ;
#14518=ORIENTED_EDGE ( 'NONE', *, *, #14565, .T. ) ;
#14520=EDGE_CURVE ( 'NONE', #6682, #10550, #6817, .T. ) ;
#14522=VECTOR ( 'NONE', #2093, 1000.000000000000000 ) ;
#14524=ADVANCED_FACE ( 'NONE', ( #2146, #6893 ), #7892, .T. ) ;
#14525=CIRCLE ( 'NONE', #2641, 2.750000000000002665 ) ;
#14527=DIRECTION ( 'NONE',  ( -0.000000000000000000, 1.000000000000000000, 0.000000000000000000 ) ) ;
#14528=DIRECTION ( 'NONE',  ( -1.000000000000000000, 0.000000000000000000, 0.000000000000000000 ) ) ;
#14533=CARTESIAN_POINT ( 'NONE',  ( -62.02799568714584666, 59.67411849586701322, -15.85886927678779834 ) ) ;
#14534=CIRCLE ( 'NONE', #1164, 5.499999999999998224 ) ;
#14537=ORIENTED_EDGE ( 'NONE', *, *, #11349, .T. ) ;
#14542=ADVANCED_FACE ( 'NONE', ( #11536 ), #10358, .T. ) ;
#14544=LINE ( 'NONE', #3926, #5845 ) ;
#14546=LINE ( 'NONE', #6495, #2790 ) ;
#14548=EDGE_CURVE ( 'NONE', #14010, #3959, #5734, .T. ) ;
#14549=DIRECTION ( 'NONE',  ( 0.000000000000000000, 0.000000000000000000, -1.000000000000000000 ) ) ;
#14550=DIRECTION ( 'NONE',  ( 0.8660254037844383745, -0.5000000000000003331, 0.000000000000000000 ) ) ;
#14551=CARTESIAN_POINT ( 'NONE',  ( -52.77438362644100067, 99.17411849586700612, -145.4984795835769944 ) ) ;
#14552=DIRECTION ( 'NONE',  ( 0.000000000000000000, 1.000000000000000000, 0.000000000000000000 ) ) ;
#14554=ORIENTED_EDGE ( 'NONE', *, *, #2783, .F. ) ;
#14555=EDGE_LOOP ( 'NONE', ( #8093, #7153, #9683 ) ) ;
#14559=CONICAL_SURFACE ( 'NONE', #2673, 3.750000000000003553, 0.7853981633974476129 ) ;
#14560=DIRECTION ( 'NONE',  ( 0.000000000000000000, -0.8571673007021106683, 0.5150380749100569311 ) ) ;
#14565=EDGE_CURVE ( 'NONE', #9704, #1058, #9191, .T. ) ;
#14568=DIRECTION ( 'NONE',  ( 0.000000000000000000, -0.000000000000000000, 1.000000000000000000 ) ) ;
#14573=VERTEX_POINT ( 'NONE', #11304 ) ;
#14575=VERTEX_POINT ( 'NONE', #1839 ) ;
#14576=VERTEX_POINT ( 'NONE', #675 ) ;
#14580=AXIS2_PLACEMENT_3D ( 'NONE', #9582, #5810, #8277 ) ;
#14582=CARTESIAN_POINT ( 'NONE',  ( -86.77438362644001302, 65.17411849586700612, -152.4984795835769944 ) ) ;
#14584=DIRECTION ( 'NONE',  ( 0.000000000000000000, 0.000000000000000000, 1.000000000000000000 ) ) ;
#14587=CARTESIAN_POINT ( 'NONE',  ( -56.85838362643999488, 65.17411849586700612, -147.9984795835769944 ) ) ;
#14591=VECTOR ( 'NONE', #12317, 1000.000000000000000 ) ;
#14592=ORIENTED_EDGE ( 'NONE', *, *, #3421, .F. ) ;
#14593=CARTESIAN_POINT ( 'NONE',  ( -55.27438362643999881, 65.17411849586700612, -145.2984795835770058 ) ) ;
#14594=ORIENTED_EDGE ( 'NONE', *, *, #12379, .F. ) ;
#14598=DIRECTION ( 'NONE',  ( -1.000000000000000000, 0.000000000000000000, 0.000000000000000000 ) ) ;
#14599=PLANE ( 'NONE',  #616 ) ;
#14600=CARTESIAN_POINT ( 'NONE',  ( -90.52438362643999881, 65.17411849586700612, -150.4984795835770228 ) ) ;
#14602=DIRECTION ( 'NONE',  ( -1.000000000000000000, 0.000000000000000000, 0.000000000000000000 ) ) ;
#14604=EDGE_CURVE ( 'NONE', #15148, #11761, #9935, .T. ) ;
#14605=DIRECTION ( 'NONE',  ( -1.000000000000000000, 0.000000000000000000, 0.000000000000000000 ) ) ;
#14608=EDGE_CURVE ( 'NONE', #10624, #3281, #6967, .T. ) ;
#14613=CARTESIAN_POINT ( 'NONE',  ( -86.77438362644001302, 99.17411849586700612, -152.4984795835769944 ) ) ;
#14618=DIRECTION ( 'NONE',  ( 2.065146995210485003E-17, 4.251773225433349175E-17, 1.000000000000000000 ) ) ;
#14619=CARTESIAN_POINT ( 'NONE',  ( -86.77438362644100778, 96.81621999649657084, -147.9984795835769944 ) ) ;
#14622=EDGE_CURVE ( 'NONE', #14101, #4356, #10169, .T. ) ;
#14623=CYLINDRICAL_SURFACE ( 'NONE', #2026, 2.000000000000001776 ) ;
#14625=ORIENTED_EDGE ( 'NONE', *, *, #2908, .T. ) ;
#14629=EDGE_CURVE ( 'NONE', #4356, #14101, #11425, .T. ) ;
#14630=EDGE_CURVE ( 'NONE', #10105, #3491, #1283, .T. ) ;
#14635=DIRECTION ( 'NONE',  ( 0.000000000000000000, 1.000000000000000000, 0.000000000000000000 ) ) ;
#14636=AXIS2_PLACEMENT_3D ( 'NONE', #6218, #1537, #5265 ) ;
#14638=DIRECTION ( 'NONE',  ( 0.000000000000000000, 0.000000000000000000, 1.000000000000000000 ) ) ;
#14639=FACE_OUTER_BOUND ( 'NONE', #11357, .T. ) ;
#14642=EDGE_CURVE ( 'NONE', #1405, #3140, #265, .T. ) ;
#14647=ORIENTED_EDGE ( 'NONE', *, *, #7749, .F. ) ;
#14648=ORIENTED_EDGE ( 'NONE', *, *, #9344, .F. ) ;
#14650=ORIENTED_EDGE ( 'NONE', *, *, #6304, .T. ) ;
#14652=CARTESIAN_POINT ( 'NONE',  ( -65.78565528768382364, 67.29799558322736175, -81.84847958357697451 ) ) ;
#14653=EDGE_CURVE ( 'NONE', #16, #13148, #3461, .T. ) ;
#14659=EDGE_CURVE ( 'NONE', #13263, #11097, #2291, .T. ) ;
#14661=VECTOR ( 'NONE', #941, 1000.000000000000000 ) ;
#14663=CARTESIAN_POINT ( 'NONE',  ( -82.52438362643998460, 65.17411849586700612, -149.9984795835770228 ) ) ;
#14665=DIRECTION ( 'NONE',  ( -1.287488025362404182E-15, -1.000000000000000000, 0.000000000000000000 ) ) ;
#14669=DIRECTION ( 'NONE',  ( 0.000000000000000000, 0.000000000000000000, 1.000000000000000000 ) ) ;
#14670=AXIS2_PLACEMENT_3D ( 'NONE', #815, #6953, #11673 ) ;
#14672=ORIENTED_EDGE ( 'NONE', *, *, #3872, .F. ) ;
#14674=DIRECTION ( 'NONE',  ( 0.000000000000000000, 0.000000000000000000, -1.000000000000000000 ) ) ;
#14675=DIRECTION ( 'NONE',  ( 7.199281117894584284E-17, -0.7071067811865485719, -0.7071067811865465735 ) ) ;
#14678=AXIS2_PLACEMENT_3D ( 'NONE', #9734, #8729, #9964 ) ;
#14683=CARTESIAN_POINT ( 'NONE',  ( -101.2743836264399988, 60.67411849586700612, -79.49847958357700861 ) ) ;
#14684=VERTEX_POINT ( 'NONE', #875 ) ;
#14685=CARTESIAN_POINT ( 'NONE',  ( -75.01311196519617397, 67.29799558322736175, -81.84847958357697451 ) ) ;
#14686=VECTOR ( 'NONE', #8256, 1000.000000000000000 ) ;
#14688=CARTESIAN_POINT ( 'NONE',  ( -88.81638362644100937, 97.99516924618178848, -150.4984795835770228 ) ) ;
#14691=AXIS2_PLACEMENT_3D ( 'NONE', #8304, #5995, #1235 ) ;
#14692=CARTESIAN_POINT ( 'NONE',  ( -52.77438362644000591, 99.17411849586700612, -86.49847958357699440 ) ) ;
#14693=EDGE_CURVE ( 'NONE', #10808, #12550, #13841, .T. ) ;
#14698=CARTESIAN_POINT ( 'NONE',  ( -53.27438362644000591, 82.17411849586700612, -150.4984795835769944 ) ) ;
#14699=LINE ( 'NONE', #3073, #5368 ) ;
#14700=CYLINDRICAL_SURFACE ( 'NONE', #7860, 16.06499999999999773 ) ;
#14705=CYLINDRICAL_SURFACE ( 'NONE', #2835, 4.249999999999996447 ) ;
#14708=AXIS2_PLACEMENT_3D ( 'NONE', #5986, #7064, #14181 ) ;
#14709=EDGE_CURVE ( 'NONE', #9995, #12177, #4453, .T. ) ;
#14710=AXIS2_PLACEMENT_3D ( 'NONE', #12480, #3086, #15014 ) ;
#14712=LINE ( 'NONE', #3948, #5407 ) ;
#14713=LINE ( 'NONE', #10128, #8774 ) ;
#14719=CONICAL_SURFACE ( 'NONE', #9512, 3.749999999999996447, 0.7853981633974476129 ) ;
#14721=EDGE_LOOP ( 'NONE', ( #15113, #9362, #11489, #13887 ) ) ;
#14723=EDGE_LOOP ( 'NONE', ( #15098, #11951, #9825, #10870 ) ) ;
#14724=ORIENTED_EDGE ( 'NONE', *, *, #9593, .F. ) ;
#14726=VERTEX_POINT ( 'NONE', #6791 ) ;
#14727=ADVANCED_FACE ( 'NONE', ( #8949, #727 ), #15064, .T. ) ;
#14728=ORIENTED_EDGE ( 'NONE', *, *, #10095, .F. ) ;
#14729=DIRECTION ( 'NONE',  ( 0.000000000000000000, 0.000000000000000000, -1.000000000000000000 ) ) ;
#14732=VECTOR ( 'NONE', #14424, 1000.000000000000000 ) ;
#14733=EDGE_CURVE ( 'NONE', #7541, #10091, #15135, .T. ) ;
#14735=CIRCLE ( 'NONE', #7084, 2.750000000000002665 ) ;
#14738=DIRECTION ( 'NONE',  ( 0.000000000000000000, 0.000000000000000000, 1.000000000000000000 ) ) ;
#14739=DIRECTION ( 'NONE',  ( 0.000000000000000000, 0.000000000000000000, -1.000000000000000000 ) ) ;
#14741=CARTESIAN_POINT ( 'NONE',  ( -54.81638362644100226, 97.99516924618178848, -150.4984795835770228 ) ) ;
#14745=ADVANCED_FACE ( 'NONE', ( #10175 ), #12831, .F. ) ;
#14746=VERTEX_POINT ( 'NONE', #1027 ) ;
#14755=CARTESIAN_POINT ( 'NONE',  ( -69.77438362644001302, 71.67411849586700612, -80.44847958357698303 ) ) ;
#14757=EDGE_CURVE ( 'NONE', #14091, #1421, #8014, .T. ) ;
#14758=EDGE_CURVE ( 'NONE', #2834, #10983, #3012, .T. ) ;
#14759=FACE_OUTER_BOUND ( 'NONE', #15178, .T. ) ;
#14760=DIRECTION ( 'NONE',  ( 0.3469356515732570645, 0.9378889346118971515, 0.000000000000000000 ) ) ;
#14765=CIRCLE ( 'NONE', #11804, 4.249999999999996447 ) ;
#14767=EDGE_LOOP ( 'NONE', ( #1204, #13529, #8595, #1530 ) ) ;
#14768=LINE ( 'NONE', #13686, #4898 ) ;
#14771=AXIS2_PLACEMENT_3D ( 'NONE', #11579, #7932, #7790 ) ;
#14774=VECTOR ( 'NONE', #5850, 1000.000000000000000 ) ;
#14776=PLANE ( 'NONE',  #9783 ) ;
#14778=VECTOR ( 'NONE', #6982, 1000.000000000000000 ) ;
#14781=DIRECTION ( 'NONE',  ( 1.000000000000000000, 0.000000000000000000, 0.000000000000000000 ) ) ;
#14782=CARTESIAN_POINT ( 'NONE',  ( -72.92551479769302603, 97.86074886511958937, -93.49847958357699440 ) ) ;
#14784=VERTEX_POINT ( 'NONE', #12672 ) ;
#14785=ORIENTED_EDGE ( 'NONE', *, *, #4110, .T. ) ;
#14789=DIRECTION ( 'NONE',  ( 0.000000000000000000, 0.000000000000000000, 1.000000000000000000 ) ) ;
#14791=DIRECTION ( 'NONE',  ( 1.000000000000000000, 0.000000000000000000, 0.000000000000000000 ) ) ;
#14792=CARTESIAN_POINT ( 'NONE',  ( -55.52438362644000591, 99.17411849586700612, -86.49847958357699440 ) ) ;
#14793=CARTESIAN_POINT ( 'NONE',  ( -35.27438362644000591, 60.67411849586700612, -67.49847958357700861 ) ) ;
#14794=EDGE_CURVE ( 'NONE', #10105, #11586, #6981, .T. ) ;
#14798=DIRECTION ( 'NONE',  ( 0.000000000000000000, 0.000000000000000000, -1.000000000000000000 ) ) ;
#14799=EDGE_CURVE ( 'NONE', #13889, #4585, #274, .T. ) ;
#14801=EDGE_LOOP ( 'NONE', ( #7921, #10447, #13750, #13073 ) ) ;
#14803=ORIENTED_EDGE ( 'NONE', *, *, #6424, .T. ) ;
#14808=CARTESIAN_POINT ( 'NONE',  ( -86.77438362644100778, 99.17411849586700612, -182.2484795835770228 ) ) ;
#14810=CARTESIAN_POINT ( 'NONE',  ( -84.73238362643999722, 63.99516924618178848, -147.9984795835769944 ) ) ;
#14811=DIRECTION ( 'NONE',  ( -1.000000000000000000, 0.000000000000000000, 0.000000000000000000 ) ) ;
#14812=DIRECTION ( 'NONE',  ( 0.000000000000000000, 0.000000000000000000, -1.000000000000000000 ) ) ;
#14814=CARTESIAN_POINT ( 'NONE',  ( -86.77438362643999881, 67.53201699523744139, -147.9984795835769944 ) ) ;
#14815=ADVANCED_FACE ( 'NONE', ( #6867 ), #2046, .F. ) ;
#14816=CARTESIAN_POINT ( 'NONE',  ( -73.01311196519618818, 67.29799558322736175, -83.44847958357698303 ) ) ;
#14819=CARTESIAN_POINT ( 'NONE',  ( -86.77438362643999881, 65.17411849586700612, -147.9984795835769944 ) ) ;
#14825=CARTESIAN_POINT ( 'NONE',  ( -69.77438362644001302, 92.67411849586700612, -80.44847958357698303 ) ) ;
#14827=EDGE_CURVE ( 'NONE', #8472, #14103, #13220, .T. ) ;
#14830=LINE ( 'NONE', #4214, #4268 ) ;
#14831=CARTESIAN_POINT ( 'NONE',  ( -59.02799568714584666, 103.6741184958669919, -73.34256232478206528 ) ) ;
#14832=CIRCLE ( 'NONE', #4193, 2.042000000000002036 ) ;
#14833=DIRECTION ( 'NONE',  ( 1.000000000000000000, 0.000000000000000000, -0.000000000000000000 ) ) ;
#14838=DIRECTION ( 'NONE',  ( 0.000000000000000000, 0.000000000000000000, 1.000000000000000000 ) ) ;
#14841=VERTEX_POINT ( 'NONE', #6021 ) ;
#14843=VERTEX_POINT ( 'NONE', #5947 ) ;
#14844=DIRECTION ( 'NONE',  ( -1.000000000000000000, 0.000000000000000000, 0.000000000000000000 ) ) ;
#14846=DIRECTION ( 'NONE',  ( 0.000000000000000000, 0.000000000000000000, -1.000000000000000000 ) ) ;
#14850=FACE_OUTER_BOUND ( 'NONE', #13406, .T. ) ;
#14851=CARTESIAN_POINT ( 'NONE',  ( -86.77438362644001302, 99.17411849586700612, -86.49847958357699440 ) ) ;
#14852=DIRECTION ( 'NONE',  ( 1.000000000000000000, 0.000000000000000000, 0.000000000000000000 ) ) ;
#14855=DIRECTION ( 'NONE',  ( 0.000000000000000000, 0.000000000000000000, 1.000000000000000000 ) ) ;
#14857=ORIENTED_EDGE ( 'NONE', *, *, #2703, .T. ) ;
#14858=DIRECTION ( 'NONE',  ( 0.000000000000000000, 0.000000000000000000, -1.000000000000000000 ) ) ;
#14862=DIRECTION ( 'NONE',  ( 0.000000000000000000, 0.000000000000000000, -1.000000000000000000 ) ) ;
#14863=DIRECTION ( 'NONE',  ( 0.000000000000000000, 0.000000000000000000, 1.000000000000000000 ) ) ;
#14864=ORIENTED_EDGE ( 'NONE', *, *, #5180, .T. ) ;
#14865=DIRECTION ( 'NONE',  ( 0.000000000000000000, 0.000000000000000000, -1.000000000000000000 ) ) ;
#14866=ORIENTED_EDGE ( 'NONE', *, *, #5955, .T. ) ;
#14867=EDGE_LOOP ( 'NONE', ( #8231, #970, #6443, #1151 ) ) ;
#14871=AXIS2_PLACEMENT_3D ( 'NONE', #5324, #437, #10040 ) ;
#14874=VECTOR ( 'NONE', #12776, 1000.000000000000000 ) ;
#14878=CARTESIAN_POINT ( 'NONE',  ( -79.11147769456633227, 68.38713492810558137, -83.44847958357698303 ) ) ;
#14885=ORIENTED_EDGE ( 'NONE', *, *, #14409, .T. ) ;
#14886=CARTESIAN_POINT ( 'NONE',  ( -69.77438362644001302, 99.17411849586700612, -81.84847958357698872 ) ) ;
#14887=EDGE_LOOP ( 'NONE', ( #3477, #8914, #11991, #9255, #1835 ) ) ;
#14888=EDGE_LOOP ( 'NONE', ( #11701, #3720, #4451, #7658 ) ) ;
#14889=ORIENTED_EDGE ( 'NONE', *, *, #1274, .F. ) ;
#14891=DIRECTION ( 'NONE',  ( 0.000000000000000000, 0.000000000000000000, 1.000000000000000000 ) ) ;
#14892=PRODUCT_DEFINITION ( 'UNKNOWN', '', #7193, #12433 ) ;
#14895=AXIS2_PLACEMENT_3D ( 'NONE', #3202, #716, #9315 ) ;
#14897=DIRECTION ( 'NONE',  ( 0.000000000000000000, 0.000000000000000000, 1.000000000000000000 ) ) ;
#14899=DIRECTION ( 'NONE',  ( 0.000000000000000000, 0.000000000000000000, 1.000000000000000000 ) ) ;
#14902=VECTOR ( 'NONE', #10063, 1000.000000000000000 ) ;
#14905=CARTESIAN_POINT ( 'NONE',  ( -52.77438362644000591, 65.17411849586700612, -86.49847958357699440 ) ) ;
#14909=CARTESIAN_POINT ( 'NONE',  ( -77.89938362643999881, 82.17411849586700612, -79.49847958357700861 ) ) ;
#14913=CIRCLE ( 'NONE', #1552, 2.699999999999993960 ) ;
#14916=DIRECTION ( 'NONE',  ( 0.000000000000000000, 0.000000000000000000, 1.000000000000000000 ) ) ;
#14918=DIRECTION ( 'NONE',  ( 1.000000000000000000, 0.000000000000000000, 0.000000000000000000 ) ) ;
#14920=ADVANCED_FACE ( 'NONE', ( #4926, #10572 ), #6474, .T. ) ;
#14921=CARTESIAN_POINT ( 'NONE',  ( -90.52438362644100778, 99.17411849586700612, -150.4984795835770228 ) ) ;
#14923=FACE_OUTER_BOUND ( 'NONE', #10775, .T. ) ;
#14925=DIRECTION ( 'NONE',  ( -0.000000000000000000, -0.000000000000000000, 1.000000000000000000 ) ) ;
#14927=VECTOR ( 'NONE', #10087, 1000.000000000000000 ) ;
#14928=CARTESIAN_POINT ( 'NONE',  ( -77.89938362643999881, 82.17411849586700612, -93.49847958357699440 ) ) ;
#14930=ORIENTED_EDGE ( 'NONE', *, *, #8298, .T. ) ;
#14933=EDGE_CURVE ( 'NONE', #9845, #4841, #9185, .T. ) ;
#14935=DIRECTION ( 'NONE',  ( -1.000000000000000000, 0.000000000000000000, 0.000000000000000000 ) ) ;
#14938=VECTOR ( 'NONE', #2171, 1000.000000000000000 ) ;
#14943=VERTEX_POINT ( 'NONE', #13221 ) ;
#14944=DIRECTION ( 'NONE',  ( 0.000000000000000000, 0.000000000000000000, 1.000000000000000000 ) ) ;
#14947=ORIENTED_EDGE ( 'NONE', *, *, #13959, .T. ) ;
#14956=AXIS2_PLACEMENT_3D ( 'NONE', #7678, #8520, #5035 ) ;
#14957=CARTESIAN_POINT ( 'NONE',  ( -86.77438362644001302, 65.17411849586700612, -152.4984795835769944 ) ) ;
#14958=VECTOR ( 'NONE', #12779, 1000.000000000000000 ) ;
#14959=DIRECTION ( 'NONE',  ( -0.000000000000000000, -1.000000000000000000, -0.000000000000000000 ) ) ;
#14960=CARTESIAN_POINT ( 'NONE',  ( -86.77438362644100778, 101.5320169952374414, -147.9984795835769944 ) ) ;
#14961=LINE ( 'NONE', #4353, #9952 ) ;
#14962=DIRECTION ( 'NONE',  ( -1.000000000000000000, 0.000000000000000000, 0.000000000000000000 ) ) ;
#14963=CARTESIAN_POINT ( 'NONE',  ( -73.51240544634549678, 65.59017466835992138, -81.84847958357697451 ) ) ;
#14966=CARTESIAN_POINT ( 'NONE',  ( -75.01311196519617397, 67.29799558322736175, -81.84847958357697451 ) ) ;
#14969=ORIENTED_EDGE ( 'NONE', *, *, #5754, .T. ) ;
#14970=EDGE_CURVE ( 'NONE', #913, #12871, #5242, .T. ) ;
#14975=LINE ( 'NONE', #12891, #13922 ) ;
#14977=CARTESIAN_POINT ( 'NONE',  ( -68.41221392010794489, 74.17411849586699191, -58.99847958357693756 ) ) ;
#14979=CARTESIAN_POINT ( 'NONE',  ( -85.75338362644100698, 100.9425423703948326, -147.9984795835769944 ) ) ;
#14980=CIRCLE ( 'NONE', #14007, 8.050000000000000711 ) ;
#14984=EDGE_CURVE ( 'NONE', #11838, #11568, #15298, .T. ) ;
#14986=ORIENTED_EDGE ( 'NONE', *, *, #8602, .T. ) ;
#14987=EDGE_CURVE ( 'NONE', #3597, #12145, #636, .T. ) ;
#14992=CIRCLE ( 'NONE', #1390, 1.250000000000001110 ) ;
#14994=DIRECTION ( 'NONE',  ( 0.8660254037844387076, 0.4999999999999998890, 0.000000000000000000 ) ) ;
#14995=DIRECTION ( 'NONE',  ( 1.000000000000000000, 0.000000000000000000, 0.000000000000000000 ) ) ;
#14997=CARTESIAN_POINT ( 'NONE',  ( -52.77438362644000591, 65.17411849586700612, -152.4984795835769944 ) ) ;
#14998=AXIS2_PLACEMENT_3D ( 'NONE', #12320, #1685, #12088 ) ;
#15000=EDGE_CURVE ( 'NONE', #7286, #3237, #11675, .T. ) ;
#15002=AXIS2_PLACEMENT_3D ( 'NONE', #9740, #7591, #8428 ) ;
#15005=DIRECTION ( 'NONE',  ( 0.000000000000000000, 0.000000000000000000, -1.000000000000000000 ) ) ;
#15007=ORIENTED_EDGE ( 'NONE', *, *, #2411, .F. ) ;
#15010=DIRECTION ( 'NONE',  ( 0.000000000000000000, -0.000000000000000000, 1.000000000000000000 ) ) ;
#15011=VECTOR ( 'NONE', #10856, 1000.000000000000000 ) ;
#15012=EDGE_CURVE ( 'NONE', #14573, #8182, #9940, .T. ) ;
#15013=DIRECTION ( 'NONE',  ( 0.000000000000000000, -4.130293990420970006E-17, 1.000000000000000000 ) ) ;
#15014=DIRECTION ( 'NONE',  ( 1.000000000000000000, 0.000000000000000000, 0.000000000000000000 ) ) ;
#15015=PLANE ( 'NONE',  #10873 ) ;
#15017=CYLINDRICAL_SURFACE ( 'NONE', #12774, 8.000000000000007105 ) ;
#15019=DIRECTION ( 'NONE',  ( -1.000000000000000000, 0.000000000000000000, 0.000000000000000000 ) ) ;
#15020=ORIENTED_EDGE ( 'NONE', *, *, #13056, .F. ) ;
#15022=AXIS2_PLACEMENT_3D ( 'NONE', #1735, #5551, #5405 ) ;
#15026=ORIENTED_EDGE ( 'NONE', *, *, #2088, .F. ) ;
#15027=ADVANCED_FACE ( 'NONE', ( #13534 ), #11183, .F. ) ;
#15035=CARTESIAN_POINT ( 'NONE',  ( -69.77438362644001302, 82.17411849586700612, -182.1969643934119745 ) ) ;
#15036=CARTESIAN_POINT ( 'NONE',  ( -69.77438362644001302, 82.17411849586700612, -80.44847958357698303 ) ) ;
#15037=AXIS2_PLACEMENT_3D ( 'NONE', #6540, #4200, #1714 ) ;
#15039=CARTESIAN_POINT ( 'NONE',  ( -52.77438362643999881, 62.81621999649657084, -147.9984795835769944 ) ) ;
#15043=ORIENTED_EDGE ( 'NONE', *, *, #10855, .T. ) ;
#15047=ORIENTED_EDGE ( 'NONE', *, *, #7879, .F. ) ;
#15052=CARTESIAN_POINT ( 'NONE',  ( -84.73238362644100619, 100.3530677455522238, -147.9984795835769944 ) ) ;
#15056=DIRECTION ( 'NONE',  ( 0.000000000000000000, 0.000000000000000000, 1.000000000000000000 ) ) ;
#15057=PLANE ( 'NONE',  #4308 ) ;
#15060=ORIENTED_EDGE ( 'NONE', *, *, #12279, .T. ) ;
#15061=LINE ( 'NONE', #1106, #4154 ) ;
#15064=PLANE ( 'NONE',  #11170 ) ;
#15065=ORIENTED_EDGE ( 'NONE', *, *, #8100, .F. ) ;
#15069=AXIS2_PLACEMENT_3D ( 'NONE', #7512, #13477, #443 ) ;
#15070=CARTESIAN_POINT ( 'NONE',  ( -73.80978675135780520, 64.78624853950366003, -83.44847958357698303 ) ) ;
#15072=DIRECTION ( 'NONE',  ( 0.000000000000000000, 0.000000000000000000, 1.000000000000000000 ) ) ;
#15074=ADVANCED_FACE ( 'NONE', ( #4061 ), #10182, .T. ) ;
#15078=ORIENTED_EDGE ( 'NONE', *, *, #14604, .T. ) ;
#15081=ORIENTED_EDGE ( 'NONE', *, *, #3273, .F. ) ;
#15082=EDGE_CURVE ( 'NONE', #5950, #10374, #3418, .T. ) ;
#15085=EDGE_CURVE ( 'NONE', #11568, #1588, #11438, .T. ) ;
#15086=FACE_OUTER_BOUND ( 'NONE', #10320, .T. ) ;
#15087=DIRECTION ( 'NONE',  ( 0.000000000000000000, 1.000000000000000000, 0.000000000000000000 ) ) ;
#15088=DIRECTION ( 'NONE',  ( 1.000000000000000000, 0.000000000000000000, 0.000000000000000000 ) ) ;
#15092=DIRECTION ( 'NONE',  ( 1.000000000000000000, 0.000000000000000000, 0.000000000000000000 ) ) ;
#15094=EDGE_CURVE ( 'NONE', #10111, #384, #12133, .T. ) ;
#15095=ORIENTED_EDGE ( 'NONE', *, *, #1356, .F. ) ;
#15097=EDGE_CURVE ( 'NONE', #11360, #858, #1502, .T. ) ;
#15098=ORIENTED_EDGE ( 'NONE', *, *, #13156, .F. ) ;
#15105=DIRECTION ( 'NONE',  ( 0.000000000000000000, -0.000000000000000000, 1.000000000000000000 ) ) ;
#15110=CARTESIAN_POINT ( 'NONE',  ( -86.77438362644001302, 65.17411849586700612, -145.4984795835769660 ) ) ;
#15111=CARTESIAN_POINT ( 'NONE',  ( -37.27438362644220149, 104.6741184958692088, -79.59847958357700293 ) ) ;
#15112=PLANE ( 'NONE',  #8749 ) ;
#15113=ORIENTED_EDGE ( 'NONE', *, *, #11417, .T. ) ;
#15114=CARTESIAN_POINT ( 'NONE',  ( -69.77438362644001302, 82.17411849586700612, -80.14847958357698587 ) ) ;
#15117=ORIENTED_EDGE ( 'NONE', *, *, #5038, .T. ) ;
#15119=FACE_BOUND ( 'NONE', #1632, .T. ) ;
#15121=ADVANCED_FACE ( 'NONE', ( #10472 ), #15199, .F. ) ;
#15122=CARTESIAN_POINT ( 'NONE',  ( -82.52438362644100778, 99.17411849586700612, -182.2484795835770228 ) ) ;
#15123=CARTESIAN_POINT ( 'NONE',  ( -48.52438362644100067, 99.17411849586700612, -145.4984795835769944 ) ) ;
#15125=DIRECTION ( 'NONE',  ( -1.000000000000000000, 0.000000000000000000, 0.000000000000000000 ) ) ;
#15126=VECTOR ( 'NONE', #1599, 1000.000000000000114 ) ;
#15127=DIRECTION ( 'NONE',  ( -0.8660254037844387076, -0.4999999999999998890, 0.000000000000000000 ) ) ;
#15128=DIRECTION ( 'NONE',  ( 0.000000000000000000, 0.000000000000000000, -1.000000000000000000 ) ) ;
#15130=VECTOR ( 'NONE', #4225, 1000.000000000000000 ) ;
#15131=VERTEX_POINT ( 'NONE', #10239 ) ;
#15133=VERTEX_POINT ( 'NONE', #12518 ) ;
#15135=LINE ( 'NONE', #3362, #5002 ) ;
#15136=ORIENTED_EDGE ( 'NONE', *, *, #5666, .T. ) ;
#15137=VECTOR ( 'NONE', #3753, 1000.000000000000000 ) ;
#15141=( GEOMETRIC_REPRESENTATION_CONTEXT ( 3 ) GLOBAL_UNCERTAINTY_ASSIGNED_CONTEXT ( ( #1724 ) ) GLOBAL_UNIT_ASSIGNED_CONTEXT ( ( #10709, #12974, #161 ) ) REPRESENTATION_CONTEXT ( 'NONE', 'WORKASPACE' ) );
#15142=DIRECTION ( 'NONE',  ( 0.000000000000000000, 0.000000000000000000, 1.000000000000000000 ) ) ;
#15144=CARTESIAN_POINT ( 'NONE',  ( -67.09329877327367342, 89.83357606928383632, -58.65793715699378197 ) ) ;
#15146=CIRCLE ( 'NONE', #14412, 4.250000000000003553 ) ;
#15147=DIRECTION ( 'NONE',  ( 1.000000000000000000, 0.000000000000000000, 0.000000000000000000 ) ) ;
#15148=VERTEX_POINT ( 'NONE', #4363 ) ;
#15151=AXIS2_PLACEMENT_3D ( 'NONE', #8319, #13976, #14058 ) ;
#15152=ORIENTED_EDGE ( 'NONE', *, *, #15012, .F. ) ;
#15153=DIRECTION ( 'NONE',  ( 0.000000000000000000, 0.000000000000000000, 1.000000000000000000 ) ) ;
#15155=ORIENTED_EDGE ( 'NONE', *, *, #9961, .T. ) ;
#15156=EDGE_CURVE ( 'NONE', #3619, #8760, #13174, .T. ) ;
#15159=CARTESIAN_POINT ( 'NONE',  ( -50.27438362644099357, 99.17411849586700612, -182.2484795835770228 ) ) ;
#15162=DIRECTION ( 'NONE',  ( 0.000000000000000000, -1.000000000000000000, 0.000000000000000000 ) ) ;
#15165=VECTOR ( 'NONE', #8891, 1000.000000000000114 ) ;
#15170=EDGE_LOOP ( 'NONE', ( #9046, #4777 ) ) ;
#15171=EDGE_LOOP ( 'NONE', ( #5614, #10295, #4414, #1692, #11796 ) ) ;
#15175=VECTOR ( 'NONE', #5880, 1000.000000000000000 ) ;
#15176=ADVANCED_FACE ( 'NONE', ( #6926 ), #1955, .F. ) ;
#15178=EDGE_LOOP ( 'NONE', ( #470, #12454 ) ) ;
#15184=LINE ( 'NONE', #12878, #9725 ) ;
#15185=LINE ( 'NONE', #9216, #11317 ) ;
#15187=DIRECTION ( 'NONE',  ( -1.000000000000000000, 0.000000000000000000, 0.000000000000000000 ) ) ;
#15188=LINE ( 'NONE', #10698, #14011 ) ;
#15189=AXIS2_PLACEMENT_3D ( 'NONE', #11052, #5166, #8714 ) ;
#15190=AXIS2_PLACEMENT_3D ( 'NONE', #11314, #14865, #1626 ) ;
#15195=ORIENTED_EDGE ( 'NONE', *, *, #2292, .F. ) ;
#15196=ORIENTED_EDGE ( 'NONE', *, *, #2029, .T. ) ;
#15197=ORIENTED_EDGE ( 'NONE', *, *, #3942, .T. ) ;
#15198=EDGE_CURVE ( 'NONE', #9914, #5515, #6267, .T. ) ;
#15199=PLANE ( 'NONE',  #13431 ) ;
#15201=AXIS2_PLACEMENT_3D ( 'NONE', #5039, #14568, #14487 ) ;
#15202=CARTESIAN_POINT ( 'NONE',  ( -50.27438362644100067, 59.67411849586700612, -79.59847958357700293 ) ) ;
#15204=CARTESIAN_POINT ( 'NONE',  ( -59.02799568714584666, 164.3482369917340122, -73.34256232478206528 ) ) ;
#15205=CARTESIAN_POINT ( 'NONE',  ( -86.77438362644001302, 99.17411849586700612, -86.49847958357699440 ) ) ;
#15210=LINE ( 'NONE', #6244, #1572 ) ;
#15211=ORIENTED_EDGE ( 'NONE', *, *, #14333, .T. ) ;
#15213=AXIS2_PLACEMENT_3D ( 'NONE', #7222, #1312, #6076 ) ;
#15214=AXIS2_PLACEMENT_3D ( 'NONE', #13329, #2606, #11073 ) ;
#15220=EDGE_CURVE ( 'NONE', #15299, #10086, #780, .T. ) ;
#15222=ORIENTED_EDGE ( 'NONE', *, *, #2619, .F. ) ;
#15225=DIRECTION ( 'NONE',  ( 0.000000000000000000, 0.000000000000000000, -1.000000000000000000 ) ) ;
#15227=CARTESIAN_POINT ( 'NONE',  ( -88.81638362644000040, 63.99516924618178848, -147.9984795835769944 ) ) ;
#15229=CARTESIAN_POINT ( 'NONE',  ( -69.77438362644001302, 82.17411849586700612, -29.37106258560738681 ) ) ;
#15230=ORIENTED_EDGE ( 'NONE', *, *, #40, .F. ) ;
#15232=LINE ( 'NONE', #11836, #4277 ) ;
#15233=AXIS2_PLACEMENT_3D ( 'NONE', #1983, #6811, #11452 ) ;
#15234=ORIENTED_EDGE ( 'NONE', *, *, #4142, .F. ) ;
#15237=VERTEX_POINT ( 'NONE', #5620 ) ;
#15243=VECTOR ( 'NONE', #12910, 1000.000000000000000 ) ;
#15248=FACE_OUTER_BOUND ( 'NONE', #177, .T. ) ;
#15249=ORIENTED_EDGE ( 'NONE', *, *, #5742, .T. ) ;
#15250=CARTESIAN_POINT ( 'NONE',  ( -86.77438362644100778, 99.17411849586700612, -145.4984795835769944 ) ) ;
#15253=ORIENTED_EDGE ( 'NONE', *, *, #5432, .T. ) ;
#15256=EDGE_LOOP ( 'NONE', ( #2513, #5923, #10236, #10156 ) ) ;
#15260=LINE ( 'NONE', #9598, #14778 ) ;
#15262=ADVANCED_FACE ( 'NONE', ( #4438 ), #12734, .F. ) ;
#15265=DIRECTION ( 'NONE',  ( 0.000000000000000000, 0.000000000000000000, -1.000000000000000000 ) ) ;
#15267=FACE_OUTER_BOUND ( 'NONE', #7119, .T. ) ;
#15269=EDGE_CURVE ( 'NONE', #13375, #11145, #2102, .T. ) ;
#15272=AXIS2_PLACEMENT_3D ( 'NONE', #1415, #6173, #2651 ) ;
#15273=VERTEX_POINT ( 'NONE', #5765 ) ;
#15274=DIRECTION ( 'NONE',  ( -1.000000000000000000, 0.000000000000000000, 0.000000000000000000 ) ) ;
#15275=ORIENTED_EDGE ( 'NONE', *, *, #14316, .T. ) ;
#15278=CARTESIAN_POINT ( 'NONE',  ( -86.77438362644100778, 101.5320169952374414, -147.9984795835769944 ) ) ;
#15280=CIRCLE ( 'NONE', #12082, 2.500000000000002220 ) ;
#15281=DIRECTION ( 'NONE',  ( -1.000000000000000000, 1.287488025362404182E-15, 0.000000000000000000 ) ) ;
#15282=DIRECTION ( 'NONE',  ( 0.7071067811865474617, 0.000000000000000000, 0.7071067811865474617 ) ) ;
#15283=PLANE ( 'NONE',  #2533 ) ;
#15284=ADVANCED_FACE ( 'NONE', ( #15119, #1880 ), #6634, .T. ) ;
#15285=DIRECTION ( 'NONE',  ( 1.224646799147351975E-16, 1.000000000000000000, 0.000000000000000000 ) ) ;
#15286=LINE ( 'NONE', #7865, #8367 ) ;
#15287=DIRECTION ( 'NONE',  ( 0.000000000000000000, 0.000000000000000000, -1.000000000000000000 ) ) ;
#15288=FACE_OUTER_BOUND ( 'NONE', #12989, .T. ) ;
#15290=CARTESIAN_POINT ( 'NONE',  ( -55.52438362644000591, 65.17411849586700612, -145.4984795835769660 ) ) ;
#15295=ORIENTED_EDGE ( 'NONE', *, *, #319, .T. ) ;
#15297=ADVANCED_FACE ( 'NONE', ( #5846 ), #2481, .F. ) ;
#15298=LINE ( 'NONE', #2351, #13906 ) ;
#15299=VERTEX_POINT ( 'NONE', #8313 ) ;
#15300=EDGE_CURVE ( 'NONE', #3363, #12177, #6752, .T. ) ;
#15305=CARTESIAN_POINT ( 'NONE',  ( -52.77438362644000591, 99.17411849586700612, -79.59847958357700293 ) ) ;
#15310=CARTESIAN_POINT ( 'NONE',  ( -55.27438362643999881, 65.17411849586700612, -182.2484795835770228 ) ) ;
#15312=ORIENTED_EDGE ( 'NONE', *, *, #2228, .F. ) ;
#15313=AXIS2_PLACEMENT_3D ( 'NONE', #9426, #11924, #7047 ) ;
#15314=FILL_AREA_STYLE_COLOUR ( '', #10283 ) ;
#15316=EDGE_LOOP ( 'NONE', ( #2873, #6950 ) ) ;
#15318=EDGE_CURVE ( 'NONE', #8134, #9846, #10795, .T. ) ;
#15319=CARTESIAN_POINT ( 'NONE',  ( -47.27438362644100778, 57.67411849586700612, -67.49847958357700861 ) ) ;
#15321=DIRECTION ( 'NONE',  ( -0.3469356515732558988, 0.9378889346118975956, 0.000000000000000000 ) ) ;
#15325=ORIENTED_EDGE ( 'NONE', *, *, #4710, .T. ) ;
#15326=CARTESIAN_POINT ( 'NONE',  ( -102.2743836264409936, 62.67411849586699901, -79.59847958357700293 ) ) ;
#15330=VERTEX_POINT ( 'NONE', #9387 ) ;
#15331=ORIENTED_EDGE ( 'NONE', *, *, #15094, .F. ) ;
#15332=ORIENTED_EDGE ( 'NONE', *, *, #7712, .T. ) ;
ENDSEC;
END-ISO-10303-21;
